ISO-10303-21;
HEADER;
/* Generated by software containing ST-Developer
 * from STEP Tools, Inc. (www.steptools.com) 
 */

FILE_DESCRIPTION(
/* description */ (''),
/* implementation_level */ '2;1');

FILE_NAME(
/* name */ 'Moving_Carriage_01.step',
/* time_stamp */ '2026-10-22T13:39:42+06:00',
/* author */ (''),
/* organization */ (''),
/* preprocessor_version */ 'ST-DEVELOPER v20.2',
/* originating_system */ 'Autodesk Translation Framework v15.15.0.0',
/* authorisation */ '');

FILE_SCHEMA (('AUTOMOTIVE_DESIGN { 1 0 10303 214 3 1 1 }'));
ENDSEC;

DATA;
#10=MECHANICAL_DESIGN_GEOMETRIC_PRESENTATION_REPRESENTATION('',(#312),#17836);
#51=B_SPLINE_CURVE_WITH_KNOTS('',3,(#15627,#15628,#15629,#15630,#15631,
#15632,#15633,#15634,#15635,#15636),.UNSPECIFIED.,.F.,.F.,(4,2,2,2,4),(0.150795783066297,
0.169644465291242,0.188493147516186,0.207360358779659,0.226227570043131),
 .UNSPECIFIED.);
#52=B_SPLINE_CURVE_WITH_KNOTS('',3,(#15640,#15641,#15642,#15643,#15644,
#15645,#15646,#15647,#15648,#15649),.UNSPECIFIED.,.F.,.F.,(4,2,2,2,4),(0.0757694987047649,
0.0947120945274103,0.113654690350056,0.1325089994291,0.151363308508144),
 .UNSPECIFIED.);
#53=B_SPLINE_CURVE_WITH_KNOTS('',3,(#15653,#15654,#15655,#15656,#15657,
#15658,#15659,#15660,#15661,#15662),.UNSPECIFIED.,.F.,.F.,(4,2,2,2,4),(0.151363299946195,
0.170217609025239,0.189071918104283,0.208014513926928,0.226957109749574),
 .UNSPECIFIED.);
#54=B_SPLINE_CURVE_WITH_KNOTS('',3,(#15666,#15667,#15668,#15669,#15670,
#15671,#15672,#15673,#15674,#15675),.UNSPECIFIED.,.F.,.F.,(4,2,2,2,4),(0.0753639993742339,
0.0942312106377064,0.113098421901179,0.131947104126123,0.150795786351068),
 .UNSPECIFIED.);
#55=B_SPLINE_CURVE_WITH_KNOTS('',3,(#15742,#15743,#15744,#15745,#15746,
#15747,#15748,#15749,#15750,#15751),.UNSPECIFIED.,.F.,.F.,(4,2,2,2,4),(0.161501820430177,
0.181202019666624,0.200902218903071,0.22218706551677,0.243471912130469),
 .UNSPECIFIED.);
#56=B_SPLINE_CURVE_WITH_KNOTS('',3,(#15755,#15756,#15757,#15758,#15759,
#15760,#15761,#15762,#15763,#15764),.UNSPECIFIED.,.F.,.F.,(4,2,2,2,4),(0.0930675005857176,
0.116580531967157,0.140093563348597,0.159964165564683,0.179834767780769),
 .UNSPECIFIED.);
#57=B_SPLINE_CURVE_WITH_KNOTS('',3,(#15768,#15769,#15770,#15771,#15772,
#15773,#15774,#15775,#15776,#15777),.UNSPECIFIED.,.F.,.F.,(4,2,2,2,4),(0.179821549944371,
0.199692152160457,0.219562754376543,0.243075785757983,0.266588817139422),
 .UNSPECIFIED.);
#58=B_SPLINE_CURVE_WITH_KNOTS('',3,(#15780,#15781,#15782,#15783,#15784,
#15785,#15786,#15787,#15788,#15789),.UNSPECIFIED.,.F.,.F.,(4,2,2,2,4),(0.0795500677920486,
0.100834914405747,0.122119761019446,0.141819960255893,0.16152015949234),
 .UNSPECIFIED.);
#59=B_SPLINE_CURVE_WITH_KNOTS('',3,(#15810,#15811,#15812,#15813,#15814,
#15815,#15816,#15817,#15818,#15819),.UNSPECIFIED.,.F.,.F.,(4,2,2,2,4),(0.150807296394123,
0.169656833408643,0.188506370423163,0.207379164314979,0.226251958206795),
 .UNSPECIFIED.);
#60=B_SPLINE_CURVE_WITH_KNOTS('',3,(#15822,#15823,#15824,#15825,#15826,
#15827,#15828,#15829,#15830,#15831),.UNSPECIFIED.,.F.,.F.,(4,2,2,2,4),(-0.0760046501525728,
-0.0568078920652052,-0.0376111339778377,-0.0188055669889188,0.),
 .UNSPECIFIED.);
#61=B_SPLINE_CURVE_WITH_KNOTS('',3,(#15833,#15834,#15835,#15836,#15837,
#15838,#15839,#15840,#15841,#15842),.UNSPECIFIED.,.F.,.F.,(4,2,2,2,4),(0.,
0.0188055669889188,0.0376111339778377,0.0568078920652052,0.0760046501525728),
 .UNSPECIFIED.);
#62=B_SPLINE_CURVE_WITH_KNOTS('',3,(#15846,#15847,#15848,#15849,#15850,
#15851,#15852,#15853,#15854,#15855),.UNSPECIFIED.,.F.,.F.,(4,2,2,2,4),(0.0753626345814508,
0.0942354284732671,0.113108222365083,0.131957759379603,0.150807296394123),
 .UNSPECIFIED.);
#63=B_SPLINE_CURVE_WITH_KNOTS('',3,(#15871,#15872,#15873,#15874,#15875,
#15876,#15877,#15878,#15879,#15880),.UNSPECIFIED.,.F.,.F.,(4,2,2,2,4),(0.150807296394123,
0.169656833408643,0.188506370423163,0.207379164314979,0.226251958206795),
 .UNSPECIFIED.);
#64=B_SPLINE_CURVE_WITH_KNOTS('',3,(#15883,#15884,#15885,#15886,#15887,
#15888,#15889,#15890,#15891,#15892),.UNSPECIFIED.,.F.,.F.,(4,2,2,2,4),(-0.0760046501525727,
-0.0568078920652052,-0.0376111339778377,-0.0188055669889188,0.),
 .UNSPECIFIED.);
#65=B_SPLINE_CURVE_WITH_KNOTS('',3,(#15894,#15895,#15896,#15897,#15898,
#15899,#15900,#15901,#15902,#15903),.UNSPECIFIED.,.F.,.F.,(4,2,2,2,4),(0.,
0.0188055669889188,0.0376111339778377,0.0568078920652052,0.0760046501525728),
 .UNSPECIFIED.);
#66=B_SPLINE_CURVE_WITH_KNOTS('',3,(#15907,#15908,#15909,#15910,#15911,
#15912,#15913,#15914,#15915,#15916),.UNSPECIFIED.,.F.,.F.,(4,2,2,2,4),(0.0753626345814508,
0.0942354284732671,0.113108222365083,0.131957759379603,0.150807296394123),
 .UNSPECIFIED.);
#67=B_SPLINE_CURVE_WITH_KNOTS('',3,(#15932,#15933,#15934,#15935,#15936,
#15937,#15938,#15939,#15940,#15941),.UNSPECIFIED.,.F.,.F.,(4,2,2,2,4),(0.150807296394123,
0.169656833408643,0.188506370423163,0.207379164314979,0.226251958206795),
 .UNSPECIFIED.);
#68=B_SPLINE_CURVE_WITH_KNOTS('',3,(#15944,#15945,#15946,#15947,#15948,
#15949,#15950,#15951,#15952,#15953),.UNSPECIFIED.,.F.,.F.,(4,2,2,2,4),(-0.0760046501525728,
-0.0568078920652053,-0.0376111339778377,-0.0188055669889188,0.),
 .UNSPECIFIED.);
#69=B_SPLINE_CURVE_WITH_KNOTS('',3,(#15955,#15956,#15957,#15958,#15959,
#15960,#15961,#15962,#15963,#15964),.UNSPECIFIED.,.F.,.F.,(4,2,2,2,4),(0.,
0.0188055669889189,0.0376111339778377,0.0568078920652053,0.0760046501525728),
 .UNSPECIFIED.);
#70=B_SPLINE_CURVE_WITH_KNOTS('',3,(#15968,#15969,#15970,#15971,#15972,
#15973,#15974,#15975,#15976,#15977),.UNSPECIFIED.,.F.,.F.,(4,2,2,2,4),(0.0753626345814508,
0.0942354284732671,0.113108222365083,0.131957759379603,0.150807296394123),
 .UNSPECIFIED.);
#71=B_SPLINE_CURVE_WITH_KNOTS('',3,(#15990,#15991,#15992,#15993,#15994,
#15995,#15996,#15997,#15998,#15999),.UNSPECIFIED.,.F.,.F.,(4,2,2,2,4),(0.161501820430177,
0.181202019666624,0.200902218903071,0.22218706551677,0.243471912130469),
 .UNSPECIFIED.);
#72=B_SPLINE_CURVE_WITH_KNOTS('',3,(#16003,#16004,#16005,#16006,#16007,
#16008,#16009,#16010,#16011,#16012),.UNSPECIFIED.,.F.,.F.,(4,2,2,2,4),(0.0930675005857173,
0.116580531967157,0.140093563348596,0.159964165564682,0.179834767780769),
 .UNSPECIFIED.);
#73=B_SPLINE_CURVE_WITH_KNOTS('',3,(#16016,#16017,#16018,#16019,#16020,
#16021,#16022,#16023,#16024,#16025),.UNSPECIFIED.,.F.,.F.,(4,2,2,2,4),(0.17982154994437,
0.199692152160456,0.219562754376542,0.243075785757982,0.266588817139421),
 .UNSPECIFIED.);
#74=B_SPLINE_CURVE_WITH_KNOTS('',3,(#16028,#16029,#16030,#16031,#16032,
#16033,#16034,#16035,#16036,#16037),.UNSPECIFIED.,.F.,.F.,(4,2,2,2,4),(0.0795500677920484,
0.100834914405747,0.122119761019446,0.141819960255893,0.16152015949234),
 .UNSPECIFIED.);
#75=B_SPLINE_CURVE_WITH_KNOTS('',3,(#16052,#16053,#16054,#16055,#16056,
#16057,#16058,#16059,#16060,#16061),.UNSPECIFIED.,.F.,.F.,(4,2,2,2,4),(0.150807296394123,
0.169656833408643,0.188506370423163,0.207379164314979,0.226251958206795),
 .UNSPECIFIED.);
#76=B_SPLINE_CURVE_WITH_KNOTS('',3,(#16064,#16065,#16066,#16067,#16068,
#16069,#16070,#16071,#16072,#16073),.UNSPECIFIED.,.F.,.F.,(4,2,2,2,4),(-0.0760046501525727,
-0.0568078920652052,-0.0376111339778377,-0.0188055669889188,0.),
 .UNSPECIFIED.);
#77=B_SPLINE_CURVE_WITH_KNOTS('',3,(#16075,#16076,#16077,#16078,#16079,
#16080,#16081,#16082,#16083,#16084),.UNSPECIFIED.,.F.,.F.,(4,2,2,2,4),(0.,
0.0188055669889188,0.0376111339778377,0.0568078920652052,0.0760046501525727),
 .UNSPECIFIED.);
#78=B_SPLINE_CURVE_WITH_KNOTS('',3,(#16088,#16089,#16090,#16091,#16092,
#16093,#16094,#16095,#16096,#16097),.UNSPECIFIED.,.F.,.F.,(4,2,2,2,4),(0.0753626345814508,
0.0942354284732671,0.113108222365083,0.131957759379603,0.150807296394123),
 .UNSPECIFIED.);
#79=B_SPLINE_CURVE_WITH_KNOTS('',3,(#16107,#16108,#16109,#16110,#16111,
#16112,#16113,#16114,#16115,#16116),.UNSPECIFIED.,.F.,.F.,(4,2,2,2,4),(0.154001562562628,
0.172841700119288,0.191681837675949,0.211603838452167,0.231525839228385),
 .UNSPECIFIED.);
#80=B_SPLINE_CURVE_WITH_KNOTS('',3,(#16120,#16121,#16122,#16123,#16124,
#16125,#16126,#16127,#16128,#16129),.UNSPECIFIED.,.F.,.F.,(4,2,2,2,4),(-0.0796560912226912,
-0.0585074655832388,-0.0373588399437865,-0.0186794199718932,0.),
 .UNSPECIFIED.);
#81=B_SPLINE_CURVE_WITH_KNOTS('',3,(#16133,#16134,#16135,#16136,#16137,
#16138,#16139,#16140,#16141,#16142),.UNSPECIFIED.,.F.,.F.,(4,2,2,2,4),(0.,
0.0186794199718932,0.0373588399437865,0.0585074655832388,0.0796560912226912),
 .UNSPECIFIED.);
#82=B_SPLINE_CURVE_WITH_KNOTS('',3,(#16146,#16147,#16148,#16149,#16150,
#16151,#16152,#16153,#16154,#16155),.UNSPECIFIED.,.F.,.F.,(4,2,2,2,4),(0.0764772858968706,
0.0963992866730888,0.116321287449307,0.135161425005967,0.154001562562628),
 .UNSPECIFIED.);
#83=B_SPLINE_CURVE_WITH_KNOTS('',3,(#16159,#16160,#16161,#16162,#16163,
#16164,#16165,#16166,#16167,#16168,#16169,#16170,#16171,#16172,#16173,#16174,
#16175,#16176,#16177,#16178,#16179),.UNSPECIFIED.,.F.,.F.,(4,2,2,2,3,2,
2,2,2,4),(-0.0487654213288014,-0.0396424658283718,-0.0198212329141859,-0.00991061645709296,
0.,0.00991061645709312,0.0198212329141862,0.0396424658283725,0.0754755088146795,
0.111308551800987),.UNSPECIFIED.);
#84=B_SPLINE_CURVE_WITH_KNOTS('',3,(#16183,#16184,#16185,#16186,#16187,
#16188,#16189,#16190,#16191,#16192,#16193,#16194,#16195,#16196,#16197,#16198),
 .UNSPECIFIED.,.F.,.F.,(4,2,2,2,2,2,2,4),(0.080261889411958,0.100728357288421,
0.121194825164885,0.139914688841483,0.158634552518082,0.177354416194681,
0.19607427987128,0.196799093526934),.UNSPECIFIED.);
#85=B_SPLINE_CURVE_WITH_KNOTS('',3,(#16202,#16203,#16204,#16205,#16206,
#16207,#16208,#16209,#16210,#16211,#16212,#16213,#16214,#16215,#16216,#16217),
 .UNSPECIFIED.,.F.,.F.,(4,2,2,2,2,2,2,4),(0.120470011509229,0.121194825164884,
0.139914688841482,0.158634552518081,0.17735441619468,0.196074279871279,
0.216540747747742,0.237007215624205),.UNSPECIFIED.);
#86=B_SPLINE_CURVE_WITH_KNOTS('',3,(#16221,#16222,#16223,#16224,#16225,
#16226,#16227,#16228,#16229,#16230,#16231,#16232,#16233,#16234,#16235,#16236,
#16237,#16238,#16239,#16240,#16241),.UNSPECIFIED.,.F.,.F.,(4,2,2,2,2,3,
2,2,2,4),(-0.111308551800987,-0.0754755088146795,-0.0396424658283724,-0.0198212329141862,
-0.00991061645709312,0.,0.00991061645709295,0.0198212329141859,0.0396424658283718,
0.0487654212438806),.UNSPECIFIED.);
#87=B_SPLINE_CURVE_WITH_KNOTS('',3,(#16251,#16252,#16253,#16254,#16255,
#16256,#16257,#16258,#16259,#16260),.UNSPECIFIED.,.F.,.F.,(4,2,2,2,4),(0.150795783066297,
0.169644465291242,0.188493147516186,0.207360358779658,0.226227570043131),
 .UNSPECIFIED.);
#88=B_SPLINE_CURVE_WITH_KNOTS('',3,(#16263,#16264,#16265,#16266,#16267,
#16268,#16269,#16270,#16271,#16272),.UNSPECIFIED.,.F.,.F.,(4,2,2,2,4),(0.0757694987047649,
0.0947120945274103,0.113654690350056,0.1325089994291,0.151363308508144),
 .UNSPECIFIED.);
#89=B_SPLINE_CURVE_WITH_KNOTS('',3,(#16274,#16275,#16276,#16277,#16278,
#16279,#16280,#16281,#16282,#16283),.UNSPECIFIED.,.F.,.F.,(4,2,2,2,4),(0.151363299946195,
0.170217609025239,0.189071918104283,0.208014513926928,0.226957109749573),
 .UNSPECIFIED.);
#90=B_SPLINE_CURVE_WITH_KNOTS('',3,(#16287,#16288,#16289,#16290,#16291,
#16292,#16293,#16294,#16295,#16296),.UNSPECIFIED.,.F.,.F.,(4,2,2,2,4),(0.075363999374234,
0.0942312106377065,0.113098421901179,0.131947104126123,0.150795786351068),
 .UNSPECIFIED.);
#91=B_SPLINE_CURVE_WITH_KNOTS('',3,(#16306,#16307,#16308,#16309,#16310,
#16311,#16312,#16313,#16314,#16315),.UNSPECIFIED.,.F.,.F.,(4,2,2,2,4),(0.154001562562628,
0.172841700119289,0.191681837675949,0.211603838452167,0.231525839228385),
 .UNSPECIFIED.);
#92=B_SPLINE_CURVE_WITH_KNOTS('',3,(#16319,#16320,#16321,#16322,#16323,
#16324,#16325,#16326,#16327,#16328),.UNSPECIFIED.,.F.,.F.,(4,2,2,2,4),(-0.0796560912226911,
-0.0585074655832388,-0.0373588399437865,-0.0186794199718933,0.),
 .UNSPECIFIED.);
#93=B_SPLINE_CURVE_WITH_KNOTS('',3,(#16332,#16333,#16334,#16335,#16336,
#16337,#16338,#16339,#16340,#16341),.UNSPECIFIED.,.F.,.F.,(4,2,2,2,4),(0.,
0.0186794199718933,0.0373588399437865,0.0585074655832388,0.0796560912226911),
 .UNSPECIFIED.);
#94=B_SPLINE_CURVE_WITH_KNOTS('',3,(#16345,#16346,#16347,#16348,#16349,
#16350,#16351,#16352,#16353,#16354),.UNSPECIFIED.,.F.,.F.,(4,2,2,2,4),(0.0764772858968706,
0.0963992866730888,0.116321287449307,0.135161425005967,0.154001562562628),
 .UNSPECIFIED.);
#95=B_SPLINE_CURVE_WITH_KNOTS('',3,(#16358,#16359,#16360,#16361,#16362,
#16363,#16364,#16365,#16366,#16367,#16368,#16369,#16370,#16371,#16372,#16373,
#16374,#16375,#16376,#16377,#16378),.UNSPECIFIED.,.F.,.F.,(4,2,2,2,3,2,
2,2,2,4),(-0.0487654213288006,-0.0396424658283715,-0.0198212329141857,-0.00991061645709285,
0.,0.00991061645709304,0.0198212329141861,0.0396424658283721,0.0754755088146788,
0.111308551800986),.UNSPECIFIED.);
#96=B_SPLINE_CURVE_WITH_KNOTS('',3,(#16382,#16383,#16384,#16385,#16386,
#16387,#16388,#16389,#16390,#16391,#16392,#16393,#16394,#16395,#16396,#16397),
 .UNSPECIFIED.,.F.,.F.,(4,2,2,2,2,2,2,4),(0.080261889411958,0.100728357288421,
0.121194825164885,0.139914688841484,0.158634552518082,0.177354416194681,
0.19607427987128,0.196799093526934),.UNSPECIFIED.);
#97=B_SPLINE_CURVE_WITH_KNOTS('',3,(#16401,#16402,#16403,#16404,#16405,
#16406,#16407,#16408,#16409,#16410,#16411,#16412,#16413,#16414,#16415,#16416),
 .UNSPECIFIED.,.F.,.F.,(4,2,2,2,2,2,2,4),(0.120470011509229,0.121194825164884,
0.139914688841482,0.158634552518081,0.17735441619468,0.196074279871279,
0.216540747747742,0.237007215624205),.UNSPECIFIED.);
#98=B_SPLINE_CURVE_WITH_KNOTS('',3,(#16420,#16421,#16422,#16423,#16424,
#16425,#16426,#16427,#16428,#16429,#16430,#16431,#16432,#16433,#16434,#16435,
#16436,#16437,#16438,#16439,#16440),.UNSPECIFIED.,.F.,.F.,(4,2,2,2,2,3,
2,2,2,4),(-0.111308551800986,-0.0754755088146788,-0.0396424658283722,-0.0198212329141861,
-0.00991061645709307,0.,0.00991061645709287,0.0198212329141857,0.0396424658283715,
0.0487654212438799),.UNSPECIFIED.);
#99=B_SPLINE_CURVE_WITH_KNOTS('',3,(#16450,#16451,#16452,#16453,#16454,
#16455,#16456,#16457,#16458,#16459),.UNSPECIFIED.,.F.,.F.,(4,2,2,2,4),(0.154001562562628,
0.172841700119288,0.191681837675949,0.211603838452167,0.231525839228385),
 .UNSPECIFIED.);
#100=B_SPLINE_CURVE_WITH_KNOTS('',3,(#16463,#16464,#16465,#16466,#16467,
#16468,#16469,#16470,#16471,#16472),.UNSPECIFIED.,.F.,.F.,(4,2,2,2,4),(-0.0796560912226909,
-0.0585074655832387,-0.0373588399437865,-0.0186794199718933,0.),
 .UNSPECIFIED.);
#101=B_SPLINE_CURVE_WITH_KNOTS('',3,(#16476,#16477,#16478,#16479,#16480,
#16481,#16482,#16483,#16484,#16485),.UNSPECIFIED.,.F.,.F.,(4,2,2,2,4),(0.,
0.0186794199718933,0.0373588399437866,0.0585074655832387,0.0796560912226909),
 .UNSPECIFIED.);
#102=B_SPLINE_CURVE_WITH_KNOTS('',3,(#16489,#16490,#16491,#16492,#16493,
#16494,#16495,#16496,#16497,#16498),.UNSPECIFIED.,.F.,.F.,(4,2,2,2,4),(0.0764772858968707,
0.0963992866730888,0.116321287449307,0.135161425005967,0.154001562562628),
 .UNSPECIFIED.);
#103=B_SPLINE_CURVE_WITH_KNOTS('',3,(#16502,#16503,#16504,#16505,#16506,
#16507,#16508,#16509,#16510,#16511,#16512,#16513,#16514,#16515,#16516,#16517,
#16518,#16519,#16520,#16521,#16522),.UNSPECIFIED.,.F.,.F.,(4,2,2,2,3,2,
2,2,2,4),(-0.0487654213288013,-0.0396424658283719,-0.019821232914186,-0.00991061645709301,
0.,0.00991061645709316,0.0198212329141863,0.0396424658283726,0.0754755088146797,
0.111308551800987),.UNSPECIFIED.);
#104=B_SPLINE_CURVE_WITH_KNOTS('',3,(#16526,#16527,#16528,#16529,#16530,
#16531,#16532,#16533,#16534,#16535,#16536,#16537,#16538,#16539,#16540,#16541),
 .UNSPECIFIED.,.F.,.F.,(4,2,2,2,2,2,2,4),(0.080261889411958,0.100728357288421,
0.121194825164885,0.139914688841484,0.158634552518082,0.177354416194681,
0.19607427987128,0.196799093526934),.UNSPECIFIED.);
#105=B_SPLINE_CURVE_WITH_KNOTS('',3,(#16545,#16546,#16547,#16548,#16549,
#16550,#16551,#16552,#16553,#16554,#16555,#16556,#16557,#16558,#16559,#16560),
 .UNSPECIFIED.,.F.,.F.,(4,2,2,2,2,2,2,4),(0.120470011509229,0.121194825164884,
0.139914688841482,0.158634552518081,0.17735441619468,0.196074279871279,
0.216540747747742,0.237007215624205),.UNSPECIFIED.);
#106=B_SPLINE_CURVE_WITH_KNOTS('',3,(#16564,#16565,#16566,#16567,#16568,
#16569,#16570,#16571,#16572,#16573,#16574,#16575,#16576,#16577,#16578,#16579,
#16580,#16581,#16582,#16583,#16584),.UNSPECIFIED.,.F.,.F.,(4,2,2,2,2,3,
2,2,2,4),(-0.111308551800987,-0.0754755088146797,-0.0396424658283726,-0.0198212329141863,
-0.00991061645709312,0.,0.00991061645709299,0.019821232914186,0.039642465828372,
0.0487654212438805),.UNSPECIFIED.);
#107=B_SPLINE_CURVE_WITH_KNOTS('',3,(#16594,#16595,#16596,#16597,#16598,
#16599,#16600,#16601,#16602,#16603),.UNSPECIFIED.,.F.,.F.,(4,2,2,2,4),(0.154001562562628,
0.172841700119288,0.191681837675949,0.211603838452167,0.231525839228385),
 .UNSPECIFIED.);
#108=B_SPLINE_CURVE_WITH_KNOTS('',3,(#16607,#16608,#16609,#16610,#16611,
#16612,#16613,#16614,#16615,#16616),.UNSPECIFIED.,.F.,.F.,(4,2,2,2,4),(-0.0796560912226908,
-0.0585074655832387,-0.0373588399437865,-0.0186794199718933,0.),
 .UNSPECIFIED.);
#109=B_SPLINE_CURVE_WITH_KNOTS('',3,(#16620,#16621,#16622,#16623,#16624,
#16625,#16626,#16627,#16628,#16629),.UNSPECIFIED.,.F.,.F.,(4,2,2,2,4),(0.,
0.0186794199718932,0.0373588399437865,0.0585074655832387,0.0796560912226908),
 .UNSPECIFIED.);
#110=B_SPLINE_CURVE_WITH_KNOTS('',3,(#16633,#16634,#16635,#16636,#16637,
#16638,#16639,#16640,#16641,#16642),.UNSPECIFIED.,.F.,.F.,(4,2,2,2,4),(0.0764772858968705,
0.0963992866730887,0.116321287449307,0.135161425005967,0.154001562562628),
 .UNSPECIFIED.);
#111=B_SPLINE_CURVE_WITH_KNOTS('',3,(#16646,#16647,#16648,#16649,#16650,
#16651,#16652,#16653,#16654,#16655,#16656,#16657,#16658,#16659,#16660,#16661,
#16662,#16663,#16664,#16665,#16666),.UNSPECIFIED.,.F.,.F.,(4,2,2,2,3,2,
2,2,2,4),(-0.0487654213288016,-0.0396424658283713,-0.0198212329141857,-0.00991061645709285,
0.,0.0099106164570932,0.0198212329141864,0.0396424658283728,0.0754755088146802,
0.111308551800988),.UNSPECIFIED.);
#112=B_SPLINE_CURVE_WITH_KNOTS('',3,(#16670,#16671,#16672,#16673,#16674,
#16675,#16676,#16677,#16678,#16679,#16680,#16681,#16682,#16683,#16684,#16685),
 .UNSPECIFIED.,.F.,.F.,(4,2,2,2,2,2,2,4),(0.0802618894119582,0.100728357288421,
0.121194825164885,0.139914688841483,0.158634552518082,0.177354416194681,
0.19607427987128,0.196799093526934),.UNSPECIFIED.);
#113=B_SPLINE_CURVE_WITH_KNOTS('',3,(#16689,#16690,#16691,#16692,#16693,
#16694,#16695,#16696,#16697,#16698,#16699,#16700,#16701,#16702,#16703,#16704),
 .UNSPECIFIED.,.F.,.F.,(4,2,2,2,2,2,2,4),(0.12047001150923,0.121194825164884,
0.139914688841483,0.158634552518082,0.17735441619468,0.196074279871279,
0.216540747747742,0.237007215624206),.UNSPECIFIED.);
#114=B_SPLINE_CURVE_WITH_KNOTS('',3,(#16708,#16709,#16710,#16711,#16712,
#16713,#16714,#16715,#16716,#16717,#16718,#16719,#16720,#16721,#16722,#16723,
#16724,#16725,#16726,#16727,#16728),.UNSPECIFIED.,.F.,.F.,(4,2,2,2,2,3,
2,2,2,4),(-0.111308551800987,-0.0754755088146801,-0.0396424658283728,-0.0198212329141864,
-0.00991061645709318,0.,0.00991061645709283,0.0198212329141857,0.0396424658283713,
0.0487654212438809),.UNSPECIFIED.);
#115=B_SPLINE_CURVE_WITH_KNOTS('',3,(#16741,#16742,#16743,#16744,#16745,
#16746,#16747,#16748,#16749,#16750),.UNSPECIFIED.,.F.,.F.,(4,2,2,2,4),(0.161501820430177,
0.181202019666624,0.200902218903071,0.22218706551677,0.243471912130469),
 .UNSPECIFIED.);
#116=B_SPLINE_CURVE_WITH_KNOTS('',3,(#16754,#16755,#16756,#16757,#16758,
#16759,#16760,#16761,#16762,#16763),.UNSPECIFIED.,.F.,.F.,(4,2,2,2,4),(0.0930675005857169,
0.116580531967156,0.140093563348596,0.159964165564682,0.179834767780768),
 .UNSPECIFIED.);
#117=B_SPLINE_CURVE_WITH_KNOTS('',3,(#16767,#16768,#16769,#16770,#16771,
#16772,#16773,#16774,#16775,#16776),.UNSPECIFIED.,.F.,.F.,(4,2,2,2,4),(0.17982154994437,
0.199692152160456,0.219562754376542,0.243075785757982,0.266588817139421),
 .UNSPECIFIED.);
#118=B_SPLINE_CURVE_WITH_KNOTS('',3,(#16779,#16780,#16781,#16782,#16783,
#16784,#16785,#16786,#16787,#16788),.UNSPECIFIED.,.F.,.F.,(4,2,2,2,4),(0.0795500677920484,
0.100834914405747,0.122119761019446,0.141819960255893,0.16152015949234),
 .UNSPECIFIED.);
#171=SPHERICAL_SURFACE('',#10585,0.500000000000025);
#172=SPHERICAL_SURFACE('',#10588,0.500000000000005);
#173=SPHERICAL_SURFACE('',#10609,0.500000000000007);
#174=SPHERICAL_SURFACE('',#10613,0.499999999999998);
#175=SPHERICAL_SURFACE('',#10618,0.500000000000007);
#176=SPHERICAL_SURFACE('',#10621,0.500000000000007);
#177=SPHERICAL_SURFACE('',#10626,0.500000000000007);
#178=SPHERICAL_SURFACE('',#10630,0.500000000000007);
#179=SPHERICAL_SURFACE('',#10635,0.500000000000007);
#180=SPHERICAL_SURFACE('',#10638,0.500000000000007);
#181=SPHERICAL_SURFACE('',#10648,0.500000000000007);
#182=SPHERICAL_SURFACE('',#10656,0.500000000000007);
#183=SPHERICAL_SURFACE('',#10660,0.500000000000007);
#184=SPHERICAL_SURFACE('',#10664,0.499999999999998);
#185=SPHERICAL_SURFACE('',#10668,0.500000000000007);
#186=SPHERICAL_SURFACE('',#10671,0.499999999999998);
#241=TOROIDAL_SURFACE('',#10591,1.,0.5);
#242=TOROIDAL_SURFACE('',#10596,1.,0.500000000000002);
#243=TOROIDAL_SURFACE('',#10600,0.999999999999996,0.499999999999998);
#244=TOROIDAL_SURFACE('',#10604,1.,0.499999999999998);
#245=TOROIDAL_SURFACE('',#10643,0.999999999999999,0.499999999999998);
#246=TOROIDAL_SURFACE('',#10652,1.,0.499999999999998);
#247=TOROIDAL_SURFACE('',#10675,0.999999999999996,0.499999999999998);
#248=TOROIDAL_SURFACE('',#10681,1.00000000000001,0.500000000000007);
#273=ELLIPSE('',#10470,7.07106781186548,5.);
#274=ELLIPSE('',#10472,7.07106781186548,5.);
#275=ELLIPSE('',#10483,7.07106781186548,5.);
#276=ELLIPSE('',#10485,7.07106781186548,5.);
#277=ELLIPSE('',#10492,7.07106781186548,5.);
#278=ELLIPSE('',#10494,7.07106781186548,5.);
#279=ELLIPSE('',#10501,7.07106781186548,5.);
#280=ELLIPSE('',#10503,7.07106781186548,5.);
#292=SHAPE_REPRESENTATION_RELATIONSHIP('SRR','None',#17879,#302);
#302=ADVANCED_BREP_SHAPE_REPRESENTATION('',(#322),#17831);
#312=STYLED_ITEM('',(#17959),#322);
#322=MANIFOLD_SOLID_BREP('Moving_Carriage_01',#9633);
#478=CYLINDRICAL_SURFACE('',#10400,12.5);
#479=CYLINDRICAL_SURFACE('',#10403,12.5);
#480=CYLINDRICAL_SURFACE('',#10420,0.5);
#481=CYLINDRICAL_SURFACE('',#10423,0.5);
#482=CYLINDRICAL_SURFACE('',#10425,5.);
#483=CYLINDRICAL_SURFACE('',#10428,5.);
#484=CYLINDRICAL_SURFACE('',#10431,5.);
#485=CYLINDRICAL_SURFACE('',#10434,5.);
#486=CYLINDRICAL_SURFACE('',#10438,12.5);
#487=CYLINDRICAL_SURFACE('',#10441,5.);
#488=CYLINDRICAL_SURFACE('',#10445,5.);
#489=CYLINDRICAL_SURFACE('',#10448,5.);
#490=CYLINDRICAL_SURFACE('',#10452,5.);
#491=CYLINDRICAL_SURFACE('',#10455,5.);
#492=CYLINDRICAL_SURFACE('',#10458,5.);
#493=CYLINDRICAL_SURFACE('',#10461,5.);
#494=CYLINDRICAL_SURFACE('',#10465,5.);
#495=CYLINDRICAL_SURFACE('',#10474,12.5);
#496=CYLINDRICAL_SURFACE('',#10478,5.);
#497=CYLINDRICAL_SURFACE('',#10487,5.);
#498=CYLINDRICAL_SURFACE('',#10496,5.);
#499=CYLINDRICAL_SURFACE('',#10505,5.);
#500=CYLINDRICAL_SURFACE('',#10508,5.);
#501=CYLINDRICAL_SURFACE('',#10511,0.5);
#502=CYLINDRICAL_SURFACE('',#10512,0.5);
#503=CYLINDRICAL_SURFACE('',#10514,0.5);
#504=CYLINDRICAL_SURFACE('',#10515,0.5);
#505=CYLINDRICAL_SURFACE('',#10517,0.5);
#506=CYLINDRICAL_SURFACE('',#10522,0.5);
#507=CYLINDRICAL_SURFACE('',#10523,0.5);
#508=CYLINDRICAL_SURFACE('',#10525,0.5);
#509=CYLINDRICAL_SURFACE('',#10526,0.5);
#510=CYLINDRICAL_SURFACE('',#10528,0.5);
#511=CYLINDRICAL_SURFACE('',#10530,0.5);
#512=CYLINDRICAL_SURFACE('',#10531,0.5);
#513=CYLINDRICAL_SURFACE('',#10533,0.5);
#514=CYLINDRICAL_SURFACE('',#10534,0.5);
#515=CYLINDRICAL_SURFACE('',#10540,0.5);
#516=CYLINDRICAL_SURFACE('',#10542,0.5);
#517=CYLINDRICAL_SURFACE('',#10543,0.5);
#518=CYLINDRICAL_SURFACE('',#10545,0.5);
#519=CYLINDRICAL_SURFACE('',#10546,0.5);
#520=CYLINDRICAL_SURFACE('',#10548,0.5);
#521=CYLINDRICAL_SURFACE('',#10549,0.5);
#522=CYLINDRICAL_SURFACE('',#10551,0.5);
#523=CYLINDRICAL_SURFACE('',#10552,0.5);
#524=CYLINDRICAL_SURFACE('',#10561,0.5);
#525=CYLINDRICAL_SURFACE('',#10563,0.5);
#526=CYLINDRICAL_SURFACE('',#10564,0.5);
#527=CYLINDRICAL_SURFACE('',#10566,0.5);
#528=CYLINDRICAL_SURFACE('',#10568,0.5);
#529=CYLINDRICAL_SURFACE('',#10569,0.5);
#530=CYLINDRICAL_SURFACE('',#10571,0.5);
#531=CYLINDRICAL_SURFACE('',#10572,0.5);
#532=CYLINDRICAL_SURFACE('',#10573,0.5);
#533=CYLINDRICAL_SURFACE('',#10578,0.5);
#534=CYLINDRICAL_SURFACE('',#10579,0.5);
#535=CYLINDRICAL_SURFACE('',#10581,0.5);
#536=CYLINDRICAL_SURFACE('',#10582,0.5);
#537=CYLINDRICAL_SURFACE('',#10595,0.5);
#538=CYLINDRICAL_SURFACE('',#10608,0.5);
#539=CYLINDRICAL_SURFACE('',#10612,0.5);
#540=CYLINDRICAL_SURFACE('',#10617,0.5);
#541=CYLINDRICAL_SURFACE('',#10625,0.5);
#542=CYLINDRICAL_SURFACE('',#10629,0.5);
#543=CYLINDRICAL_SURFACE('',#10634,0.5);
#544=CYLINDRICAL_SURFACE('',#10642,0.5);
#545=CYLINDRICAL_SURFACE('',#10647,0.5);
#546=CYLINDRICAL_SURFACE('',#10663,0.5);
#547=CYLINDRICAL_SURFACE('',#10679,0.5);
#548=CYLINDRICAL_SURFACE('',#10680,0.5);
#549=CYLINDRICAL_SURFACE('',#10685,0.5);
#550=CYLINDRICAL_SURFACE('',#10686,0.5);
#551=CYLINDRICAL_SURFACE('',#10687,0.5);
#552=CYLINDRICAL_SURFACE('',#10688,0.5);
#553=CYLINDRICAL_SURFACE('',#10689,0.5);
#554=CYLINDRICAL_SURFACE('',#10690,0.5);
#555=CYLINDRICAL_SURFACE('',#10691,0.5);
#556=CYLINDRICAL_SURFACE('',#10692,0.5);
#557=CYLINDRICAL_SURFACE('',#10693,0.5);
#558=CYLINDRICAL_SURFACE('',#10694,0.5);
#559=CYLINDRICAL_SURFACE('',#10695,0.5);
#560=CYLINDRICAL_SURFACE('',#10696,0.5);
#561=CYLINDRICAL_SURFACE('',#10697,0.5);
#562=CYLINDRICAL_SURFACE('',#10698,0.5);
#563=CYLINDRICAL_SURFACE('',#10699,0.5);
#564=CYLINDRICAL_SURFACE('',#10700,0.5);
#565=CYLINDRICAL_SURFACE('',#10701,0.5);
#566=CYLINDRICAL_SURFACE('',#10702,0.5);
#567=CYLINDRICAL_SURFACE('',#10703,0.5);
#568=CYLINDRICAL_SURFACE('',#10704,0.5);
#973=LINE('',#15617,#1638);
#974=LINE('',#15623,#1639);
#975=LINE('',#15638,#1640);
#976=LINE('',#15664,#1641);
#977=LINE('',#15679,#1642);
#978=LINE('',#15681,#1643);
#979=LINE('',#15683,#1644);
#980=LINE('',#15687,#1645);
#981=LINE('',#15691,#1646);
#982=LINE('',#15695,#1647);
#983=LINE('',#15699,#1648);
#984=LINE('',#15701,#1649);
#985=LINE('',#15703,#1650);
#986=LINE('',#15707,#1651);
#987=LINE('',#15713,#1652);
#988=LINE('',#15719,#1653);
#989=LINE('',#15724,#1654);
#990=LINE('',#15727,#1655);
#991=LINE('',#15731,#1656);
#992=LINE('',#15732,#1657);
#993=LINE('',#15735,#1658);
#994=LINE('',#15740,#1659);
#995=LINE('',#15753,#1660);
#996=LINE('',#15779,#1661);
#997=LINE('',#15794,#1662);
#998=LINE('',#15800,#1663);
#999=LINE('',#15806,#1664);
#1000=LINE('',#15821,#1665);
#1001=LINE('',#15844,#1666);
#1002=LINE('',#15861,#1667);
#1003=LINE('',#15867,#1668);
#1004=LINE('',#15882,#1669);
#1005=LINE('',#15905,#1670);
#1006=LINE('',#15922,#1671);
#1007=LINE('',#15928,#1672);
#1008=LINE('',#15943,#1673);
#1009=LINE('',#15966,#1674);
#1010=LINE('',#15983,#1675);
#1011=LINE('',#15988,#1676);
#1012=LINE('',#16001,#1677);
#1013=LINE('',#16027,#1678);
#1014=LINE('',#16042,#1679);
#1015=LINE('',#16048,#1680);
#1016=LINE('',#16063,#1681);
#1017=LINE('',#16086,#1682);
#1018=LINE('',#16103,#1683);
#1019=LINE('',#16118,#1684);
#1020=LINE('',#16144,#1685);
#1021=LINE('',#16247,#1686);
#1022=LINE('',#16262,#1687);
#1023=LINE('',#16285,#1688);
#1024=LINE('',#16302,#1689);
#1025=LINE('',#16317,#1690);
#1026=LINE('',#16343,#1691);
#1027=LINE('',#16446,#1692);
#1028=LINE('',#16461,#1693);
#1029=LINE('',#16487,#1694);
#1030=LINE('',#16590,#1695);
#1031=LINE('',#16605,#1696);
#1032=LINE('',#16631,#1697);
#1033=LINE('',#16734,#1698);
#1034=LINE('',#16739,#1699);
#1035=LINE('',#16752,#1700);
#1036=LINE('',#16778,#1701);
#1037=LINE('',#16790,#1702);
#1038=LINE('',#16794,#1703);
#1039=LINE('',#16796,#1704);
#1040=LINE('',#16799,#1705);
#1041=LINE('',#16802,#1706);
#1042=LINE('',#16805,#1707);
#1043=LINE('',#16806,#1708);
#1044=LINE('',#16808,#1709);
#1045=LINE('',#16811,#1710);
#1046=LINE('',#16812,#1711);
#1047=LINE('',#16814,#1712);
#1048=LINE('',#16816,#1713);
#1049=LINE('',#16820,#1714);
#1050=LINE('',#16822,#1715);
#1051=LINE('',#16825,#1716);
#1052=LINE('',#16829,#1717);
#1053=LINE('',#16832,#1718);
#1054=LINE('',#16834,#1719);
#1055=LINE('',#16835,#1720);
#1056=LINE('',#16838,#1721);
#1057=LINE('',#16841,#1722);
#1058=LINE('',#16843,#1723);
#1059=LINE('',#16844,#1724);
#1060=LINE('',#16846,#1725);
#1061=LINE('',#16847,#1726);
#1062=LINE('',#16850,#1727);
#1063=LINE('',#16851,#1728);
#1064=LINE('',#16853,#1729);
#1065=LINE('',#16856,#1730);
#1066=LINE('',#16857,#1731);
#1067=LINE('',#16859,#1732);
#1068=LINE('',#16861,#1733);
#1069=LINE('',#16864,#1734);
#1070=LINE('',#16867,#1735);
#1071=LINE('',#16869,#1736);
#1072=LINE('',#16870,#1737);
#1073=LINE('',#16873,#1738);
#1074=LINE('',#16876,#1739);
#1075=LINE('',#16878,#1740);
#1076=LINE('',#16879,#1741);
#1077=LINE('',#16883,#1742);
#1078=LINE('',#16885,#1743);
#1079=LINE('',#16888,#1744);
#1080=LINE('',#16891,#1745);
#1081=LINE('',#16893,#1746);
#1082=LINE('',#16896,#1747);
#1083=LINE('',#16897,#1748);
#1084=LINE('',#16899,#1749);
#1085=LINE('',#16902,#1750);
#1086=LINE('',#16903,#1751);
#1087=LINE('',#16905,#1752);
#1088=LINE('',#16908,#1753);
#1089=LINE('',#16909,#1754);
#1090=LINE('',#16912,#1755);
#1091=LINE('',#16913,#1756);
#1092=LINE('',#16915,#1757);
#1093=LINE('',#16917,#1758);
#1094=LINE('',#16925,#1759);
#1095=LINE('',#16926,#1760);
#1096=LINE('',#16927,#1761);
#1097=LINE('',#16928,#1762);
#1098=LINE('',#16930,#1763);
#1099=LINE('',#16932,#1764);
#1100=LINE('',#16934,#1765);
#1101=LINE('',#16935,#1766);
#1102=LINE('',#16937,#1767);
#1103=LINE('',#16940,#1768);
#1104=LINE('',#16943,#1769);
#1105=LINE('',#16945,#1770);
#1106=LINE('',#16947,#1771);
#1107=LINE('',#16950,#1772);
#1108=LINE('',#16951,#1773);
#1109=LINE('',#16953,#1774);
#1110=LINE('',#16955,#1775);
#1111=LINE('',#16957,#1776);
#1112=LINE('',#16964,#1777);
#1113=LINE('',#16965,#1778);
#1114=LINE('',#16966,#1779);
#1115=LINE('',#16968,#1780);
#1116=LINE('',#16970,#1781);
#1117=LINE('',#16972,#1782);
#1118=LINE('',#16973,#1783);
#1119=LINE('',#16989,#1784);
#1120=LINE('',#17009,#1785);
#1121=LINE('',#17015,#1786);
#1122=LINE('',#17023,#1787);
#1123=LINE('',#17035,#1788);
#1124=LINE('',#17041,#1789);
#1125=LINE('',#17050,#1790);
#1126=LINE('',#17051,#1791);
#1127=LINE('',#17064,#1792);
#1128=LINE('',#17065,#1793);
#1129=LINE('',#17073,#1794);
#1130=LINE('',#17099,#1795);
#1131=LINE('',#17123,#1796);
#1132=LINE('',#17125,#1797);
#1133=LINE('',#17133,#1798);
#1134=LINE('',#17135,#1799);
#1135=LINE('',#17137,#1800);
#1136=LINE('',#17139,#1801);
#1137=LINE('',#17140,#1802);
#1138=LINE('',#17142,#1803);
#1139=LINE('',#17144,#1804);
#1140=LINE('',#17146,#1805);
#1141=LINE('',#17147,#1806);
#1142=LINE('',#17149,#1807);
#1143=LINE('',#17150,#1808);
#1144=LINE('',#17152,#1809);
#1145=LINE('',#17153,#1810);
#1146=LINE('',#17155,#1811);
#1147=LINE('',#17157,#1812);
#1148=LINE('',#17158,#1813);
#1149=LINE('',#17160,#1814);
#1150=LINE('',#17161,#1815);
#1151=LINE('',#17163,#1816);
#1152=LINE('',#17165,#1817);
#1153=LINE('',#17167,#1818);
#1154=LINE('',#17169,#1819);
#1155=LINE('',#17171,#1820);
#1156=LINE('',#17173,#1821);
#1157=LINE('',#17175,#1822);
#1158=LINE('',#17177,#1823);
#1159=LINE('',#17178,#1824);
#1638=VECTOR('',#12671,12.5);
#1639=VECTOR('',#12678,12.5);
#1640=VECTOR('',#12681,10.);
#1641=VECTOR('',#12684,10.);
#1642=VECTOR('',#12689,10.);
#1643=VECTOR('',#12690,10.);
#1644=VECTOR('',#12691,10.);
#1645=VECTOR('',#12694,10.);
#1646=VECTOR('',#12697,10.);
#1647=VECTOR('',#12700,10.);
#1648=VECTOR('',#12703,10.);
#1649=VECTOR('',#12704,10.);
#1650=VECTOR('',#12705,10.);
#1651=VECTOR('',#12708,10.);
#1652=VECTOR('',#12713,10.);
#1653=VECTOR('',#12718,10.);
#1654=VECTOR('',#12723,10.);
#1655=VECTOR('',#12726,10.);
#1656=VECTOR('',#12731,10.);
#1657=VECTOR('',#12732,10.);
#1658=VECTOR('',#12735,10.);
#1659=VECTOR('',#12742,5.);
#1660=VECTOR('',#12743,10.);
#1661=VECTOR('',#12746,10.);
#1662=VECTOR('',#12751,5.);
#1663=VECTOR('',#12758,5.);
#1664=VECTOR('',#12765,5.);
#1665=VECTOR('',#12768,10.);
#1666=VECTOR('',#12769,10.);
#1667=VECTOR('',#12776,12.5);
#1668=VECTOR('',#12783,5.);
#1669=VECTOR('',#12786,10.);
#1670=VECTOR('',#12787,10.);
#1671=VECTOR('',#12794,5.);
#1672=VECTOR('',#12801,5.);
#1673=VECTOR('',#12804,10.);
#1674=VECTOR('',#12805,10.);
#1675=VECTOR('',#12812,5.);
#1676=VECTOR('',#12819,5.);
#1677=VECTOR('',#12820,10.);
#1678=VECTOR('',#12823,10.);
#1679=VECTOR('',#12828,5.);
#1680=VECTOR('',#12835,5.);
#1681=VECTOR('',#12838,10.);
#1682=VECTOR('',#12839,10.);
#1683=VECTOR('',#12846,5.);
#1684=VECTOR('',#12849,10.);
#1685=VECTOR('',#12852,10.);
#1686=VECTOR('',#12867,12.5);
#1687=VECTOR('',#12870,10.);
#1688=VECTOR('',#12871,10.);
#1689=VECTOR('',#12878,5.);
#1690=VECTOR('',#12881,10.);
#1691=VECTOR('',#12884,10.);
#1692=VECTOR('',#12899,5.);
#1693=VECTOR('',#12902,10.);
#1694=VECTOR('',#12905,10.);
#1695=VECTOR('',#12920,5.);
#1696=VECTOR('',#12923,10.);
#1697=VECTOR('',#12926,10.);
#1698=VECTOR('',#12941,5.);
#1699=VECTOR('',#12948,5.);
#1700=VECTOR('',#12949,10.);
#1701=VECTOR('',#12952,10.);
#1702=VECTOR('',#12955,10.);
#1703=VECTOR('',#12960,10.);
#1704=VECTOR('',#12963,10.);
#1705=VECTOR('',#12966,10.);
#1706=VECTOR('',#12971,10.);
#1707=VECTOR('',#12974,10.);
#1708=VECTOR('',#12975,10.);
#1709=VECTOR('',#12978,10.);
#1710=VECTOR('',#12981,10.);
#1711=VECTOR('',#12982,10.);
#1712=VECTOR('',#12985,10.);
#1713=VECTOR('',#12988,10.);
#1714=VECTOR('',#12993,10.);
#1715=VECTOR('',#12996,10.);
#1716=VECTOR('',#12999,10.);
#1717=VECTOR('',#13004,10.);
#1718=VECTOR('',#13007,10.);
#1719=VECTOR('',#13010,10.);
#1720=VECTOR('',#13011,10.);
#1721=VECTOR('',#13014,10.);
#1722=VECTOR('',#13017,10.);
#1723=VECTOR('',#13020,10.);
#1724=VECTOR('',#13021,10.);
#1725=VECTOR('',#13024,10.);
#1726=VECTOR('',#13025,10.);
#1727=VECTOR('',#13028,10.);
#1728=VECTOR('',#13029,10.);
#1729=VECTOR('',#13032,10.);
#1730=VECTOR('',#13035,10.);
#1731=VECTOR('',#13036,10.);
#1732=VECTOR('',#13039,10.);
#1733=VECTOR('',#13042,10.);
#1734=VECTOR('',#13045,10.);
#1735=VECTOR('',#13048,10.);
#1736=VECTOR('',#13051,10.);
#1737=VECTOR('',#13052,10.);
#1738=VECTOR('',#13055,10.);
#1739=VECTOR('',#13058,10.);
#1740=VECTOR('',#13061,10.);
#1741=VECTOR('',#13062,10.);
#1742=VECTOR('',#13067,10.);
#1743=VECTOR('',#13070,10.);
#1744=VECTOR('',#13073,10.);
#1745=VECTOR('',#13078,10.);
#1746=VECTOR('',#13081,10.);
#1747=VECTOR('',#13084,10.);
#1748=VECTOR('',#13085,10.);
#1749=VECTOR('',#13088,10.);
#1750=VECTOR('',#13091,10.);
#1751=VECTOR('',#13092,10.);
#1752=VECTOR('',#13095,10.);
#1753=VECTOR('',#13098,10.);
#1754=VECTOR('',#13099,10.);
#1755=VECTOR('',#13102,10.);
#1756=VECTOR('',#13103,10.);
#1757=VECTOR('',#13106,10.);
#1758=VECTOR('',#13109,10.);
#1759=VECTOR('',#13124,10.);
#1760=VECTOR('',#13125,10.);
#1761=VECTOR('',#13126,10.);
#1762=VECTOR('',#13127,10.);
#1763=VECTOR('',#13128,10.);
#1764=VECTOR('',#13129,10.);
#1765=VECTOR('',#13130,10.);
#1766=VECTOR('',#13131,10.);
#1767=VECTOR('',#13134,10.);
#1768=VECTOR('',#13137,10.);
#1769=VECTOR('',#13142,10.);
#1770=VECTOR('',#13145,10.);
#1771=VECTOR('',#13148,10.);
#1772=VECTOR('',#13151,10.);
#1773=VECTOR('',#13152,10.);
#1774=VECTOR('',#13155,10.);
#1775=VECTOR('',#13158,10.);
#1776=VECTOR('',#13161,10.);
#1777=VECTOR('',#13174,10.);
#1778=VECTOR('',#13175,10.);
#1779=VECTOR('',#13176,10.);
#1780=VECTOR('',#13179,10.);
#1781=VECTOR('',#13180,10.);
#1782=VECTOR('',#13181,10.);
#1783=VECTOR('',#13182,10.);
#1784=VECTOR('',#13205,10.);
#1785=VECTOR('',#13232,10.);
#1786=VECTOR('',#13241,10.);
#1787=VECTOR('',#13252,10.);
#1788=VECTOR('',#13269,10.);
#1789=VECTOR('',#13278,10.);
#1790=VECTOR('',#13289,10.);
#1791=VECTOR('',#13290,10.);
#1792=VECTOR('',#13307,10.);
#1793=VECTOR('',#13308,10.);
#1794=VECTOR('',#13319,10.);
#1795=VECTOR('',#13352,10.);
#1796=VECTOR('',#13385,10.);
#1797=VECTOR('',#13388,10.);
#1798=VECTOR('',#13399,10.);
#1799=VECTOR('',#13402,10.);
#1800=VECTOR('',#13405,10.);
#1801=VECTOR('',#13408,10.);
#1802=VECTOR('',#13409,10.);
#1803=VECTOR('',#13412,10.);
#1804=VECTOR('',#13415,10.);
#1805=VECTOR('',#13418,10.);
#1806=VECTOR('',#13419,10.);
#1807=VECTOR('',#13422,10.);
#1808=VECTOR('',#13423,10.);
#1809=VECTOR('',#13426,10.);
#1810=VECTOR('',#13427,10.);
#1811=VECTOR('',#13430,10.);
#1812=VECTOR('',#13433,10.);
#1813=VECTOR('',#13434,10.);
#1814=VECTOR('',#13437,10.);
#1815=VECTOR('',#13438,10.);
#1816=VECTOR('',#13441,10.);
#1817=VECTOR('',#13444,10.);
#1818=VECTOR('',#13447,10.);
#1819=VECTOR('',#13450,10.);
#1820=VECTOR('',#13453,10.);
#1821=VECTOR('',#13456,10.);
#1822=VECTOR('',#13459,10.);
#1823=VECTOR('',#13462,10.);
#1824=VECTOR('',#13463,10.);
#1991=FACE_BOUND('',#3058,.T.);
#1992=FACE_BOUND('',#3059,.T.);
#1993=FACE_BOUND('',#3060,.T.);
#1994=FACE_BOUND('',#3062,.T.);
#1995=FACE_BOUND('',#3063,.T.);
#1996=FACE_BOUND('',#3064,.T.);
#1997=FACE_BOUND('',#3065,.T.);
#1998=FACE_BOUND('',#3066,.T.);
#1999=FACE_BOUND('',#3129,.T.);
#2000=FACE_BOUND('',#3130,.T.);
#2001=FACE_BOUND('',#3131,.T.);
#2002=FACE_BOUND('',#3132,.T.);
#2003=FACE_BOUND('',#3133,.T.);
#2004=FACE_BOUND('',#3134,.T.);
#2005=FACE_BOUND('',#3135,.T.);
#2006=FACE_BOUND('',#3136,.T.);
#2007=FACE_BOUND('',#3137,.T.);
#2008=FACE_BOUND('',#3138,.T.);
#2009=FACE_BOUND('',#3139,.T.);
#2010=FACE_BOUND('',#3140,.T.);
#2011=FACE_BOUND('',#3141,.T.);
#2012=FACE_BOUND('',#3142,.T.);
#2013=FACE_BOUND('',#3143,.T.);
#2014=FACE_BOUND('',#3144,.T.);
#2015=FACE_BOUND('',#3145,.T.);
#2016=FACE_BOUND('',#3146,.T.);
#2017=FACE_BOUND('',#3147,.T.);
#2018=FACE_BOUND('',#3148,.T.);
#2019=FACE_BOUND('',#3149,.T.);
#2343=FACE_OUTER_BOUND('',#2974,.T.);
#2344=FACE_OUTER_BOUND('',#2975,.T.);
#2345=FACE_OUTER_BOUND('',#2976,.T.);
#2346=FACE_OUTER_BOUND('',#2977,.T.);
#2347=FACE_OUTER_BOUND('',#2978,.T.);
#2348=FACE_OUTER_BOUND('',#2979,.T.);
#2349=FACE_OUTER_BOUND('',#2980,.T.);
#2350=FACE_OUTER_BOUND('',#2981,.T.);
#2351=FACE_OUTER_BOUND('',#2982,.T.);
#2352=FACE_OUTER_BOUND('',#2983,.T.);
#2353=FACE_OUTER_BOUND('',#2984,.T.);
#2354=FACE_OUTER_BOUND('',#2985,.T.);
#2355=FACE_OUTER_BOUND('',#2986,.T.);
#2356=FACE_OUTER_BOUND('',#2987,.T.);
#2357=FACE_OUTER_BOUND('',#2988,.T.);
#2358=FACE_OUTER_BOUND('',#2989,.T.);
#2359=FACE_OUTER_BOUND('',#2990,.T.);
#2360=FACE_OUTER_BOUND('',#2991,.T.);
#2361=FACE_OUTER_BOUND('',#2992,.T.);
#2362=FACE_OUTER_BOUND('',#2993,.T.);
#2363=FACE_OUTER_BOUND('',#2994,.T.);
#2364=FACE_OUTER_BOUND('',#2995,.T.);
#2365=FACE_OUTER_BOUND('',#2996,.T.);
#2366=FACE_OUTER_BOUND('',#2997,.T.);
#2367=FACE_OUTER_BOUND('',#2998,.T.);
#2368=FACE_OUTER_BOUND('',#2999,.T.);
#2369=FACE_OUTER_BOUND('',#3000,.T.);
#2370=FACE_OUTER_BOUND('',#3001,.T.);
#2371=FACE_OUTER_BOUND('',#3002,.T.);
#2372=FACE_OUTER_BOUND('',#3003,.T.);
#2373=FACE_OUTER_BOUND('',#3004,.T.);
#2374=FACE_OUTER_BOUND('',#3005,.T.);
#2375=FACE_OUTER_BOUND('',#3006,.T.);
#2376=FACE_OUTER_BOUND('',#3007,.T.);
#2377=FACE_OUTER_BOUND('',#3008,.T.);
#2378=FACE_OUTER_BOUND('',#3009,.T.);
#2379=FACE_OUTER_BOUND('',#3010,.T.);
#2380=FACE_OUTER_BOUND('',#3011,.T.);
#2381=FACE_OUTER_BOUND('',#3012,.T.);
#2382=FACE_OUTER_BOUND('',#3013,.T.);
#2383=FACE_OUTER_BOUND('',#3014,.T.);
#2384=FACE_OUTER_BOUND('',#3015,.T.);
#2385=FACE_OUTER_BOUND('',#3016,.T.);
#2386=FACE_OUTER_BOUND('',#3017,.T.);
#2387=FACE_OUTER_BOUND('',#3018,.T.);
#2388=FACE_OUTER_BOUND('',#3019,.T.);
#2389=FACE_OUTER_BOUND('',#3020,.T.);
#2390=FACE_OUTER_BOUND('',#3021,.T.);
#2391=FACE_OUTER_BOUND('',#3022,.T.);
#2392=FACE_OUTER_BOUND('',#3023,.T.);
#2393=FACE_OUTER_BOUND('',#3024,.T.);
#2394=FACE_OUTER_BOUND('',#3025,.T.);
#2395=FACE_OUTER_BOUND('',#3026,.T.);
#2396=FACE_OUTER_BOUND('',#3027,.T.);
#2397=FACE_OUTER_BOUND('',#3028,.T.);
#2398=FACE_OUTER_BOUND('',#3029,.T.);
#2399=FACE_OUTER_BOUND('',#3030,.T.);
#2400=FACE_OUTER_BOUND('',#3031,.T.);
#2401=FACE_OUTER_BOUND('',#3032,.T.);
#2402=FACE_OUTER_BOUND('',#3033,.T.);
#2403=FACE_OUTER_BOUND('',#3034,.T.);
#2404=FACE_OUTER_BOUND('',#3035,.T.);
#2405=FACE_OUTER_BOUND('',#3036,.T.);
#2406=FACE_OUTER_BOUND('',#3037,.T.);
#2407=FACE_OUTER_BOUND('',#3038,.T.);
#2408=FACE_OUTER_BOUND('',#3039,.T.);
#2409=FACE_OUTER_BOUND('',#3040,.T.);
#2410=FACE_OUTER_BOUND('',#3041,.T.);
#2411=FACE_OUTER_BOUND('',#3042,.T.);
#2412=FACE_OUTER_BOUND('',#3043,.T.);
#2413=FACE_OUTER_BOUND('',#3044,.T.);
#2414=FACE_OUTER_BOUND('',#3045,.T.);
#2415=FACE_OUTER_BOUND('',#3046,.T.);
#2416=FACE_OUTER_BOUND('',#3047,.T.);
#2417=FACE_OUTER_BOUND('',#3048,.T.);
#2418=FACE_OUTER_BOUND('',#3049,.T.);
#2419=FACE_OUTER_BOUND('',#3050,.T.);
#2420=FACE_OUTER_BOUND('',#3051,.T.);
#2421=FACE_OUTER_BOUND('',#3052,.T.);
#2422=FACE_OUTER_BOUND('',#3053,.T.);
#2423=FACE_OUTER_BOUND('',#3054,.T.);
#2424=FACE_OUTER_BOUND('',#3055,.T.);
#2425=FACE_OUTER_BOUND('',#3056,.T.);
#2426=FACE_OUTER_BOUND('',#3057,.T.);
#2427=FACE_OUTER_BOUND('',#3061,.T.);
#2428=FACE_OUTER_BOUND('',#3067,.T.);
#2429=FACE_OUTER_BOUND('',#3068,.T.);
#2430=FACE_OUTER_BOUND('',#3069,.T.);
#2431=FACE_OUTER_BOUND('',#3070,.T.);
#2432=FACE_OUTER_BOUND('',#3071,.T.);
#2433=FACE_OUTER_BOUND('',#3072,.T.);
#2434=FACE_OUTER_BOUND('',#3073,.T.);
#2435=FACE_OUTER_BOUND('',#3074,.T.);
#2436=FACE_OUTER_BOUND('',#3075,.T.);
#2437=FACE_OUTER_BOUND('',#3076,.T.);
#2438=FACE_OUTER_BOUND('',#3077,.T.);
#2439=FACE_OUTER_BOUND('',#3078,.T.);
#2440=FACE_OUTER_BOUND('',#3079,.T.);
#2441=FACE_OUTER_BOUND('',#3080,.T.);
#2442=FACE_OUTER_BOUND('',#3081,.T.);
#2443=FACE_OUTER_BOUND('',#3082,.T.);
#2444=FACE_OUTER_BOUND('',#3083,.T.);
#2445=FACE_OUTER_BOUND('',#3084,.T.);
#2446=FACE_OUTER_BOUND('',#3085,.T.);
#2447=FACE_OUTER_BOUND('',#3086,.T.);
#2448=FACE_OUTER_BOUND('',#3087,.T.);
#2449=FACE_OUTER_BOUND('',#3088,.T.);
#2450=FACE_OUTER_BOUND('',#3089,.T.);
#2451=FACE_OUTER_BOUND('',#3090,.T.);
#2452=FACE_OUTER_BOUND('',#3091,.T.);
#2453=FACE_OUTER_BOUND('',#3092,.T.);
#2454=FACE_OUTER_BOUND('',#3093,.T.);
#2455=FACE_OUTER_BOUND('',#3094,.T.);
#2456=FACE_OUTER_BOUND('',#3095,.T.);
#2457=FACE_OUTER_BOUND('',#3096,.T.);
#2458=FACE_OUTER_BOUND('',#3097,.T.);
#2459=FACE_OUTER_BOUND('',#3098,.T.);
#2460=FACE_OUTER_BOUND('',#3099,.T.);
#2461=FACE_OUTER_BOUND('',#3100,.T.);
#2462=FACE_OUTER_BOUND('',#3101,.T.);
#2463=FACE_OUTER_BOUND('',#3102,.T.);
#2464=FACE_OUTER_BOUND('',#3103,.T.);
#2465=FACE_OUTER_BOUND('',#3104,.T.);
#2466=FACE_OUTER_BOUND('',#3105,.T.);
#2467=FACE_OUTER_BOUND('',#3106,.T.);
#2468=FACE_OUTER_BOUND('',#3107,.T.);
#2469=FACE_OUTER_BOUND('',#3108,.T.);
#2470=FACE_OUTER_BOUND('',#3109,.T.);
#2471=FACE_OUTER_BOUND('',#3110,.T.);
#2472=FACE_OUTER_BOUND('',#3111,.T.);
#2473=FACE_OUTER_BOUND('',#3112,.T.);
#2474=FACE_OUTER_BOUND('',#3113,.T.);
#2475=FACE_OUTER_BOUND('',#3114,.T.);
#2476=FACE_OUTER_BOUND('',#3115,.T.);
#2477=FACE_OUTER_BOUND('',#3116,.T.);
#2478=FACE_OUTER_BOUND('',#3117,.T.);
#2479=FACE_OUTER_BOUND('',#3118,.T.);
#2480=FACE_OUTER_BOUND('',#3119,.T.);
#2481=FACE_OUTER_BOUND('',#3120,.T.);
#2482=FACE_OUTER_BOUND('',#3121,.T.);
#2483=FACE_OUTER_BOUND('',#3122,.T.);
#2484=FACE_OUTER_BOUND('',#3123,.T.);
#2485=FACE_OUTER_BOUND('',#3124,.T.);
#2486=FACE_OUTER_BOUND('',#3125,.T.);
#2487=FACE_OUTER_BOUND('',#3126,.T.);
#2488=FACE_OUTER_BOUND('',#3127,.T.);
#2489=FACE_OUTER_BOUND('',#3128,.T.);
#2490=FACE_OUTER_BOUND('',#3150,.T.);
#2491=FACE_OUTER_BOUND('',#3151,.T.);
#2492=FACE_OUTER_BOUND('',#3152,.T.);
#2974=EDGE_LOOP('',(#7425,#7426,#7427,#7428));
#2975=EDGE_LOOP('',(#7429,#7430,#7431,#7432,#7433,#7434,#7435,#7436,#7437,
#7438,#7439,#7440));
#2976=EDGE_LOOP('',(#7441,#7442,#7443,#7444,#7445,#7446,#7447,#7448,#7449,
#7450,#7451,#7452,#7453,#7454,#7455,#7456,#7457,#7458,#7459,#7460,#7461,
#7462,#7463,#7464,#7465));
#2977=EDGE_LOOP('',(#7466,#7467,#7468,#7469));
#2978=EDGE_LOOP('',(#7470,#7471,#7472,#7473));
#2979=EDGE_LOOP('',(#7474,#7475,#7476,#7477));
#2980=EDGE_LOOP('',(#7478,#7479,#7480,#7481,#7482,#7483,#7484,#7485,#7486,
#7487,#7488,#7489));
#2981=EDGE_LOOP('',(#7490,#7491,#7492,#7493));
#2982=EDGE_LOOP('',(#7494,#7495,#7496,#7497));
#2983=EDGE_LOOP('',(#7498,#7499,#7500,#7501,#7502,#7503,#7504,#7505,#7506,
#7507,#7508,#7509));
#2984=EDGE_LOOP('',(#7510,#7511,#7512,#7513));
#2985=EDGE_LOOP('',(#7514,#7515,#7516,#7517,#7518,#7519,#7520,#7521,#7522,
#7523,#7524,#7525));
#2986=EDGE_LOOP('',(#7526,#7527,#7528,#7529));
#2987=EDGE_LOOP('',(#7530,#7531,#7532,#7533,#7534,#7535,#7536,#7537,#7538,
#7539,#7540,#7541));
#2988=EDGE_LOOP('',(#7542,#7543,#7544,#7545));
#2989=EDGE_LOOP('',(#7546,#7547,#7548,#7549,#7550,#7551,#7552,#7553,#7554,
#7555,#7556,#7557));
#2990=EDGE_LOOP('',(#7558,#7559,#7560,#7561));
#2991=EDGE_LOOP('',(#7562,#7563,#7564,#7565,#7566,#7567,#7568,#7569,#7570,
#7571,#7572,#7573));
#2992=EDGE_LOOP('',(#7574,#7575,#7576,#7577,#7578,#7579,#7580,#7581,#7582,
#7583,#7584,#7585,#7586,#7587,#7588,#7589,#7590,#7591,#7592,#7593));
#2993=EDGE_LOOP('',(#7594,#7595,#7596,#7597,#7598,#7599,#7600,#7601,#7602,
#7603,#7604,#7605));
#2994=EDGE_LOOP('',(#7606,#7607,#7608,#7609,#7610,#7611,#7612,#7613,#7614,
#7615,#7616,#7617,#7618,#7619,#7620,#7621,#7622,#7623,#7624,#7625));
#2995=EDGE_LOOP('',(#7626,#7627,#7628,#7629,#7630,#7631,#7632,#7633,#7634,
#7635,#7636,#7637,#7638,#7639,#7640,#7641,#7642,#7643,#7644,#7645));
#2996=EDGE_LOOP('',(#7646,#7647,#7648,#7649,#7650,#7651,#7652,#7653,#7654,
#7655,#7656,#7657,#7658,#7659,#7660,#7661,#7662,#7663,#7664,#7665));
#2997=EDGE_LOOP('',(#7666,#7667,#7668,#7669));
#2998=EDGE_LOOP('',(#7670,#7671,#7672,#7673,#7674,#7675,#7676,#7677,#7678,
#7679,#7680,#7681));
#2999=EDGE_LOOP('',(#7682,#7683,#7684,#7685));
#3000=EDGE_LOOP('',(#7686,#7687,#7688,#7689));
#3001=EDGE_LOOP('',(#7690,#7691,#7692,#7693));
#3002=EDGE_LOOP('',(#7694,#7695,#7696,#7697));
#3003=EDGE_LOOP('',(#7698,#7699,#7700,#7701));
#3004=EDGE_LOOP('',(#7702,#7703,#7704,#7705));
#3005=EDGE_LOOP('',(#7706,#7707,#7708,#7709));
#3006=EDGE_LOOP('',(#7710,#7711,#7712,#7713));
#3007=EDGE_LOOP('',(#7714,#7715,#7716,#7717));
#3008=EDGE_LOOP('',(#7718,#7719,#7720,#7721));
#3009=EDGE_LOOP('',(#7722,#7723,#7724,#7725));
#3010=EDGE_LOOP('',(#7726,#7727,#7728,#7729));
#3011=EDGE_LOOP('',(#7730,#7731,#7732,#7733));
#3012=EDGE_LOOP('',(#7734,#7735,#7736,#7737));
#3013=EDGE_LOOP('',(#7738,#7739,#7740,#7741));
#3014=EDGE_LOOP('',(#7742,#7743,#7744,#7745));
#3015=EDGE_LOOP('',(#7746,#7747,#7748,#7749));
#3016=EDGE_LOOP('',(#7750,#7751,#7752,#7753));
#3017=EDGE_LOOP('',(#7754,#7755,#7756,#7757));
#3018=EDGE_LOOP('',(#7758,#7759,#7760,#7761));
#3019=EDGE_LOOP('',(#7762,#7763,#7764,#7765));
#3020=EDGE_LOOP('',(#7766,#7767,#7768,#7769));
#3021=EDGE_LOOP('',(#7770,#7771,#7772,#7773));
#3022=EDGE_LOOP('',(#7774,#7775,#7776,#7777));
#3023=EDGE_LOOP('',(#7778,#7779,#7780,#7781));
#3024=EDGE_LOOP('',(#7782,#7783,#7784,#7785));
#3025=EDGE_LOOP('',(#7786,#7787,#7788,#7789));
#3026=EDGE_LOOP('',(#7790,#7791,#7792,#7793));
#3027=EDGE_LOOP('',(#7794,#7795,#7796,#7797));
#3028=EDGE_LOOP('',(#7798,#7799,#7800,#7801));
#3029=EDGE_LOOP('',(#7802,#7803,#7804,#7805));
#3030=EDGE_LOOP('',(#7806,#7807,#7808,#7809));
#3031=EDGE_LOOP('',(#7810,#7811,#7812,#7813));
#3032=EDGE_LOOP('',(#7814,#7815,#7816,#7817));
#3033=EDGE_LOOP('',(#7818,#7819,#7820,#7821));
#3034=EDGE_LOOP('',(#7822,#7823,#7824,#7825));
#3035=EDGE_LOOP('',(#7826,#7827,#7828,#7829,#7830));
#3036=EDGE_LOOP('',(#7831,#7832,#7833,#7834));
#3037=EDGE_LOOP('',(#7835,#7836,#7837,#7838,#7839));
#3038=EDGE_LOOP('',(#7840,#7841,#7842,#7843,#7844));
#3039=EDGE_LOOP('',(#7845,#7846,#7847,#7848));
#3040=EDGE_LOOP('',(#7849,#7850,#7851,#7852));
#3041=EDGE_LOOP('',(#7853,#7854,#7855,#7856));
#3042=EDGE_LOOP('',(#7857,#7858,#7859,#7860));
#3043=EDGE_LOOP('',(#7861,#7862,#7863,#7864,#7865,#7866,#7867,#7868,#7869,
#7870,#7871,#7872,#7873,#7874,#7875,#7876));
#3044=EDGE_LOOP('',(#7877,#7878,#7879,#7880));
#3045=EDGE_LOOP('',(#7881,#7882,#7883,#7884));
#3046=EDGE_LOOP('',(#7885,#7886,#7887,#7888));
#3047=EDGE_LOOP('',(#7889,#7890,#7891,#7892));
#3048=EDGE_LOOP('',(#7893,#7894,#7895,#7896));
#3049=EDGE_LOOP('',(#7897,#7898,#7899,#7900));
#3050=EDGE_LOOP('',(#7901,#7902,#7903,#7904));
#3051=EDGE_LOOP('',(#7905,#7906,#7907,#7908));
#3052=EDGE_LOOP('',(#7909,#7910,#7911,#7912));
#3053=EDGE_LOOP('',(#7913,#7914,#7915,#7916));
#3054=EDGE_LOOP('',(#7917,#7918,#7919,#7920));
#3055=EDGE_LOOP('',(#7921,#7922,#7923,#7924));
#3056=EDGE_LOOP('',(#7925,#7926,#7927,#7928));
#3057=EDGE_LOOP('',(#7929,#7930,#7931,#7932,#7933,#7934,#7935,#7936,#7937,
#7938,#7939,#7940,#7941,#7942,#7943,#7944,#7945,#7946,#7947,#7948,#7949,
#7950,#7951,#7952));
#3058=EDGE_LOOP('',(#7953));
#3059=EDGE_LOOP('',(#7954));
#3060=EDGE_LOOP('',(#7955));
#3061=EDGE_LOOP('',(#7956,#7957,#7958,#7959,#7960,#7961,#7962,#7963,#7964,
#7965,#7966,#7967));
#3062=EDGE_LOOP('',(#7968));
#3063=EDGE_LOOP('',(#7969));
#3064=EDGE_LOOP('',(#7970));
#3065=EDGE_LOOP('',(#7971));
#3066=EDGE_LOOP('',(#7972));
#3067=EDGE_LOOP('',(#7973,#7974,#7975));
#3068=EDGE_LOOP('',(#7976,#7977,#7978));
#3069=EDGE_LOOP('',(#7979,#7980,#7981,#7982));
#3070=EDGE_LOOP('',(#7983,#7984,#7985,#7986));
#3071=EDGE_LOOP('',(#7987,#7988,#7989,#7990));
#3072=EDGE_LOOP('',(#7991,#7992,#7993,#7994));
#3073=EDGE_LOOP('',(#7995,#7996,#7997,#7998));
#3074=EDGE_LOOP('',(#7999,#8000,#8001,#8002));
#3075=EDGE_LOOP('',(#8003,#8004,#8005));
#3076=EDGE_LOOP('',(#8006,#8007,#8008,#8009));
#3077=EDGE_LOOP('',(#8010,#8011,#8012));
#3078=EDGE_LOOP('',(#8013,#8014,#8015,#8016));
#3079=EDGE_LOOP('',(#8017,#8018,#8019));
#3080=EDGE_LOOP('',(#8020,#8021,#8022));
#3081=EDGE_LOOP('',(#8023,#8024,#8025,#8026));
#3082=EDGE_LOOP('',(#8027,#8028,#8029));
#3083=EDGE_LOOP('',(#8030,#8031,#8032,#8033));
#3084=EDGE_LOOP('',(#8034,#8035,#8036));
#3085=EDGE_LOOP('',(#8037,#8038,#8039,#8040));
#3086=EDGE_LOOP('',(#8041,#8042,#8043));
#3087=EDGE_LOOP('',(#8044,#8045,#8046));
#3088=EDGE_LOOP('',(#8047,#8048,#8049,#8050));
#3089=EDGE_LOOP('',(#8051,#8052,#8053,#8054));
#3090=EDGE_LOOP('',(#8055,#8056,#8057,#8058));
#3091=EDGE_LOOP('',(#8059,#8060,#8061));
#3092=EDGE_LOOP('',(#8062,#8063,#8064,#8065));
#3093=EDGE_LOOP('',(#8066,#8067,#8068));
#3094=EDGE_LOOP('',(#8069,#8070,#8071));
#3095=EDGE_LOOP('',(#8072,#8073,#8074,#8075));
#3096=EDGE_LOOP('',(#8076,#8077,#8078));
#3097=EDGE_LOOP('',(#8079,#8080,#8081));
#3098=EDGE_LOOP('',(#8082,#8083,#8084));
#3099=EDGE_LOOP('',(#8085,#8086,#8087,#8088));
#3100=EDGE_LOOP('',(#8089,#8090,#8091,#8092));
#3101=EDGE_LOOP('',(#8093,#8094,#8095,#8096));
#3102=EDGE_LOOP('',(#8097,#8098,#8099,#8100));
#3103=EDGE_LOOP('',(#8101,#8102,#8103,#8104));
#3104=EDGE_LOOP('',(#8105,#8106,#8107,#8108));
#3105=EDGE_LOOP('',(#8109,#8110,#8111,#8112));
#3106=EDGE_LOOP('',(#8113,#8114,#8115,#8116));
#3107=EDGE_LOOP('',(#8117,#8118,#8119,#8120));
#3108=EDGE_LOOP('',(#8121,#8122,#8123,#8124));
#3109=EDGE_LOOP('',(#8125,#8126,#8127,#8128));
#3110=EDGE_LOOP('',(#8129,#8130,#8131,#8132));
#3111=EDGE_LOOP('',(#8133,#8134,#8135,#8136));
#3112=EDGE_LOOP('',(#8137,#8138,#8139,#8140));
#3113=EDGE_LOOP('',(#8141,#8142,#8143,#8144));
#3114=EDGE_LOOP('',(#8145,#8146,#8147,#8148));
#3115=EDGE_LOOP('',(#8149,#8150,#8151,#8152));
#3116=EDGE_LOOP('',(#8153,#8154,#8155,#8156));
#3117=EDGE_LOOP('',(#8157,#8158,#8159,#8160));
#3118=EDGE_LOOP('',(#8161,#8162,#8163,#8164));
#3119=EDGE_LOOP('',(#8165,#8166,#8167,#8168));
#3120=EDGE_LOOP('',(#8169,#8170,#8171,#8172));
#3121=EDGE_LOOP('',(#8173,#8174,#8175,#8176));
#3122=EDGE_LOOP('',(#8177,#8178,#8179,#8180));
#3123=EDGE_LOOP('',(#8181,#8182,#8183,#8184,#8185,#8186,#8187,#8188,#8189,
#8190,#8191,#8192,#8193,#8194,#8195,#8196));
#3124=EDGE_LOOP('',(#8197,#8198,#8199,#8200));
#3125=EDGE_LOOP('',(#8201,#8202,#8203,#8204));
#3126=EDGE_LOOP('',(#8205,#8206,#8207,#8208));
#3127=EDGE_LOOP('',(#8209,#8210,#8211,#8212));
#3128=EDGE_LOOP('',(#8213,#8214,#8215,#8216));
#3129=EDGE_LOOP('',(#8217));
#3130=EDGE_LOOP('',(#8218));
#3131=EDGE_LOOP('',(#8219));
#3132=EDGE_LOOP('',(#8220));
#3133=EDGE_LOOP('',(#8221));
#3134=EDGE_LOOP('',(#8222));
#3135=EDGE_LOOP('',(#8223));
#3136=EDGE_LOOP('',(#8224));
#3137=EDGE_LOOP('',(#8225));
#3138=EDGE_LOOP('',(#8226));
#3139=EDGE_LOOP('',(#8227));
#3140=EDGE_LOOP('',(#8228));
#3141=EDGE_LOOP('',(#8229));
#3142=EDGE_LOOP('',(#8230));
#3143=EDGE_LOOP('',(#8231));
#3144=EDGE_LOOP('',(#8232));
#3145=EDGE_LOOP('',(#8233));
#3146=EDGE_LOOP('',(#8234));
#3147=EDGE_LOOP('',(#8235));
#3148=EDGE_LOOP('',(#8236));
#3149=EDGE_LOOP('',(#8237));
#3150=EDGE_LOOP('',(#8238,#8239,#8240,#8241));
#3151=EDGE_LOOP('',(#8242,#8243,#8244,#8245,#8246));
#3152=EDGE_LOOP('',(#8247,#8248,#8249,#8250,#8251,#8252,#8253,#8254,#8255,
#8256,#8257,#8258,#8259,#8260,#8261,#8262));
#3630=CIRCLE('',#10401,12.5);
#3631=CIRCLE('',#10402,12.5);
#3632=CIRCLE('',#10404,12.5);
#3633=CIRCLE('',#10405,12.5);
#3634=CIRCLE('',#10406,12.5);
#3635=CIRCLE('',#10407,12.5);
#3636=CIRCLE('',#10409,5.);
#3637=CIRCLE('',#10410,5.);
#3638=CIRCLE('',#10411,5.);
#3639=CIRCLE('',#10412,5.);
#3640=CIRCLE('',#10413,12.5);
#3641=CIRCLE('',#10414,5.);
#3642=CIRCLE('',#10415,5.);
#3643=CIRCLE('',#10416,5.);
#3644=CIRCLE('',#10417,5.);
#3645=CIRCLE('',#10418,5.);
#3646=CIRCLE('',#10419,5.);
#3647=CIRCLE('',#10421,0.499999999999998);
#3648=CIRCLE('',#10424,0.499999999999998);
#3649=CIRCLE('',#10426,5.);
#3650=CIRCLE('',#10427,5.);
#3651=CIRCLE('',#10429,5.);
#3652=CIRCLE('',#10430,5.);
#3653=CIRCLE('',#10432,5.);
#3654=CIRCLE('',#10433,5.);
#3655=CIRCLE('',#10435,5.);
#3656=CIRCLE('',#10436,5.);
#3657=CIRCLE('',#10437,5.);
#3658=CIRCLE('',#10439,12.5);
#3659=CIRCLE('',#10440,12.5);
#3660=CIRCLE('',#10442,5.);
#3661=CIRCLE('',#10443,5.);
#3662=CIRCLE('',#10444,5.);
#3663=CIRCLE('',#10446,5.);
#3664=CIRCLE('',#10447,5.);
#3665=CIRCLE('',#10449,5.);
#3666=CIRCLE('',#10450,5.);
#3667=CIRCLE('',#10451,5.);
#3668=CIRCLE('',#10453,5.);
#3669=CIRCLE('',#10454,5.);
#3670=CIRCLE('',#10456,5.);
#3671=CIRCLE('',#10457,5.);
#3672=CIRCLE('',#10459,5.);
#3673=CIRCLE('',#10460,5.);
#3674=CIRCLE('',#10462,5.);
#3675=CIRCLE('',#10463,5.);
#3676=CIRCLE('',#10464,5.);
#3677=CIRCLE('',#10466,5.);
#3678=CIRCLE('',#10467,5.);
#3679=CIRCLE('',#10468,5.);
#3680=CIRCLE('',#10469,5.);
#3681=CIRCLE('',#10471,5.);
#3682=CIRCLE('',#10473,5.);
#3683=CIRCLE('',#10475,12.5);
#3684=CIRCLE('',#10476,12.5);
#3685=CIRCLE('',#10477,12.5);
#3686=CIRCLE('',#10479,5.);
#3687=CIRCLE('',#10480,5.);
#3688=CIRCLE('',#10481,5.);
#3689=CIRCLE('',#10482,5.);
#3690=CIRCLE('',#10484,5.);
#3691=CIRCLE('',#10486,5.);
#3692=CIRCLE('',#10488,5.);
#3693=CIRCLE('',#10489,5.);
#3694=CIRCLE('',#10490,5.);
#3695=CIRCLE('',#10491,5.);
#3696=CIRCLE('',#10493,5.);
#3697=CIRCLE('',#10495,5.);
#3698=CIRCLE('',#10497,5.);
#3699=CIRCLE('',#10498,5.);
#3700=CIRCLE('',#10499,5.);
#3701=CIRCLE('',#10500,5.);
#3702=CIRCLE('',#10502,5.);
#3703=CIRCLE('',#10504,5.);
#3704=CIRCLE('',#10506,5.);
#3705=CIRCLE('',#10507,5.);
#3706=CIRCLE('',#10509,5.);
#3707=CIRCLE('',#10510,5.);
#3708=CIRCLE('',#10513,0.5);
#3709=CIRCLE('',#10516,0.499999999999998);
#3710=CIRCLE('',#10524,0.499999999999998);
#3711=CIRCLE('',#10527,0.5);
#3712=CIRCLE('',#10529,0.499999999999999);
#3713=CIRCLE('',#10532,0.5);
#3714=CIRCLE('',#10541,0.499999999999999);
#3715=CIRCLE('',#10544,0.499999999999998);
#3716=CIRCLE('',#10547,0.5);
#3717=CIRCLE('',#10550,0.499999999999998);
#3718=CIRCLE('',#10562,0.5);
#3719=CIRCLE('',#10565,0.499999999999999);
#3720=CIRCLE('',#10570,0.499999999999998);
#3721=CIRCLE('',#10580,0.499999999999998);
#3722=CIRCLE('',#10586,0.500000000000025);
#3723=CIRCLE('',#10587,0.499999999999998);
#3724=CIRCLE('',#10589,0.500000000000007);
#3725=CIRCLE('',#10590,0.500000000000005);
#3726=CIRCLE('',#10592,0.500000000000007);
#3727=CIRCLE('',#10593,0.999999999999996);
#3728=CIRCLE('',#10594,0.5);
#3729=CIRCLE('',#10597,1.);
#3730=CIRCLE('',#10598,0.500000000000002);
#3731=CIRCLE('',#10599,0.500000000000007);
#3732=CIRCLE('',#10601,0.500000000000007);
#3733=CIRCLE('',#10602,1.);
#3734=CIRCLE('',#10603,0.499999999999998);
#3735=CIRCLE('',#10605,1.00000000000001);
#3736=CIRCLE('',#10606,0.499999999999998);
#3737=CIRCLE('',#10607,0.500000000000007);
#3738=CIRCLE('',#10610,0.500000000000007);
#3739=CIRCLE('',#10611,0.499999999999999);
#3740=CIRCLE('',#10614,0.500000000000007);
#3741=CIRCLE('',#10615,0.499999999999998);
#3742=CIRCLE('',#10616,0.499999999999998);
#3743=CIRCLE('',#10619,0.500000000000007);
#3744=CIRCLE('',#10620,0.5);
#3745=CIRCLE('',#10622,0.499999999999998);
#3746=CIRCLE('',#10623,0.500000000000007);
#3747=CIRCLE('',#10624,0.500000000000007);
#3748=CIRCLE('',#10627,0.500000000000007);
#3749=CIRCLE('',#10628,0.499999999999998);
#3750=CIRCLE('',#10631,0.500000000000007);
#3751=CIRCLE('',#10632,0.500000000000007);
#3752=CIRCLE('',#10633,0.499999999999998);
#3753=CIRCLE('',#10636,0.500000000000007);
#3754=CIRCLE('',#10637,0.499999999999999);
#3755=CIRCLE('',#10639,0.499999999999998);
#3756=CIRCLE('',#10640,0.500000000000007);
#3757=CIRCLE('',#10641,0.499999999999998);
#3758=CIRCLE('',#10644,0.500000000000007);
#3759=CIRCLE('',#10645,0.999999999999996);
#3760=CIRCLE('',#10646,0.499999999999998);
#3761=CIRCLE('',#10649,0.499999999999998);
#3762=CIRCLE('',#10650,0.500000000000007);
#3763=CIRCLE('',#10651,0.499999999999998);
#3764=CIRCLE('',#10653,0.500000000000007);
#3765=CIRCLE('',#10654,0.999999999999999);
#3766=CIRCLE('',#10655,0.499999999999998);
#3767=CIRCLE('',#10657,0.500000000000007);
#3768=CIRCLE('',#10658,0.500000000000007);
#3769=CIRCLE('',#10659,0.499999999999998);
#3770=CIRCLE('',#10661,0.500000000000007);
#3771=CIRCLE('',#10662,0.500000000000007);
#3772=CIRCLE('',#10665,0.500000000000007);
#3773=CIRCLE('',#10666,0.499999999999998);
#3774=CIRCLE('',#10667,0.500000000000007);
#3775=CIRCLE('',#10669,0.500000000000007);
#3776=CIRCLE('',#10670,0.499999999999998);
#3777=CIRCLE('',#10672,0.500000000000007);
#3778=CIRCLE('',#10673,0.499999999999998);
#3779=CIRCLE('',#10674,0.499999999999998);
#3780=CIRCLE('',#10676,0.500000000000007);
#3781=CIRCLE('',#10677,1.00000000000001);
#3782=CIRCLE('',#10678,0.499999999999998);
#3783=CIRCLE('',#10682,0.500000000000007);
#3784=CIRCLE('',#10683,0.999999999999996);
#3785=CIRCLE('',#10684,0.500000000000007);
#4302=VERTEX_POINT('',#15614);
#4303=VERTEX_POINT('',#15616);
#4304=VERTEX_POINT('',#15620);
#4305=VERTEX_POINT('',#15622);
#4306=VERTEX_POINT('',#15624);
#4307=VERTEX_POINT('',#15626);
#4308=VERTEX_POINT('',#15637);
#4309=VERTEX_POINT('',#15639);
#4310=VERTEX_POINT('',#15650);
#4311=VERTEX_POINT('',#15652);
#4312=VERTEX_POINT('',#15663);
#4313=VERTEX_POINT('',#15665);
#4314=VERTEX_POINT('',#15678);
#4315=VERTEX_POINT('',#15680);
#4316=VERTEX_POINT('',#15682);
#4317=VERTEX_POINT('',#15684);
#4318=VERTEX_POINT('',#15686);
#4319=VERTEX_POINT('',#15688);
#4320=VERTEX_POINT('',#15690);
#4321=VERTEX_POINT('',#15692);
#4322=VERTEX_POINT('',#15694);
#4323=VERTEX_POINT('',#15696);
#4324=VERTEX_POINT('',#15698);
#4325=VERTEX_POINT('',#15700);
#4326=VERTEX_POINT('',#15702);
#4327=VERTEX_POINT('',#15704);
#4328=VERTEX_POINT('',#15706);
#4329=VERTEX_POINT('',#15708);
#4330=VERTEX_POINT('',#15710);
#4331=VERTEX_POINT('',#15712);
#4332=VERTEX_POINT('',#15714);
#4333=VERTEX_POINT('',#15716);
#4334=VERTEX_POINT('',#15718);
#4335=VERTEX_POINT('',#15720);
#4336=VERTEX_POINT('',#15722);
#4337=VERTEX_POINT('',#15726);
#4338=VERTEX_POINT('',#15730);
#4339=VERTEX_POINT('',#15734);
#4340=VERTEX_POINT('',#15738);
#4341=VERTEX_POINT('',#15741);
#4342=VERTEX_POINT('',#15752);
#4343=VERTEX_POINT('',#15754);
#4344=VERTEX_POINT('',#15765);
#4345=VERTEX_POINT('',#15767);
#4346=VERTEX_POINT('',#15778);
#4347=VERTEX_POINT('',#15791);
#4348=VERTEX_POINT('',#15793);
#4349=VERTEX_POINT('',#15797);
#4350=VERTEX_POINT('',#15799);
#4351=VERTEX_POINT('',#15803);
#4352=VERTEX_POINT('',#15805);
#4353=VERTEX_POINT('',#15807);
#4354=VERTEX_POINT('',#15809);
#4355=VERTEX_POINT('',#15820);
#4356=VERTEX_POINT('',#15832);
#4357=VERTEX_POINT('',#15843);
#4358=VERTEX_POINT('',#15845);
#4359=VERTEX_POINT('',#15858);
#4360=VERTEX_POINT('',#15860);
#4361=VERTEX_POINT('',#15864);
#4362=VERTEX_POINT('',#15866);
#4363=VERTEX_POINT('',#15868);
#4364=VERTEX_POINT('',#15870);
#4365=VERTEX_POINT('',#15881);
#4366=VERTEX_POINT('',#15893);
#4367=VERTEX_POINT('',#15904);
#4368=VERTEX_POINT('',#15906);
#4369=VERTEX_POINT('',#15919);
#4370=VERTEX_POINT('',#15921);
#4371=VERTEX_POINT('',#15925);
#4372=VERTEX_POINT('',#15927);
#4373=VERTEX_POINT('',#15929);
#4374=VERTEX_POINT('',#15931);
#4375=VERTEX_POINT('',#15942);
#4376=VERTEX_POINT('',#15954);
#4377=VERTEX_POINT('',#15965);
#4378=VERTEX_POINT('',#15967);
#4379=VERTEX_POINT('',#15980);
#4380=VERTEX_POINT('',#15982);
#4381=VERTEX_POINT('',#15986);
#4382=VERTEX_POINT('',#15989);
#4383=VERTEX_POINT('',#16000);
#4384=VERTEX_POINT('',#16002);
#4385=VERTEX_POINT('',#16013);
#4386=VERTEX_POINT('',#16015);
#4387=VERTEX_POINT('',#16026);
#4388=VERTEX_POINT('',#16039);
#4389=VERTEX_POINT('',#16041);
#4390=VERTEX_POINT('',#16045);
#4391=VERTEX_POINT('',#16047);
#4392=VERTEX_POINT('',#16049);
#4393=VERTEX_POINT('',#16051);
#4394=VERTEX_POINT('',#16062);
#4395=VERTEX_POINT('',#16074);
#4396=VERTEX_POINT('',#16085);
#4397=VERTEX_POINT('',#16087);
#4398=VERTEX_POINT('',#16100);
#4399=VERTEX_POINT('',#16102);
#4400=VERTEX_POINT('',#16104);
#4401=VERTEX_POINT('',#16106);
#4402=VERTEX_POINT('',#16117);
#4403=VERTEX_POINT('',#16119);
#4404=VERTEX_POINT('',#16130);
#4405=VERTEX_POINT('',#16132);
#4406=VERTEX_POINT('',#16143);
#4407=VERTEX_POINT('',#16145);
#4408=VERTEX_POINT('',#16156);
#4409=VERTEX_POINT('',#16158);
#4410=VERTEX_POINT('',#16180);
#4411=VERTEX_POINT('',#16182);
#4412=VERTEX_POINT('',#16199);
#4413=VERTEX_POINT('',#16201);
#4414=VERTEX_POINT('',#16218);
#4415=VERTEX_POINT('',#16220);
#4416=VERTEX_POINT('',#16244);
#4417=VERTEX_POINT('',#16246);
#4418=VERTEX_POINT('',#16248);
#4419=VERTEX_POINT('',#16250);
#4420=VERTEX_POINT('',#16261);
#4421=VERTEX_POINT('',#16273);
#4422=VERTEX_POINT('',#16284);
#4423=VERTEX_POINT('',#16286);
#4424=VERTEX_POINT('',#16299);
#4425=VERTEX_POINT('',#16301);
#4426=VERTEX_POINT('',#16303);
#4427=VERTEX_POINT('',#16305);
#4428=VERTEX_POINT('',#16316);
#4429=VERTEX_POINT('',#16318);
#4430=VERTEX_POINT('',#16329);
#4431=VERTEX_POINT('',#16331);
#4432=VERTEX_POINT('',#16342);
#4433=VERTEX_POINT('',#16344);
#4434=VERTEX_POINT('',#16355);
#4435=VERTEX_POINT('',#16357);
#4436=VERTEX_POINT('',#16379);
#4437=VERTEX_POINT('',#16381);
#4438=VERTEX_POINT('',#16398);
#4439=VERTEX_POINT('',#16400);
#4440=VERTEX_POINT('',#16417);
#4441=VERTEX_POINT('',#16419);
#4442=VERTEX_POINT('',#16443);
#4443=VERTEX_POINT('',#16445);
#4444=VERTEX_POINT('',#16447);
#4445=VERTEX_POINT('',#16449);
#4446=VERTEX_POINT('',#16460);
#4447=VERTEX_POINT('',#16462);
#4448=VERTEX_POINT('',#16473);
#4449=VERTEX_POINT('',#16475);
#4450=VERTEX_POINT('',#16486);
#4451=VERTEX_POINT('',#16488);
#4452=VERTEX_POINT('',#16499);
#4453=VERTEX_POINT('',#16501);
#4454=VERTEX_POINT('',#16523);
#4455=VERTEX_POINT('',#16525);
#4456=VERTEX_POINT('',#16542);
#4457=VERTEX_POINT('',#16544);
#4458=VERTEX_POINT('',#16561);
#4459=VERTEX_POINT('',#16563);
#4460=VERTEX_POINT('',#16587);
#4461=VERTEX_POINT('',#16589);
#4462=VERTEX_POINT('',#16591);
#4463=VERTEX_POINT('',#16593);
#4464=VERTEX_POINT('',#16604);
#4465=VERTEX_POINT('',#16606);
#4466=VERTEX_POINT('',#16617);
#4467=VERTEX_POINT('',#16619);
#4468=VERTEX_POINT('',#16630);
#4469=VERTEX_POINT('',#16632);
#4470=VERTEX_POINT('',#16643);
#4471=VERTEX_POINT('',#16645);
#4472=VERTEX_POINT('',#16667);
#4473=VERTEX_POINT('',#16669);
#4474=VERTEX_POINT('',#16686);
#4475=VERTEX_POINT('',#16688);
#4476=VERTEX_POINT('',#16705);
#4477=VERTEX_POINT('',#16707);
#4478=VERTEX_POINT('',#16731);
#4479=VERTEX_POINT('',#16733);
#4480=VERTEX_POINT('',#16737);
#4481=VERTEX_POINT('',#16740);
#4482=VERTEX_POINT('',#16751);
#4483=VERTEX_POINT('',#16753);
#4484=VERTEX_POINT('',#16764);
#4485=VERTEX_POINT('',#16766);
#4486=VERTEX_POINT('',#16777);
#4487=VERTEX_POINT('',#16792);
#4488=VERTEX_POINT('',#16798);
#4489=VERTEX_POINT('',#16804);
#4490=VERTEX_POINT('',#16810);
#4491=VERTEX_POINT('',#16818);
#4492=VERTEX_POINT('',#16824);
#4493=VERTEX_POINT('',#16828);
#4494=VERTEX_POINT('',#16830);
#4495=VERTEX_POINT('',#16837);
#4496=VERTEX_POINT('',#16839);
#4497=VERTEX_POINT('',#16849);
#4498=VERTEX_POINT('',#16855);
#4499=VERTEX_POINT('',#16863);
#4500=VERTEX_POINT('',#16865);
#4501=VERTEX_POINT('',#16872);
#4502=VERTEX_POINT('',#16874);
#4503=VERTEX_POINT('',#16881);
#4504=VERTEX_POINT('',#16887);
#4505=VERTEX_POINT('',#16895);
#4506=VERTEX_POINT('',#16901);
#4507=VERTEX_POINT('',#16907);
#4508=VERTEX_POINT('',#16911);
#4509=VERTEX_POINT('',#16929);
#4510=VERTEX_POINT('',#16931);
#4511=VERTEX_POINT('',#16933);
#4512=VERTEX_POINT('',#16939);
#4513=VERTEX_POINT('',#16949);
#4514=VERTEX_POINT('',#16969);
#4515=VERTEX_POINT('',#16971);
#4516=VERTEX_POINT('',#16975);
#4517=VERTEX_POINT('',#16979);
#4518=VERTEX_POINT('',#16983);
#4519=VERTEX_POINT('',#16985);
#4520=VERTEX_POINT('',#16991);
#4521=VERTEX_POINT('',#16992);
#4522=VERTEX_POINT('',#16997);
#4523=VERTEX_POINT('',#16999);
#4524=VERTEX_POINT('',#17003);
#4525=VERTEX_POINT('',#17004);
#4526=VERTEX_POINT('',#17011);
#4527=VERTEX_POINT('',#17017);
#4528=VERTEX_POINT('',#17018);
#4529=VERTEX_POINT('',#17025);
#4530=VERTEX_POINT('',#17029);
#4531=VERTEX_POINT('',#17031);
#4532=VERTEX_POINT('',#17037);
#4533=VERTEX_POINT('',#17043);
#4534=VERTEX_POINT('',#17044);
#4535=VERTEX_POINT('',#17046);
#4536=VERTEX_POINT('',#17053);
#4537=VERTEX_POINT('',#17057);
#4538=VERTEX_POINT('',#17058);
#4539=VERTEX_POINT('',#17060);
#4540=VERTEX_POINT('',#17067);
#4541=VERTEX_POINT('',#17069);
#4542=VERTEX_POINT('',#17075);
#4543=VERTEX_POINT('',#17076);
#4544=VERTEX_POINT('',#17078);
#4545=VERTEX_POINT('',#17082);
#4546=VERTEX_POINT('',#17084);
#4547=VERTEX_POINT('',#17088);
#4548=VERTEX_POINT('',#17089);
#4549=VERTEX_POINT('',#17091);
#4550=VERTEX_POINT('',#17095);
#4551=VERTEX_POINT('',#17101);
#4552=VERTEX_POINT('',#17102);
#4553=VERTEX_POINT('',#17107);
#4554=VERTEX_POINT('',#17111);
#4555=VERTEX_POINT('',#17112);
#4556=VERTEX_POINT('',#17117);
#4557=VERTEX_POINT('',#17119);
#4558=VERTEX_POINT('',#17127);
#4559=VERTEX_POINT('',#17129);
#5383=EDGE_CURVE('',#4302,#4302,#3630,.T.);
#5384=EDGE_CURVE('',#4302,#4303,#973,.T.);
#5385=EDGE_CURVE('',#4303,#4303,#3631,.T.);
#5386=EDGE_CURVE('',#4304,#4304,#3632,.T.);
#5387=EDGE_CURVE('',#4304,#4305,#974,.T.);
#5388=EDGE_CURVE('',#4306,#4305,#3633,.T.);
#5389=EDGE_CURVE('',#4307,#4306,#51,.T.);
#5390=EDGE_CURVE('',#4308,#4307,#975,.T.);
#5391=EDGE_CURVE('',#4309,#4308,#52,.T.);
#5392=EDGE_CURVE('',#4310,#4309,#3634,.T.);
#5393=EDGE_CURVE('',#4311,#4310,#53,.T.);
#5394=EDGE_CURVE('',#4312,#4311,#976,.T.);
#5395=EDGE_CURVE('',#4313,#4312,#54,.T.);
#5396=EDGE_CURVE('',#4305,#4313,#3635,.T.);
#5397=EDGE_CURVE('',#4314,#4309,#977,.T.);
#5398=EDGE_CURVE('',#4315,#4314,#978,.T.);
#5399=EDGE_CURVE('',#4316,#4315,#979,.T.);
#5400=EDGE_CURVE('',#4316,#4317,#3636,.T.);
#5401=EDGE_CURVE('',#4318,#4317,#980,.T.);
#5402=EDGE_CURVE('',#4318,#4319,#3637,.T.);
#5403=EDGE_CURVE('',#4320,#4319,#981,.T.);
#5404=EDGE_CURVE('',#4320,#4321,#3638,.T.);
#5405=EDGE_CURVE('',#4322,#4321,#982,.T.);
#5406=EDGE_CURVE('',#4322,#4323,#3639,.T.);
#5407=EDGE_CURVE('',#4324,#4323,#983,.T.);
#5408=EDGE_CURVE('',#4325,#4324,#984,.T.);
#5409=EDGE_CURVE('',#4326,#4325,#985,.T.);
#5410=EDGE_CURVE('',#4326,#4327,#3640,.T.);
#5411=EDGE_CURVE('',#4328,#4327,#986,.T.);
#5412=EDGE_CURVE('',#4328,#4329,#3641,.T.);
#5413=EDGE_CURVE('',#4329,#4330,#3642,.T.);
#5414=EDGE_CURVE('',#4331,#4330,#987,.T.);
#5415=EDGE_CURVE('',#4331,#4332,#3643,.T.);
#5416=EDGE_CURVE('',#4332,#4333,#3644,.T.);
#5417=EDGE_CURVE('',#4334,#4333,#988,.T.);
#5418=EDGE_CURVE('',#4334,#4335,#3645,.T.);
#5419=EDGE_CURVE('',#4335,#4336,#3646,.T.);
#5420=EDGE_CURVE('',#4310,#4336,#989,.T.);
#5421=EDGE_CURVE('',#4308,#4337,#990,.T.);
#5422=EDGE_CURVE('',#4337,#4314,#3647,.F.);
#5423=EDGE_CURVE('',#4338,#4307,#991,.T.);
#5424=EDGE_CURVE('',#4337,#4338,#992,.T.);
#5425=EDGE_CURVE('',#4306,#4339,#993,.T.);
#5426=EDGE_CURVE('',#4339,#4338,#3648,.F.);
#5427=EDGE_CURVE('',#4340,#4340,#3649,.T.);
#5428=EDGE_CURVE('',#4340,#4329,#994,.T.);
#5429=EDGE_CURVE('',#4341,#4328,#55,.T.);
#5430=EDGE_CURVE('',#4342,#4341,#995,.T.);
#5431=EDGE_CURVE('',#4343,#4342,#56,.T.);
#5432=EDGE_CURVE('',#4344,#4343,#3650,.T.);
#5433=EDGE_CURVE('',#4345,#4344,#57,.T.);
#5434=EDGE_CURVE('',#4346,#4345,#996,.T.);
#5435=EDGE_CURVE('',#4330,#4346,#58,.T.);
#5436=EDGE_CURVE('',#4347,#4347,#3651,.T.);
#5437=EDGE_CURVE('',#4347,#4348,#997,.T.);
#5438=EDGE_CURVE('',#4348,#4348,#3652,.T.);
#5439=EDGE_CURVE('',#4349,#4349,#3653,.T.);
#5440=EDGE_CURVE('',#4349,#4350,#998,.T.);
#5441=EDGE_CURVE('',#4350,#4350,#3654,.T.);
#5442=EDGE_CURVE('',#4351,#4351,#3655,.T.);
#5443=EDGE_CURVE('',#4351,#4352,#999,.T.);
#5444=EDGE_CURVE('',#4353,#4352,#3656,.T.);
#5445=EDGE_CURVE('',#4354,#4353,#59,.T.);
#5446=EDGE_CURVE('',#4355,#4354,#1000,.T.);
#5447=EDGE_CURVE('',#4323,#4355,#60,.T.);
#5448=EDGE_CURVE('',#4356,#4322,#61,.T.);
#5449=EDGE_CURVE('',#4357,#4356,#1001,.T.);
#5450=EDGE_CURVE('',#4358,#4357,#62,.T.);
#5451=EDGE_CURVE('',#4352,#4358,#3657,.T.);
#5452=EDGE_CURVE('',#4359,#4359,#3658,.T.);
#5453=EDGE_CURVE('',#4359,#4360,#1002,.T.);
#5454=EDGE_CURVE('',#4360,#4360,#3659,.T.);
#5455=EDGE_CURVE('',#4361,#4361,#3660,.T.);
#5456=EDGE_CURVE('',#4361,#4362,#1003,.T.);
#5457=EDGE_CURVE('',#4363,#4362,#3661,.T.);
#5458=EDGE_CURVE('',#4364,#4363,#63,.T.);
#5459=EDGE_CURVE('',#4365,#4364,#1004,.T.);
#5460=EDGE_CURVE('',#4321,#4365,#64,.T.);
#5461=EDGE_CURVE('',#4366,#4320,#65,.T.);
#5462=EDGE_CURVE('',#4367,#4366,#1005,.T.);
#5463=EDGE_CURVE('',#4368,#4367,#66,.T.);
#5464=EDGE_CURVE('',#4362,#4368,#3662,.T.);
#5465=EDGE_CURVE('',#4369,#4369,#3663,.T.);
#5466=EDGE_CURVE('',#4369,#4370,#1006,.T.);
#5467=EDGE_CURVE('',#4370,#4370,#3664,.T.);
#5468=EDGE_CURVE('',#4371,#4371,#3665,.T.);
#5469=EDGE_CURVE('',#4371,#4372,#1007,.T.);
#5470=EDGE_CURVE('',#4373,#4372,#3666,.T.);
#5471=EDGE_CURVE('',#4374,#4373,#67,.T.);
#5472=EDGE_CURVE('',#4375,#4374,#1008,.T.);
#5473=EDGE_CURVE('',#4317,#4375,#68,.T.);
#5474=EDGE_CURVE('',#4376,#4316,#69,.T.);
#5475=EDGE_CURVE('',#4377,#4376,#1009,.T.);
#5476=EDGE_CURVE('',#4378,#4377,#70,.T.);
#5477=EDGE_CURVE('',#4372,#4378,#3667,.T.);
#5478=EDGE_CURVE('',#4379,#4379,#3668,.T.);
#5479=EDGE_CURVE('',#4379,#4380,#1010,.T.);
#5480=EDGE_CURVE('',#4380,#4380,#3669,.T.);
#5481=EDGE_CURVE('',#4381,#4381,#3670,.T.);
#5482=EDGE_CURVE('',#4381,#4332,#1011,.T.);
#5483=EDGE_CURVE('',#4382,#4331,#71,.T.);
#5484=EDGE_CURVE('',#4383,#4382,#1012,.T.);
#5485=EDGE_CURVE('',#4384,#4383,#72,.T.);
#5486=EDGE_CURVE('',#4385,#4384,#3671,.T.);
#5487=EDGE_CURVE('',#4386,#4385,#73,.T.);
#5488=EDGE_CURVE('',#4387,#4386,#1013,.T.);
#5489=EDGE_CURVE('',#4333,#4387,#74,.T.);
#5490=EDGE_CURVE('',#4388,#4388,#3672,.T.);
#5491=EDGE_CURVE('',#4388,#4389,#1014,.T.);
#5492=EDGE_CURVE('',#4389,#4389,#3673,.T.);
#5493=EDGE_CURVE('',#4390,#4390,#3674,.T.);
#5494=EDGE_CURVE('',#4390,#4391,#1015,.T.);
#5495=EDGE_CURVE('',#4392,#4391,#3675,.T.);
#5496=EDGE_CURVE('',#4393,#4392,#75,.T.);
#5497=EDGE_CURVE('',#4394,#4393,#1016,.T.);
#5498=EDGE_CURVE('',#4319,#4394,#76,.T.);
#5499=EDGE_CURVE('',#4395,#4318,#77,.T.);
#5500=EDGE_CURVE('',#4396,#4395,#1017,.T.);
#5501=EDGE_CURVE('',#4397,#4396,#78,.T.);
#5502=EDGE_CURVE('',#4391,#4397,#3676,.T.);
#5503=EDGE_CURVE('',#4398,#4398,#3677,.T.);
#5504=EDGE_CURVE('',#4398,#4399,#1018,.T.);
#5505=EDGE_CURVE('',#4400,#4399,#3678,.T.);
#5506=EDGE_CURVE('',#4401,#4400,#79,.T.);
#5507=EDGE_CURVE('',#4402,#4401,#1019,.T.);
#5508=EDGE_CURVE('',#4403,#4402,#80,.T.);
#5509=EDGE_CURVE('',#4404,#4403,#3679,.T.);
#5510=EDGE_CURVE('',#4405,#4404,#81,.T.);
#5511=EDGE_CURVE('',#4406,#4405,#1020,.T.);
#5512=EDGE_CURVE('',#4407,#4406,#82,.T.);
#5513=EDGE_CURVE('',#4408,#4407,#3680,.T.);
#5514=EDGE_CURVE('',#4409,#4408,#83,.T.);
#5515=EDGE_CURVE('',#4410,#4409,#273,.T.);
#5516=EDGE_CURVE('',#4411,#4410,#84,.T.);
#5517=EDGE_CURVE('',#4412,#4411,#3681,.T.);
#5518=EDGE_CURVE('',#4413,#4412,#85,.T.);
#5519=EDGE_CURVE('',#4414,#4413,#274,.T.);
#5520=EDGE_CURVE('',#4415,#4414,#86,.T.);
#5521=EDGE_CURVE('',#4399,#4415,#3682,.T.);
#5522=EDGE_CURVE('',#4416,#4416,#3683,.T.);
#5523=EDGE_CURVE('',#4416,#4417,#1021,.T.);
#5524=EDGE_CURVE('',#4418,#4417,#3684,.T.);
#5525=EDGE_CURVE('',#4419,#4418,#87,.T.);
#5526=EDGE_CURVE('',#4420,#4419,#1022,.T.);
#5527=EDGE_CURVE('',#4327,#4420,#88,.T.);
#5528=EDGE_CURVE('',#4421,#4326,#89,.T.);
#5529=EDGE_CURVE('',#4422,#4421,#1023,.T.);
#5530=EDGE_CURVE('',#4423,#4422,#90,.T.);
#5531=EDGE_CURVE('',#4417,#4423,#3685,.T.);
#5532=EDGE_CURVE('',#4424,#4424,#3686,.T.);
#5533=EDGE_CURVE('',#4424,#4425,#1024,.T.);
#5534=EDGE_CURVE('',#4426,#4425,#3687,.T.);
#5535=EDGE_CURVE('',#4427,#4426,#91,.T.);
#5536=EDGE_CURVE('',#4428,#4427,#1025,.T.);
#5537=EDGE_CURVE('',#4429,#4428,#92,.T.);
#5538=EDGE_CURVE('',#4430,#4429,#3688,.T.);
#5539=EDGE_CURVE('',#4431,#4430,#93,.T.);
#5540=EDGE_CURVE('',#4432,#4431,#1026,.T.);
#5541=EDGE_CURVE('',#4433,#4432,#94,.T.);
#5542=EDGE_CURVE('',#4434,#4433,#3689,.T.);
#5543=EDGE_CURVE('',#4435,#4434,#95,.T.);
#5544=EDGE_CURVE('',#4436,#4435,#275,.T.);
#5545=EDGE_CURVE('',#4437,#4436,#96,.T.);
#5546=EDGE_CURVE('',#4438,#4437,#3690,.T.);
#5547=EDGE_CURVE('',#4439,#4438,#97,.T.);
#5548=EDGE_CURVE('',#4440,#4439,#276,.T.);
#5549=EDGE_CURVE('',#4441,#4440,#98,.T.);
#5550=EDGE_CURVE('',#4425,#4441,#3691,.T.);
#5551=EDGE_CURVE('',#4442,#4442,#3692,.T.);
#5552=EDGE_CURVE('',#4442,#4443,#1027,.T.);
#5553=EDGE_CURVE('',#4444,#4443,#3693,.T.);
#5554=EDGE_CURVE('',#4445,#4444,#99,.T.);
#5555=EDGE_CURVE('',#4446,#4445,#1028,.T.);
#5556=EDGE_CURVE('',#4447,#4446,#100,.T.);
#5557=EDGE_CURVE('',#4448,#4447,#3694,.T.);
#5558=EDGE_CURVE('',#4449,#4448,#101,.T.);
#5559=EDGE_CURVE('',#4450,#4449,#1029,.T.);
#5560=EDGE_CURVE('',#4451,#4450,#102,.T.);
#5561=EDGE_CURVE('',#4452,#4451,#3695,.T.);
#5562=EDGE_CURVE('',#4453,#4452,#103,.T.);
#5563=EDGE_CURVE('',#4454,#4453,#277,.T.);
#5564=EDGE_CURVE('',#4455,#4454,#104,.T.);
#5565=EDGE_CURVE('',#4456,#4455,#3696,.T.);
#5566=EDGE_CURVE('',#4457,#4456,#105,.T.);
#5567=EDGE_CURVE('',#4458,#4457,#278,.T.);
#5568=EDGE_CURVE('',#4459,#4458,#106,.T.);
#5569=EDGE_CURVE('',#4443,#4459,#3697,.T.);
#5570=EDGE_CURVE('',#4460,#4460,#3698,.T.);
#5571=EDGE_CURVE('',#4460,#4461,#1030,.T.);
#5572=EDGE_CURVE('',#4462,#4461,#3699,.T.);
#5573=EDGE_CURVE('',#4463,#4462,#107,.T.);
#5574=EDGE_CURVE('',#4464,#4463,#1031,.T.);
#5575=EDGE_CURVE('',#4465,#4464,#108,.T.);
#5576=EDGE_CURVE('',#4466,#4465,#3700,.T.);
#5577=EDGE_CURVE('',#4467,#4466,#109,.T.);
#5578=EDGE_CURVE('',#4468,#4467,#1032,.T.);
#5579=EDGE_CURVE('',#4469,#4468,#110,.T.);
#5580=EDGE_CURVE('',#4470,#4469,#3701,.T.);
#5581=EDGE_CURVE('',#4471,#4470,#111,.T.);
#5582=EDGE_CURVE('',#4472,#4471,#279,.T.);
#5583=EDGE_CURVE('',#4473,#4472,#112,.T.);
#5584=EDGE_CURVE('',#4474,#4473,#3702,.T.);
#5585=EDGE_CURVE('',#4475,#4474,#113,.T.);
#5586=EDGE_CURVE('',#4476,#4475,#280,.T.);
#5587=EDGE_CURVE('',#4477,#4476,#114,.T.);
#5588=EDGE_CURVE('',#4461,#4477,#3703,.T.);
#5589=EDGE_CURVE('',#4478,#4478,#3704,.T.);
#5590=EDGE_CURVE('',#4478,#4479,#1033,.T.);
#5591=EDGE_CURVE('',#4479,#4479,#3705,.T.);
#5592=EDGE_CURVE('',#4480,#4480,#3706,.T.);
#5593=EDGE_CURVE('',#4480,#4335,#1034,.T.);
#5594=EDGE_CURVE('',#4481,#4334,#115,.T.);
#5595=EDGE_CURVE('',#4482,#4481,#1035,.T.);
#5596=EDGE_CURVE('',#4483,#4482,#116,.T.);
#5597=EDGE_CURVE('',#4484,#4483,#3707,.T.);
#5598=EDGE_CURVE('',#4485,#4484,#117,.T.);
#5599=EDGE_CURVE('',#4486,#4485,#1036,.T.);
#5600=EDGE_CURVE('',#4336,#4486,#118,.T.);
#5601=EDGE_CURVE('',#4375,#4395,#1037,.T.);
#5602=EDGE_CURVE('',#4315,#4487,#3708,.F.);
#5603=EDGE_CURVE('',#4487,#4376,#1038,.T.);
#5604=EDGE_CURVE('',#4394,#4366,#1039,.T.);
#5605=EDGE_CURVE('',#4355,#4488,#1040,.T.);
#5606=EDGE_CURVE('',#4488,#4324,#3709,.F.);
#5607=EDGE_CURVE('',#4365,#4356,#1041,.T.);
#5608=EDGE_CURVE('',#4489,#4354,#1042,.T.);
#5609=EDGE_CURVE('',#4488,#4489,#1043,.T.);
#5610=EDGE_CURVE('',#4396,#4374,#1044,.T.);
#5611=EDGE_CURVE('',#4490,#4487,#1045,.T.);
#5612=EDGE_CURVE('',#4377,#4490,#1046,.T.);
#5613=EDGE_CURVE('',#4367,#4393,#1047,.T.);
#5614=EDGE_CURVE('',#4373,#4397,#1048,.T.);
#5615=EDGE_CURVE('',#4490,#4491,#3710,.F.);
#5616=EDGE_CURVE('',#4491,#4378,#1049,.T.);
#5617=EDGE_CURVE('',#4392,#4368,#1050,.T.);
#5618=EDGE_CURVE('',#4353,#4492,#1051,.T.);
#5619=EDGE_CURVE('',#4492,#4489,#3711,.F.);
#5620=EDGE_CURVE('',#4466,#4493,#1052,.T.);
#5621=EDGE_CURVE('',#4493,#4494,#3712,.F.);
#5622=EDGE_CURVE('',#4494,#4467,#1053,.T.);
#5623=EDGE_CURVE('',#4448,#4465,#1054,.T.);
#5624=EDGE_CURVE('',#4464,#4449,#1055,.T.);
#5625=EDGE_CURVE('',#4428,#4495,#1056,.T.);
#5626=EDGE_CURVE('',#4495,#4496,#3713,.F.);
#5627=EDGE_CURVE('',#4496,#4429,#1057,.T.);
#5628=EDGE_CURVE('',#4402,#4431,#1058,.T.);
#5629=EDGE_CURVE('',#4430,#4403,#1059,.T.);
#5630=EDGE_CURVE('',#4404,#4447,#1060,.T.);
#5631=EDGE_CURVE('',#4446,#4405,#1061,.T.);
#5632=EDGE_CURVE('',#4497,#4494,#1062,.T.);
#5633=EDGE_CURVE('',#4468,#4497,#1063,.T.);
#5634=EDGE_CURVE('',#4450,#4463,#1064,.T.);
#5635=EDGE_CURVE('',#4498,#4427,#1065,.T.);
#5636=EDGE_CURVE('',#4495,#4498,#1066,.T.);
#5637=EDGE_CURVE('',#4432,#4401,#1067,.T.);
#5638=EDGE_CURVE('',#4406,#4445,#1068,.T.);
#5639=EDGE_CURVE('',#4472,#4499,#1069,.T.);
#5640=EDGE_CURVE('',#4499,#4500,#3714,.F.);
#5641=EDGE_CURVE('',#4500,#4473,#1070,.T.);
#5642=EDGE_CURVE('',#4454,#4475,#1071,.T.);
#5643=EDGE_CURVE('',#4474,#4455,#1072,.T.);
#5644=EDGE_CURVE('',#4438,#4501,#1073,.T.);
#5645=EDGE_CURVE('',#4501,#4502,#3715,.F.);
#5646=EDGE_CURVE('',#4502,#4439,#1074,.T.);
#5647=EDGE_CURVE('',#4412,#4437,#1075,.T.);
#5648=EDGE_CURVE('',#4436,#4413,#1076,.T.);
#5649=EDGE_CURVE('',#4497,#4503,#3716,.F.);
#5650=EDGE_CURVE('',#4503,#4469,#1077,.T.);
#5651=EDGE_CURVE('',#4462,#4451,#1078,.T.);
#5652=EDGE_CURVE('',#4426,#4504,#1079,.T.);
#5653=EDGE_CURVE('',#4504,#4498,#3717,.F.);
#5654=EDGE_CURVE('',#4400,#4433,#1080,.T.);
#5655=EDGE_CURVE('',#4444,#4407,#1081,.T.);
#5656=EDGE_CURVE('',#4505,#4471,#1082,.T.);
#5657=EDGE_CURVE('',#4499,#4505,#1083,.T.);
#5658=EDGE_CURVE('',#4476,#4453,#1084,.T.);
#5659=EDGE_CURVE('',#4506,#4502,#1085,.T.);
#5660=EDGE_CURVE('',#4440,#4506,#1086,.T.);
#5661=EDGE_CURVE('',#4414,#4435,#1087,.T.);
#5662=EDGE_CURVE('',#4507,#4441,#1088,.T.);
#5663=EDGE_CURVE('',#4504,#4507,#1089,.T.);
#5664=EDGE_CURVE('',#4508,#4503,#1090,.T.);
#5665=EDGE_CURVE('',#4470,#4508,#1091,.T.);
#5666=EDGE_CURVE('',#4452,#4477,#1092,.T.);
#5667=EDGE_CURVE('',#4434,#4415,#1093,.T.);
#5668=EDGE_CURVE('',#4508,#4505,#3718,.F.);
#5669=EDGE_CURVE('',#4506,#4507,#3719,.F.);
#5670=EDGE_CURVE('',#4484,#4313,#1094,.T.);
#5671=EDGE_CURVE('',#4385,#4483,#1095,.T.);
#5672=EDGE_CURVE('',#4344,#4384,#1096,.T.);
#5673=EDGE_CURVE('',#4418,#4343,#1097,.T.);
#5674=EDGE_CURVE('',#4509,#4423,#1098,.T.);
#5675=EDGE_CURVE('',#4510,#4509,#1099,.T.);
#5676=EDGE_CURVE('',#4511,#4510,#1100,.T.);
#5677=EDGE_CURVE('',#4339,#4511,#1101,.T.);
#5678=EDGE_CURVE('',#4312,#4485,#1102,.T.);
#5679=EDGE_CURVE('',#4422,#4512,#1103,.T.);
#5680=EDGE_CURVE('',#4512,#4509,#3720,.F.);
#5681=EDGE_CURVE('',#4482,#4386,#1104,.T.);
#5682=EDGE_CURVE('',#4342,#4419,#1105,.T.);
#5683=EDGE_CURVE('',#4383,#4345,#1106,.T.);
#5684=EDGE_CURVE('',#4513,#4421,#1107,.T.);
#5685=EDGE_CURVE('',#4512,#4513,#1108,.T.);
#5686=EDGE_CURVE('',#4486,#4311,#1109,.T.);
#5687=EDGE_CURVE('',#4420,#4341,#1110,.T.);
#5688=EDGE_CURVE('',#4387,#4481,#1111,.T.);
#5689=EDGE_CURVE('',#4325,#4513,#3721,.F.);
#5690=EDGE_CURVE('',#4363,#4358,#1112,.T.);
#5691=EDGE_CURVE('',#4493,#4491,#1113,.T.);
#5692=EDGE_CURVE('',#4492,#4496,#1114,.T.);
#5693=EDGE_CURVE('',#4456,#4411,#1115,.T.);
#5694=EDGE_CURVE('',#4514,#4500,#1116,.T.);
#5695=EDGE_CURVE('',#4515,#4514,#1117,.T.);
#5696=EDGE_CURVE('',#4501,#4515,#1118,.T.);
#5697=EDGE_CURVE('',#4516,#4506,#3722,.F.);
#5698=EDGE_CURVE('',#4507,#4516,#3723,.F.);
#5699=EDGE_CURVE('',#4517,#4508,#3724,.F.);
#5700=EDGE_CURVE('',#4505,#4517,#3725,.F.);
#5701=EDGE_CURVE('',#4518,#4504,#3726,.T.);
#5702=EDGE_CURVE('',#4518,#4519,#3727,.T.);
#5703=EDGE_CURVE('',#4498,#4519,#3728,.T.);
#5704=EDGE_CURVE('',#4516,#4518,#1119,.T.);
#5705=EDGE_CURVE('',#4520,#4521,#3729,.T.);
#5706=EDGE_CURVE('',#4502,#4521,#3730,.T.);
#5707=EDGE_CURVE('',#4520,#4501,#3731,.T.);
#5708=EDGE_CURVE('',#4522,#4497,#3732,.T.);
#5709=EDGE_CURVE('',#4522,#4523,#3733,.T.);
#5710=EDGE_CURVE('',#4503,#4523,#3734,.T.);
#5711=EDGE_CURVE('',#4524,#4525,#3735,.T.);
#5712=EDGE_CURVE('',#4500,#4525,#3736,.T.);
#5713=EDGE_CURVE('',#4524,#4499,#3737,.T.);
#5714=EDGE_CURVE('',#4517,#4524,#1120,.T.);
#5715=EDGE_CURVE('',#4526,#4495,#3738,.F.);
#5716=EDGE_CURVE('',#4496,#4526,#3739,.F.);
#5717=EDGE_CURVE('',#4519,#4526,#1121,.T.);
#5718=EDGE_CURVE('',#4527,#4528,#3740,.F.);
#5719=EDGE_CURVE('',#4515,#4527,#3741,.F.);
#5720=EDGE_CURVE('',#4528,#4515,#3742,.F.);
#5721=EDGE_CURVE('',#4527,#4520,#1122,.T.);
#5722=EDGE_CURVE('',#4529,#4493,#3743,.F.);
#5723=EDGE_CURVE('',#4494,#4529,#3744,.F.);
#5724=EDGE_CURVE('',#4514,#4530,#3745,.F.);
#5725=EDGE_CURVE('',#4531,#4514,#3746,.F.);
#5726=EDGE_CURVE('',#4530,#4531,#3747,.F.);
#5727=EDGE_CURVE('',#4525,#4531,#1123,.T.);
#5728=EDGE_CURVE('',#4532,#4492,#3748,.F.);
#5729=EDGE_CURVE('',#4489,#4532,#3749,.F.);
#5730=EDGE_CURVE('',#4526,#4532,#1124,.T.);
#5731=EDGE_CURVE('',#4533,#4534,#3750,.F.);
#5732=EDGE_CURVE('',#4535,#4533,#3751,.F.);
#5733=EDGE_CURVE('',#4534,#4535,#3752,.F.);
#5734=EDGE_CURVE('',#4533,#4527,#1125,.T.);
#5735=EDGE_CURVE('',#4528,#4535,#1126,.T.);
#5736=EDGE_CURVE('',#4536,#4490,#3753,.F.);
#5737=EDGE_CURVE('',#4491,#4536,#3754,.F.);
#5738=EDGE_CURVE('',#4537,#4538,#3755,.F.);
#5739=EDGE_CURVE('',#4539,#4537,#3756,.F.);
#5740=EDGE_CURVE('',#4538,#4539,#3757,.F.);
#5741=EDGE_CURVE('',#4537,#4530,#1127,.T.);
#5742=EDGE_CURVE('',#4531,#4539,#1128,.T.);
#5743=EDGE_CURVE('',#4540,#4488,#3758,.T.);
#5744=EDGE_CURVE('',#4540,#4541,#3759,.T.);
#5745=EDGE_CURVE('',#4324,#4541,#3760,.T.);
#5746=EDGE_CURVE('',#4532,#4540,#1129,.T.);
#5747=EDGE_CURVE('',#4542,#4543,#3761,.F.);
#5748=EDGE_CURVE('',#4544,#4542,#3762,.F.);
#5749=EDGE_CURVE('',#4543,#4544,#3763,.F.);
#5750=EDGE_CURVE('',#4545,#4315,#3764,.T.);
#5751=EDGE_CURVE('',#4545,#4546,#3765,.T.);
#5752=EDGE_CURVE('',#4487,#4546,#3766,.T.);
#5753=EDGE_CURVE('',#4547,#4548,#3767,.F.);
#5754=EDGE_CURVE('',#4549,#4547,#3768,.F.);
#5755=EDGE_CURVE('',#4548,#4549,#3769,.F.);
#5756=EDGE_CURVE('',#4550,#4325,#3770,.F.);
#5757=EDGE_CURVE('',#4513,#4550,#3771,.F.);
#5758=EDGE_CURVE('',#4541,#4550,#1130,.T.);
#5759=EDGE_CURVE('',#4551,#4552,#3772,.F.);
#5760=EDGE_CURVE('',#4510,#4551,#3773,.F.);
#5761=EDGE_CURVE('',#4552,#4510,#3774,.F.);
#5762=EDGE_CURVE('',#4553,#4337,#3775,.F.);
#5763=EDGE_CURVE('',#4314,#4553,#3776,.F.);
#5764=EDGE_CURVE('',#4554,#4555,#3777,.F.);
#5765=EDGE_CURVE('',#4511,#4554,#3778,.F.);
#5766=EDGE_CURVE('',#4555,#4511,#3779,.F.);
#5767=EDGE_CURVE('',#4556,#4512,#3780,.T.);
#5768=EDGE_CURVE('',#4556,#4557,#3781,.T.);
#5769=EDGE_CURVE('',#4509,#4557,#3782,.T.);
#5770=EDGE_CURVE('',#4550,#4556,#1131,.T.);
#5771=EDGE_CURVE('',#4557,#4552,#1132,.T.);
#5772=EDGE_CURVE('',#4558,#4339,#3783,.T.);
#5773=EDGE_CURVE('',#4558,#4559,#3784,.T.);
#5774=EDGE_CURVE('',#4338,#4559,#3785,.T.);
#5775=EDGE_CURVE('',#4554,#4558,#1133,.T.);
#5776=EDGE_CURVE('',#4559,#4553,#1134,.T.);
#5777=EDGE_CURVE('',#4551,#4555,#1135,.T.);
#5778=EDGE_CURVE('',#4547,#4554,#1136,.T.);
#5779=EDGE_CURVE('',#4555,#4549,#1137,.T.);
#5780=EDGE_CURVE('',#4553,#4545,#1138,.T.);
#5781=EDGE_CURVE('',#4346,#4382,#1139,.T.);
#5782=EDGE_CURVE('',#4542,#4551,#1140,.T.);
#5783=EDGE_CURVE('',#4552,#4544,#1141,.T.);
#5784=EDGE_CURVE('',#4543,#4548,#1142,.T.);
#5785=EDGE_CURVE('',#4549,#4542,#1143,.T.);
#5786=EDGE_CURVE('',#4548,#4538,#1144,.T.);
#5787=EDGE_CURVE('',#4539,#4547,#1145,.T.);
#5788=EDGE_CURVE('',#4546,#4536,#1146,.T.);
#5789=EDGE_CURVE('',#4534,#4543,#1147,.T.);
#5790=EDGE_CURVE('',#4544,#4533,#1148,.T.);
#5791=EDGE_CURVE('',#4538,#4534,#1149,.T.);
#5792=EDGE_CURVE('',#4535,#4537,#1150,.T.);
#5793=EDGE_CURVE('',#4536,#4529,#1151,.T.);
#5794=EDGE_CURVE('',#4357,#4364,#1152,.T.);
#5795=EDGE_CURVE('',#4530,#4528,#1153,.T.);
#5796=EDGE_CURVE('',#4529,#4522,#1154,.T.);
#5797=EDGE_CURVE('',#4410,#4457,#1155,.T.);
#5798=EDGE_CURVE('',#4523,#4517,#1156,.T.);
#5799=EDGE_CURVE('',#4521,#4516,#1157,.T.);
#5800=EDGE_CURVE('',#4408,#4459,#1158,.T.);
#5801=EDGE_CURVE('',#4458,#4409,#1159,.T.);
#7425=ORIENTED_EDGE('',*,*,#5383,.F.);
#7426=ORIENTED_EDGE('',*,*,#5384,.T.);
#7427=ORIENTED_EDGE('',*,*,#5385,.F.);
#7428=ORIENTED_EDGE('',*,*,#5384,.F.);
#7429=ORIENTED_EDGE('',*,*,#5386,.F.);
#7430=ORIENTED_EDGE('',*,*,#5387,.T.);
#7431=ORIENTED_EDGE('',*,*,#5388,.F.);
#7432=ORIENTED_EDGE('',*,*,#5389,.F.);
#7433=ORIENTED_EDGE('',*,*,#5390,.F.);
#7434=ORIENTED_EDGE('',*,*,#5391,.F.);
#7435=ORIENTED_EDGE('',*,*,#5392,.F.);
#7436=ORIENTED_EDGE('',*,*,#5393,.F.);
#7437=ORIENTED_EDGE('',*,*,#5394,.F.);
#7438=ORIENTED_EDGE('',*,*,#5395,.F.);
#7439=ORIENTED_EDGE('',*,*,#5396,.F.);
#7440=ORIENTED_EDGE('',*,*,#5387,.F.);
#7441=ORIENTED_EDGE('',*,*,#5392,.T.);
#7442=ORIENTED_EDGE('',*,*,#5397,.F.);
#7443=ORIENTED_EDGE('',*,*,#5398,.F.);
#7444=ORIENTED_EDGE('',*,*,#5399,.F.);
#7445=ORIENTED_EDGE('',*,*,#5400,.T.);
#7446=ORIENTED_EDGE('',*,*,#5401,.F.);
#7447=ORIENTED_EDGE('',*,*,#5402,.T.);
#7448=ORIENTED_EDGE('',*,*,#5403,.F.);
#7449=ORIENTED_EDGE('',*,*,#5404,.T.);
#7450=ORIENTED_EDGE('',*,*,#5405,.F.);
#7451=ORIENTED_EDGE('',*,*,#5406,.T.);
#7452=ORIENTED_EDGE('',*,*,#5407,.F.);
#7453=ORIENTED_EDGE('',*,*,#5408,.F.);
#7454=ORIENTED_EDGE('',*,*,#5409,.F.);
#7455=ORIENTED_EDGE('',*,*,#5410,.T.);
#7456=ORIENTED_EDGE('',*,*,#5411,.F.);
#7457=ORIENTED_EDGE('',*,*,#5412,.T.);
#7458=ORIENTED_EDGE('',*,*,#5413,.T.);
#7459=ORIENTED_EDGE('',*,*,#5414,.F.);
#7460=ORIENTED_EDGE('',*,*,#5415,.T.);
#7461=ORIENTED_EDGE('',*,*,#5416,.T.);
#7462=ORIENTED_EDGE('',*,*,#5417,.F.);
#7463=ORIENTED_EDGE('',*,*,#5418,.T.);
#7464=ORIENTED_EDGE('',*,*,#5419,.T.);
#7465=ORIENTED_EDGE('',*,*,#5420,.F.);
#7466=ORIENTED_EDGE('',*,*,#5391,.T.);
#7467=ORIENTED_EDGE('',*,*,#5421,.T.);
#7468=ORIENTED_EDGE('',*,*,#5422,.T.);
#7469=ORIENTED_EDGE('',*,*,#5397,.T.);
#7470=ORIENTED_EDGE('',*,*,#5390,.T.);
#7471=ORIENTED_EDGE('',*,*,#5423,.F.);
#7472=ORIENTED_EDGE('',*,*,#5424,.F.);
#7473=ORIENTED_EDGE('',*,*,#5421,.F.);
#7474=ORIENTED_EDGE('',*,*,#5389,.T.);
#7475=ORIENTED_EDGE('',*,*,#5425,.T.);
#7476=ORIENTED_EDGE('',*,*,#5426,.T.);
#7477=ORIENTED_EDGE('',*,*,#5423,.T.);
#7478=ORIENTED_EDGE('',*,*,#5427,.F.);
#7479=ORIENTED_EDGE('',*,*,#5428,.T.);
#7480=ORIENTED_EDGE('',*,*,#5412,.F.);
#7481=ORIENTED_EDGE('',*,*,#5429,.F.);
#7482=ORIENTED_EDGE('',*,*,#5430,.F.);
#7483=ORIENTED_EDGE('',*,*,#5431,.F.);
#7484=ORIENTED_EDGE('',*,*,#5432,.F.);
#7485=ORIENTED_EDGE('',*,*,#5433,.F.);
#7486=ORIENTED_EDGE('',*,*,#5434,.F.);
#7487=ORIENTED_EDGE('',*,*,#5435,.F.);
#7488=ORIENTED_EDGE('',*,*,#5413,.F.);
#7489=ORIENTED_EDGE('',*,*,#5428,.F.);
#7490=ORIENTED_EDGE('',*,*,#5436,.F.);
#7491=ORIENTED_EDGE('',*,*,#5437,.T.);
#7492=ORIENTED_EDGE('',*,*,#5438,.F.);
#7493=ORIENTED_EDGE('',*,*,#5437,.F.);
#7494=ORIENTED_EDGE('',*,*,#5439,.F.);
#7495=ORIENTED_EDGE('',*,*,#5440,.T.);
#7496=ORIENTED_EDGE('',*,*,#5441,.F.);
#7497=ORIENTED_EDGE('',*,*,#5440,.F.);
#7498=ORIENTED_EDGE('',*,*,#5442,.F.);
#7499=ORIENTED_EDGE('',*,*,#5443,.T.);
#7500=ORIENTED_EDGE('',*,*,#5444,.F.);
#7501=ORIENTED_EDGE('',*,*,#5445,.F.);
#7502=ORIENTED_EDGE('',*,*,#5446,.F.);
#7503=ORIENTED_EDGE('',*,*,#5447,.F.);
#7504=ORIENTED_EDGE('',*,*,#5406,.F.);
#7505=ORIENTED_EDGE('',*,*,#5448,.F.);
#7506=ORIENTED_EDGE('',*,*,#5449,.F.);
#7507=ORIENTED_EDGE('',*,*,#5450,.F.);
#7508=ORIENTED_EDGE('',*,*,#5451,.F.);
#7509=ORIENTED_EDGE('',*,*,#5443,.F.);
#7510=ORIENTED_EDGE('',*,*,#5452,.F.);
#7511=ORIENTED_EDGE('',*,*,#5453,.T.);
#7512=ORIENTED_EDGE('',*,*,#5454,.F.);
#7513=ORIENTED_EDGE('',*,*,#5453,.F.);
#7514=ORIENTED_EDGE('',*,*,#5455,.F.);
#7515=ORIENTED_EDGE('',*,*,#5456,.T.);
#7516=ORIENTED_EDGE('',*,*,#5457,.F.);
#7517=ORIENTED_EDGE('',*,*,#5458,.F.);
#7518=ORIENTED_EDGE('',*,*,#5459,.F.);
#7519=ORIENTED_EDGE('',*,*,#5460,.F.);
#7520=ORIENTED_EDGE('',*,*,#5404,.F.);
#7521=ORIENTED_EDGE('',*,*,#5461,.F.);
#7522=ORIENTED_EDGE('',*,*,#5462,.F.);
#7523=ORIENTED_EDGE('',*,*,#5463,.F.);
#7524=ORIENTED_EDGE('',*,*,#5464,.F.);
#7525=ORIENTED_EDGE('',*,*,#5456,.F.);
#7526=ORIENTED_EDGE('',*,*,#5465,.F.);
#7527=ORIENTED_EDGE('',*,*,#5466,.T.);
#7528=ORIENTED_EDGE('',*,*,#5467,.F.);
#7529=ORIENTED_EDGE('',*,*,#5466,.F.);
#7530=ORIENTED_EDGE('',*,*,#5468,.F.);
#7531=ORIENTED_EDGE('',*,*,#5469,.T.);
#7532=ORIENTED_EDGE('',*,*,#5470,.F.);
#7533=ORIENTED_EDGE('',*,*,#5471,.F.);
#7534=ORIENTED_EDGE('',*,*,#5472,.F.);
#7535=ORIENTED_EDGE('',*,*,#5473,.F.);
#7536=ORIENTED_EDGE('',*,*,#5400,.F.);
#7537=ORIENTED_EDGE('',*,*,#5474,.F.);
#7538=ORIENTED_EDGE('',*,*,#5475,.F.);
#7539=ORIENTED_EDGE('',*,*,#5476,.F.);
#7540=ORIENTED_EDGE('',*,*,#5477,.F.);
#7541=ORIENTED_EDGE('',*,*,#5469,.F.);
#7542=ORIENTED_EDGE('',*,*,#5478,.F.);
#7543=ORIENTED_EDGE('',*,*,#5479,.T.);
#7544=ORIENTED_EDGE('',*,*,#5480,.F.);
#7545=ORIENTED_EDGE('',*,*,#5479,.F.);
#7546=ORIENTED_EDGE('',*,*,#5481,.F.);
#7547=ORIENTED_EDGE('',*,*,#5482,.T.);
#7548=ORIENTED_EDGE('',*,*,#5415,.F.);
#7549=ORIENTED_EDGE('',*,*,#5483,.F.);
#7550=ORIENTED_EDGE('',*,*,#5484,.F.);
#7551=ORIENTED_EDGE('',*,*,#5485,.F.);
#7552=ORIENTED_EDGE('',*,*,#5486,.F.);
#7553=ORIENTED_EDGE('',*,*,#5487,.F.);
#7554=ORIENTED_EDGE('',*,*,#5488,.F.);
#7555=ORIENTED_EDGE('',*,*,#5489,.F.);
#7556=ORIENTED_EDGE('',*,*,#5416,.F.);
#7557=ORIENTED_EDGE('',*,*,#5482,.F.);
#7558=ORIENTED_EDGE('',*,*,#5490,.F.);
#7559=ORIENTED_EDGE('',*,*,#5491,.T.);
#7560=ORIENTED_EDGE('',*,*,#5492,.F.);
#7561=ORIENTED_EDGE('',*,*,#5491,.F.);
#7562=ORIENTED_EDGE('',*,*,#5493,.F.);
#7563=ORIENTED_EDGE('',*,*,#5494,.T.);
#7564=ORIENTED_EDGE('',*,*,#5495,.F.);
#7565=ORIENTED_EDGE('',*,*,#5496,.F.);
#7566=ORIENTED_EDGE('',*,*,#5497,.F.);
#7567=ORIENTED_EDGE('',*,*,#5498,.F.);
#7568=ORIENTED_EDGE('',*,*,#5402,.F.);
#7569=ORIENTED_EDGE('',*,*,#5499,.F.);
#7570=ORIENTED_EDGE('',*,*,#5500,.F.);
#7571=ORIENTED_EDGE('',*,*,#5501,.F.);
#7572=ORIENTED_EDGE('',*,*,#5502,.F.);
#7573=ORIENTED_EDGE('',*,*,#5494,.F.);
#7574=ORIENTED_EDGE('',*,*,#5503,.F.);
#7575=ORIENTED_EDGE('',*,*,#5504,.T.);
#7576=ORIENTED_EDGE('',*,*,#5505,.F.);
#7577=ORIENTED_EDGE('',*,*,#5506,.F.);
#7578=ORIENTED_EDGE('',*,*,#5507,.F.);
#7579=ORIENTED_EDGE('',*,*,#5508,.F.);
#7580=ORIENTED_EDGE('',*,*,#5509,.F.);
#7581=ORIENTED_EDGE('',*,*,#5510,.F.);
#7582=ORIENTED_EDGE('',*,*,#5511,.F.);
#7583=ORIENTED_EDGE('',*,*,#5512,.F.);
#7584=ORIENTED_EDGE('',*,*,#5513,.F.);
#7585=ORIENTED_EDGE('',*,*,#5514,.F.);
#7586=ORIENTED_EDGE('',*,*,#5515,.F.);
#7587=ORIENTED_EDGE('',*,*,#5516,.F.);
#7588=ORIENTED_EDGE('',*,*,#5517,.F.);
#7589=ORIENTED_EDGE('',*,*,#5518,.F.);
#7590=ORIENTED_EDGE('',*,*,#5519,.F.);
#7591=ORIENTED_EDGE('',*,*,#5520,.F.);
#7592=ORIENTED_EDGE('',*,*,#5521,.F.);
#7593=ORIENTED_EDGE('',*,*,#5504,.F.);
#7594=ORIENTED_EDGE('',*,*,#5522,.F.);
#7595=ORIENTED_EDGE('',*,*,#5523,.T.);
#7596=ORIENTED_EDGE('',*,*,#5524,.F.);
#7597=ORIENTED_EDGE('',*,*,#5525,.F.);
#7598=ORIENTED_EDGE('',*,*,#5526,.F.);
#7599=ORIENTED_EDGE('',*,*,#5527,.F.);
#7600=ORIENTED_EDGE('',*,*,#5410,.F.);
#7601=ORIENTED_EDGE('',*,*,#5528,.F.);
#7602=ORIENTED_EDGE('',*,*,#5529,.F.);
#7603=ORIENTED_EDGE('',*,*,#5530,.F.);
#7604=ORIENTED_EDGE('',*,*,#5531,.F.);
#7605=ORIENTED_EDGE('',*,*,#5523,.F.);
#7606=ORIENTED_EDGE('',*,*,#5532,.F.);
#7607=ORIENTED_EDGE('',*,*,#5533,.T.);
#7608=ORIENTED_EDGE('',*,*,#5534,.F.);
#7609=ORIENTED_EDGE('',*,*,#5535,.F.);
#7610=ORIENTED_EDGE('',*,*,#5536,.F.);
#7611=ORIENTED_EDGE('',*,*,#5537,.F.);
#7612=ORIENTED_EDGE('',*,*,#5538,.F.);
#7613=ORIENTED_EDGE('',*,*,#5539,.F.);
#7614=ORIENTED_EDGE('',*,*,#5540,.F.);
#7615=ORIENTED_EDGE('',*,*,#5541,.F.);
#7616=ORIENTED_EDGE('',*,*,#5542,.F.);
#7617=ORIENTED_EDGE('',*,*,#5543,.F.);
#7618=ORIENTED_EDGE('',*,*,#5544,.F.);
#7619=ORIENTED_EDGE('',*,*,#5545,.F.);
#7620=ORIENTED_EDGE('',*,*,#5546,.F.);
#7621=ORIENTED_EDGE('',*,*,#5547,.F.);
#7622=ORIENTED_EDGE('',*,*,#5548,.F.);
#7623=ORIENTED_EDGE('',*,*,#5549,.F.);
#7624=ORIENTED_EDGE('',*,*,#5550,.F.);
#7625=ORIENTED_EDGE('',*,*,#5533,.F.);
#7626=ORIENTED_EDGE('',*,*,#5551,.F.);
#7627=ORIENTED_EDGE('',*,*,#5552,.T.);
#7628=ORIENTED_EDGE('',*,*,#5553,.F.);
#7629=ORIENTED_EDGE('',*,*,#5554,.F.);
#7630=ORIENTED_EDGE('',*,*,#5555,.F.);
#7631=ORIENTED_EDGE('',*,*,#5556,.F.);
#7632=ORIENTED_EDGE('',*,*,#5557,.F.);
#7633=ORIENTED_EDGE('',*,*,#5558,.F.);
#7634=ORIENTED_EDGE('',*,*,#5559,.F.);
#7635=ORIENTED_EDGE('',*,*,#5560,.F.);
#7636=ORIENTED_EDGE('',*,*,#5561,.F.);
#7637=ORIENTED_EDGE('',*,*,#5562,.F.);
#7638=ORIENTED_EDGE('',*,*,#5563,.F.);
#7639=ORIENTED_EDGE('',*,*,#5564,.F.);
#7640=ORIENTED_EDGE('',*,*,#5565,.F.);
#7641=ORIENTED_EDGE('',*,*,#5566,.F.);
#7642=ORIENTED_EDGE('',*,*,#5567,.F.);
#7643=ORIENTED_EDGE('',*,*,#5568,.F.);
#7644=ORIENTED_EDGE('',*,*,#5569,.F.);
#7645=ORIENTED_EDGE('',*,*,#5552,.F.);
#7646=ORIENTED_EDGE('',*,*,#5570,.F.);
#7647=ORIENTED_EDGE('',*,*,#5571,.T.);
#7648=ORIENTED_EDGE('',*,*,#5572,.F.);
#7649=ORIENTED_EDGE('',*,*,#5573,.F.);
#7650=ORIENTED_EDGE('',*,*,#5574,.F.);
#7651=ORIENTED_EDGE('',*,*,#5575,.F.);
#7652=ORIENTED_EDGE('',*,*,#5576,.F.);
#7653=ORIENTED_EDGE('',*,*,#5577,.F.);
#7654=ORIENTED_EDGE('',*,*,#5578,.F.);
#7655=ORIENTED_EDGE('',*,*,#5579,.F.);
#7656=ORIENTED_EDGE('',*,*,#5580,.F.);
#7657=ORIENTED_EDGE('',*,*,#5581,.F.);
#7658=ORIENTED_EDGE('',*,*,#5582,.F.);
#7659=ORIENTED_EDGE('',*,*,#5583,.F.);
#7660=ORIENTED_EDGE('',*,*,#5584,.F.);
#7661=ORIENTED_EDGE('',*,*,#5585,.F.);
#7662=ORIENTED_EDGE('',*,*,#5586,.F.);
#7663=ORIENTED_EDGE('',*,*,#5587,.F.);
#7664=ORIENTED_EDGE('',*,*,#5588,.F.);
#7665=ORIENTED_EDGE('',*,*,#5571,.F.);
#7666=ORIENTED_EDGE('',*,*,#5589,.F.);
#7667=ORIENTED_EDGE('',*,*,#5590,.T.);
#7668=ORIENTED_EDGE('',*,*,#5591,.F.);
#7669=ORIENTED_EDGE('',*,*,#5590,.F.);
#7670=ORIENTED_EDGE('',*,*,#5592,.F.);
#7671=ORIENTED_EDGE('',*,*,#5593,.T.);
#7672=ORIENTED_EDGE('',*,*,#5418,.F.);
#7673=ORIENTED_EDGE('',*,*,#5594,.F.);
#7674=ORIENTED_EDGE('',*,*,#5595,.F.);
#7675=ORIENTED_EDGE('',*,*,#5596,.F.);
#7676=ORIENTED_EDGE('',*,*,#5597,.F.);
#7677=ORIENTED_EDGE('',*,*,#5598,.F.);
#7678=ORIENTED_EDGE('',*,*,#5599,.F.);
#7679=ORIENTED_EDGE('',*,*,#5600,.F.);
#7680=ORIENTED_EDGE('',*,*,#5419,.F.);
#7681=ORIENTED_EDGE('',*,*,#5593,.F.);
#7682=ORIENTED_EDGE('',*,*,#5473,.T.);
#7683=ORIENTED_EDGE('',*,*,#5601,.T.);
#7684=ORIENTED_EDGE('',*,*,#5499,.T.);
#7685=ORIENTED_EDGE('',*,*,#5401,.T.);
#7686=ORIENTED_EDGE('',*,*,#5474,.T.);
#7687=ORIENTED_EDGE('',*,*,#5399,.T.);
#7688=ORIENTED_EDGE('',*,*,#5602,.T.);
#7689=ORIENTED_EDGE('',*,*,#5603,.T.);
#7690=ORIENTED_EDGE('',*,*,#5461,.T.);
#7691=ORIENTED_EDGE('',*,*,#5403,.T.);
#7692=ORIENTED_EDGE('',*,*,#5498,.T.);
#7693=ORIENTED_EDGE('',*,*,#5604,.T.);
#7694=ORIENTED_EDGE('',*,*,#5447,.T.);
#7695=ORIENTED_EDGE('',*,*,#5605,.T.);
#7696=ORIENTED_EDGE('',*,*,#5606,.T.);
#7697=ORIENTED_EDGE('',*,*,#5407,.T.);
#7698=ORIENTED_EDGE('',*,*,#5448,.T.);
#7699=ORIENTED_EDGE('',*,*,#5405,.T.);
#7700=ORIENTED_EDGE('',*,*,#5460,.T.);
#7701=ORIENTED_EDGE('',*,*,#5607,.T.);
#7702=ORIENTED_EDGE('',*,*,#5446,.T.);
#7703=ORIENTED_EDGE('',*,*,#5608,.F.);
#7704=ORIENTED_EDGE('',*,*,#5609,.F.);
#7705=ORIENTED_EDGE('',*,*,#5605,.F.);
#7706=ORIENTED_EDGE('',*,*,#5472,.T.);
#7707=ORIENTED_EDGE('',*,*,#5610,.F.);
#7708=ORIENTED_EDGE('',*,*,#5500,.T.);
#7709=ORIENTED_EDGE('',*,*,#5601,.F.);
#7710=ORIENTED_EDGE('',*,*,#5475,.T.);
#7711=ORIENTED_EDGE('',*,*,#5603,.F.);
#7712=ORIENTED_EDGE('',*,*,#5611,.F.);
#7713=ORIENTED_EDGE('',*,*,#5612,.F.);
#7714=ORIENTED_EDGE('',*,*,#5462,.T.);
#7715=ORIENTED_EDGE('',*,*,#5604,.F.);
#7716=ORIENTED_EDGE('',*,*,#5497,.T.);
#7717=ORIENTED_EDGE('',*,*,#5613,.F.);
#7718=ORIENTED_EDGE('',*,*,#5471,.T.);
#7719=ORIENTED_EDGE('',*,*,#5614,.T.);
#7720=ORIENTED_EDGE('',*,*,#5501,.T.);
#7721=ORIENTED_EDGE('',*,*,#5610,.T.);
#7722=ORIENTED_EDGE('',*,*,#5476,.T.);
#7723=ORIENTED_EDGE('',*,*,#5612,.T.);
#7724=ORIENTED_EDGE('',*,*,#5615,.T.);
#7725=ORIENTED_EDGE('',*,*,#5616,.T.);
#7726=ORIENTED_EDGE('',*,*,#5463,.T.);
#7727=ORIENTED_EDGE('',*,*,#5613,.T.);
#7728=ORIENTED_EDGE('',*,*,#5496,.T.);
#7729=ORIENTED_EDGE('',*,*,#5617,.T.);
#7730=ORIENTED_EDGE('',*,*,#5445,.T.);
#7731=ORIENTED_EDGE('',*,*,#5618,.T.);
#7732=ORIENTED_EDGE('',*,*,#5619,.T.);
#7733=ORIENTED_EDGE('',*,*,#5608,.T.);
#7734=ORIENTED_EDGE('',*,*,#5577,.T.);
#7735=ORIENTED_EDGE('',*,*,#5620,.T.);
#7736=ORIENTED_EDGE('',*,*,#5621,.T.);
#7737=ORIENTED_EDGE('',*,*,#5622,.T.);
#7738=ORIENTED_EDGE('',*,*,#5558,.T.);
#7739=ORIENTED_EDGE('',*,*,#5623,.T.);
#7740=ORIENTED_EDGE('',*,*,#5575,.T.);
#7741=ORIENTED_EDGE('',*,*,#5624,.T.);
#7742=ORIENTED_EDGE('',*,*,#5537,.T.);
#7743=ORIENTED_EDGE('',*,*,#5625,.T.);
#7744=ORIENTED_EDGE('',*,*,#5626,.T.);
#7745=ORIENTED_EDGE('',*,*,#5627,.T.);
#7746=ORIENTED_EDGE('',*,*,#5508,.T.);
#7747=ORIENTED_EDGE('',*,*,#5628,.T.);
#7748=ORIENTED_EDGE('',*,*,#5539,.T.);
#7749=ORIENTED_EDGE('',*,*,#5629,.T.);
#7750=ORIENTED_EDGE('',*,*,#5510,.T.);
#7751=ORIENTED_EDGE('',*,*,#5630,.T.);
#7752=ORIENTED_EDGE('',*,*,#5556,.T.);
#7753=ORIENTED_EDGE('',*,*,#5631,.T.);
#7754=ORIENTED_EDGE('',*,*,#5578,.T.);
#7755=ORIENTED_EDGE('',*,*,#5622,.F.);
#7756=ORIENTED_EDGE('',*,*,#5632,.F.);
#7757=ORIENTED_EDGE('',*,*,#5633,.F.);
#7758=ORIENTED_EDGE('',*,*,#5559,.T.);
#7759=ORIENTED_EDGE('',*,*,#5624,.F.);
#7760=ORIENTED_EDGE('',*,*,#5574,.T.);
#7761=ORIENTED_EDGE('',*,*,#5634,.F.);
#7762=ORIENTED_EDGE('',*,*,#5536,.T.);
#7763=ORIENTED_EDGE('',*,*,#5635,.F.);
#7764=ORIENTED_EDGE('',*,*,#5636,.F.);
#7765=ORIENTED_EDGE('',*,*,#5625,.F.);
#7766=ORIENTED_EDGE('',*,*,#5507,.T.);
#7767=ORIENTED_EDGE('',*,*,#5637,.F.);
#7768=ORIENTED_EDGE('',*,*,#5540,.T.);
#7769=ORIENTED_EDGE('',*,*,#5628,.F.);
#7770=ORIENTED_EDGE('',*,*,#5511,.T.);
#7771=ORIENTED_EDGE('',*,*,#5631,.F.);
#7772=ORIENTED_EDGE('',*,*,#5555,.T.);
#7773=ORIENTED_EDGE('',*,*,#5638,.F.);
#7774=ORIENTED_EDGE('',*,*,#5583,.T.);
#7775=ORIENTED_EDGE('',*,*,#5639,.T.);
#7776=ORIENTED_EDGE('',*,*,#5640,.T.);
#7777=ORIENTED_EDGE('',*,*,#5641,.T.);
#7778=ORIENTED_EDGE('',*,*,#5564,.T.);
#7779=ORIENTED_EDGE('',*,*,#5642,.T.);
#7780=ORIENTED_EDGE('',*,*,#5585,.T.);
#7781=ORIENTED_EDGE('',*,*,#5643,.T.);
#7782=ORIENTED_EDGE('',*,*,#5547,.T.);
#7783=ORIENTED_EDGE('',*,*,#5644,.T.);
#7784=ORIENTED_EDGE('',*,*,#5645,.T.);
#7785=ORIENTED_EDGE('',*,*,#5646,.T.);
#7786=ORIENTED_EDGE('',*,*,#5518,.T.);
#7787=ORIENTED_EDGE('',*,*,#5647,.T.);
#7788=ORIENTED_EDGE('',*,*,#5545,.T.);
#7789=ORIENTED_EDGE('',*,*,#5648,.T.);
#7790=ORIENTED_EDGE('',*,*,#5579,.T.);
#7791=ORIENTED_EDGE('',*,*,#5633,.T.);
#7792=ORIENTED_EDGE('',*,*,#5649,.T.);
#7793=ORIENTED_EDGE('',*,*,#5650,.T.);
#7794=ORIENTED_EDGE('',*,*,#5560,.T.);
#7795=ORIENTED_EDGE('',*,*,#5634,.T.);
#7796=ORIENTED_EDGE('',*,*,#5573,.T.);
#7797=ORIENTED_EDGE('',*,*,#5651,.T.);
#7798=ORIENTED_EDGE('',*,*,#5535,.T.);
#7799=ORIENTED_EDGE('',*,*,#5652,.T.);
#7800=ORIENTED_EDGE('',*,*,#5653,.T.);
#7801=ORIENTED_EDGE('',*,*,#5635,.T.);
#7802=ORIENTED_EDGE('',*,*,#5506,.T.);
#7803=ORIENTED_EDGE('',*,*,#5654,.T.);
#7804=ORIENTED_EDGE('',*,*,#5541,.T.);
#7805=ORIENTED_EDGE('',*,*,#5637,.T.);
#7806=ORIENTED_EDGE('',*,*,#5512,.T.);
#7807=ORIENTED_EDGE('',*,*,#5638,.T.);
#7808=ORIENTED_EDGE('',*,*,#5554,.T.);
#7809=ORIENTED_EDGE('',*,*,#5655,.T.);
#7810=ORIENTED_EDGE('',*,*,#5582,.T.);
#7811=ORIENTED_EDGE('',*,*,#5656,.F.);
#7812=ORIENTED_EDGE('',*,*,#5657,.F.);
#7813=ORIENTED_EDGE('',*,*,#5639,.F.);
#7814=ORIENTED_EDGE('',*,*,#5563,.T.);
#7815=ORIENTED_EDGE('',*,*,#5658,.F.);
#7816=ORIENTED_EDGE('',*,*,#5586,.T.);
#7817=ORIENTED_EDGE('',*,*,#5642,.F.);
#7818=ORIENTED_EDGE('',*,*,#5548,.T.);
#7819=ORIENTED_EDGE('',*,*,#5646,.F.);
#7820=ORIENTED_EDGE('',*,*,#5659,.F.);
#7821=ORIENTED_EDGE('',*,*,#5660,.F.);
#7822=ORIENTED_EDGE('',*,*,#5519,.T.);
#7823=ORIENTED_EDGE('',*,*,#5648,.F.);
#7824=ORIENTED_EDGE('',*,*,#5544,.T.);
#7825=ORIENTED_EDGE('',*,*,#5661,.F.);
#7826=ORIENTED_EDGE('',*,*,#5534,.T.);
#7827=ORIENTED_EDGE('',*,*,#5550,.T.);
#7828=ORIENTED_EDGE('',*,*,#5662,.F.);
#7829=ORIENTED_EDGE('',*,*,#5663,.F.);
#7830=ORIENTED_EDGE('',*,*,#5652,.F.);
#7831=ORIENTED_EDGE('',*,*,#5580,.T.);
#7832=ORIENTED_EDGE('',*,*,#5650,.F.);
#7833=ORIENTED_EDGE('',*,*,#5664,.F.);
#7834=ORIENTED_EDGE('',*,*,#5665,.F.);
#7835=ORIENTED_EDGE('',*,*,#5561,.T.);
#7836=ORIENTED_EDGE('',*,*,#5651,.F.);
#7837=ORIENTED_EDGE('',*,*,#5572,.T.);
#7838=ORIENTED_EDGE('',*,*,#5588,.T.);
#7839=ORIENTED_EDGE('',*,*,#5666,.F.);
#7840=ORIENTED_EDGE('',*,*,#5505,.T.);
#7841=ORIENTED_EDGE('',*,*,#5521,.T.);
#7842=ORIENTED_EDGE('',*,*,#5667,.F.);
#7843=ORIENTED_EDGE('',*,*,#5542,.T.);
#7844=ORIENTED_EDGE('',*,*,#5654,.F.);
#7845=ORIENTED_EDGE('',*,*,#5581,.T.);
#7846=ORIENTED_EDGE('',*,*,#5665,.T.);
#7847=ORIENTED_EDGE('',*,*,#5668,.T.);
#7848=ORIENTED_EDGE('',*,*,#5656,.T.);
#7849=ORIENTED_EDGE('',*,*,#5562,.T.);
#7850=ORIENTED_EDGE('',*,*,#5666,.T.);
#7851=ORIENTED_EDGE('',*,*,#5587,.T.);
#7852=ORIENTED_EDGE('',*,*,#5658,.T.);
#7853=ORIENTED_EDGE('',*,*,#5549,.T.);
#7854=ORIENTED_EDGE('',*,*,#5660,.T.);
#7855=ORIENTED_EDGE('',*,*,#5669,.T.);
#7856=ORIENTED_EDGE('',*,*,#5662,.T.);
#7857=ORIENTED_EDGE('',*,*,#5520,.T.);
#7858=ORIENTED_EDGE('',*,*,#5661,.T.);
#7859=ORIENTED_EDGE('',*,*,#5543,.T.);
#7860=ORIENTED_EDGE('',*,*,#5667,.T.);
#7861=ORIENTED_EDGE('',*,*,#5388,.T.);
#7862=ORIENTED_EDGE('',*,*,#5396,.T.);
#7863=ORIENTED_EDGE('',*,*,#5670,.F.);
#7864=ORIENTED_EDGE('',*,*,#5597,.T.);
#7865=ORIENTED_EDGE('',*,*,#5671,.F.);
#7866=ORIENTED_EDGE('',*,*,#5486,.T.);
#7867=ORIENTED_EDGE('',*,*,#5672,.F.);
#7868=ORIENTED_EDGE('',*,*,#5432,.T.);
#7869=ORIENTED_EDGE('',*,*,#5673,.F.);
#7870=ORIENTED_EDGE('',*,*,#5524,.T.);
#7871=ORIENTED_EDGE('',*,*,#5531,.T.);
#7872=ORIENTED_EDGE('',*,*,#5674,.F.);
#7873=ORIENTED_EDGE('',*,*,#5675,.F.);
#7874=ORIENTED_EDGE('',*,*,#5676,.F.);
#7875=ORIENTED_EDGE('',*,*,#5677,.F.);
#7876=ORIENTED_EDGE('',*,*,#5425,.F.);
#7877=ORIENTED_EDGE('',*,*,#5395,.T.);
#7878=ORIENTED_EDGE('',*,*,#5678,.T.);
#7879=ORIENTED_EDGE('',*,*,#5598,.T.);
#7880=ORIENTED_EDGE('',*,*,#5670,.T.);
#7881=ORIENTED_EDGE('',*,*,#5530,.T.);
#7882=ORIENTED_EDGE('',*,*,#5679,.T.);
#7883=ORIENTED_EDGE('',*,*,#5680,.T.);
#7884=ORIENTED_EDGE('',*,*,#5674,.T.);
#7885=ORIENTED_EDGE('',*,*,#5487,.T.);
#7886=ORIENTED_EDGE('',*,*,#5671,.T.);
#7887=ORIENTED_EDGE('',*,*,#5596,.T.);
#7888=ORIENTED_EDGE('',*,*,#5681,.T.);
#7889=ORIENTED_EDGE('',*,*,#5431,.T.);
#7890=ORIENTED_EDGE('',*,*,#5682,.T.);
#7891=ORIENTED_EDGE('',*,*,#5525,.T.);
#7892=ORIENTED_EDGE('',*,*,#5673,.T.);
#7893=ORIENTED_EDGE('',*,*,#5433,.T.);
#7894=ORIENTED_EDGE('',*,*,#5672,.T.);
#7895=ORIENTED_EDGE('',*,*,#5485,.T.);
#7896=ORIENTED_EDGE('',*,*,#5683,.T.);
#7897=ORIENTED_EDGE('',*,*,#5529,.T.);
#7898=ORIENTED_EDGE('',*,*,#5684,.F.);
#7899=ORIENTED_EDGE('',*,*,#5685,.F.);
#7900=ORIENTED_EDGE('',*,*,#5679,.F.);
#7901=ORIENTED_EDGE('',*,*,#5394,.T.);
#7902=ORIENTED_EDGE('',*,*,#5686,.F.);
#7903=ORIENTED_EDGE('',*,*,#5599,.T.);
#7904=ORIENTED_EDGE('',*,*,#5678,.F.);
#7905=ORIENTED_EDGE('',*,*,#5430,.T.);
#7906=ORIENTED_EDGE('',*,*,#5687,.F.);
#7907=ORIENTED_EDGE('',*,*,#5526,.T.);
#7908=ORIENTED_EDGE('',*,*,#5682,.F.);
#7909=ORIENTED_EDGE('',*,*,#5488,.T.);
#7910=ORIENTED_EDGE('',*,*,#5681,.F.);
#7911=ORIENTED_EDGE('',*,*,#5595,.T.);
#7912=ORIENTED_EDGE('',*,*,#5688,.F.);
#7913=ORIENTED_EDGE('',*,*,#5393,.T.);
#7914=ORIENTED_EDGE('',*,*,#5420,.T.);
#7915=ORIENTED_EDGE('',*,*,#5600,.T.);
#7916=ORIENTED_EDGE('',*,*,#5686,.T.);
#7917=ORIENTED_EDGE('',*,*,#5528,.T.);
#7918=ORIENTED_EDGE('',*,*,#5409,.T.);
#7919=ORIENTED_EDGE('',*,*,#5689,.T.);
#7920=ORIENTED_EDGE('',*,*,#5684,.T.);
#7921=ORIENTED_EDGE('',*,*,#5489,.T.);
#7922=ORIENTED_EDGE('',*,*,#5688,.T.);
#7923=ORIENTED_EDGE('',*,*,#5594,.T.);
#7924=ORIENTED_EDGE('',*,*,#5417,.T.);
#7925=ORIENTED_EDGE('',*,*,#5429,.T.);
#7926=ORIENTED_EDGE('',*,*,#5411,.T.);
#7927=ORIENTED_EDGE('',*,*,#5527,.T.);
#7928=ORIENTED_EDGE('',*,*,#5687,.T.);
#7929=ORIENTED_EDGE('',*,*,#5444,.T.);
#7930=ORIENTED_EDGE('',*,*,#5451,.T.);
#7931=ORIENTED_EDGE('',*,*,#5690,.F.);
#7932=ORIENTED_EDGE('',*,*,#5457,.T.);
#7933=ORIENTED_EDGE('',*,*,#5464,.T.);
#7934=ORIENTED_EDGE('',*,*,#5617,.F.);
#7935=ORIENTED_EDGE('',*,*,#5495,.T.);
#7936=ORIENTED_EDGE('',*,*,#5502,.T.);
#7937=ORIENTED_EDGE('',*,*,#5614,.F.);
#7938=ORIENTED_EDGE('',*,*,#5470,.T.);
#7939=ORIENTED_EDGE('',*,*,#5477,.T.);
#7940=ORIENTED_EDGE('',*,*,#5616,.F.);
#7941=ORIENTED_EDGE('',*,*,#5691,.F.);
#7942=ORIENTED_EDGE('',*,*,#5620,.F.);
#7943=ORIENTED_EDGE('',*,*,#5576,.T.);
#7944=ORIENTED_EDGE('',*,*,#5623,.F.);
#7945=ORIENTED_EDGE('',*,*,#5557,.T.);
#7946=ORIENTED_EDGE('',*,*,#5630,.F.);
#7947=ORIENTED_EDGE('',*,*,#5509,.T.);
#7948=ORIENTED_EDGE('',*,*,#5629,.F.);
#7949=ORIENTED_EDGE('',*,*,#5538,.T.);
#7950=ORIENTED_EDGE('',*,*,#5627,.F.);
#7951=ORIENTED_EDGE('',*,*,#5692,.F.);
#7952=ORIENTED_EDGE('',*,*,#5618,.F.);
#7953=ORIENTED_EDGE('',*,*,#5467,.T.);
#7954=ORIENTED_EDGE('',*,*,#5441,.T.);
#7955=ORIENTED_EDGE('',*,*,#5438,.T.);
#7956=ORIENTED_EDGE('',*,*,#5517,.T.);
#7957=ORIENTED_EDGE('',*,*,#5693,.F.);
#7958=ORIENTED_EDGE('',*,*,#5565,.T.);
#7959=ORIENTED_EDGE('',*,*,#5643,.F.);
#7960=ORIENTED_EDGE('',*,*,#5584,.T.);
#7961=ORIENTED_EDGE('',*,*,#5641,.F.);
#7962=ORIENTED_EDGE('',*,*,#5694,.F.);
#7963=ORIENTED_EDGE('',*,*,#5695,.F.);
#7964=ORIENTED_EDGE('',*,*,#5696,.F.);
#7965=ORIENTED_EDGE('',*,*,#5644,.F.);
#7966=ORIENTED_EDGE('',*,*,#5546,.T.);
#7967=ORIENTED_EDGE('',*,*,#5647,.F.);
#7968=ORIENTED_EDGE('',*,*,#5385,.T.);
#7969=ORIENTED_EDGE('',*,*,#5591,.T.);
#7970=ORIENTED_EDGE('',*,*,#5492,.T.);
#7971=ORIENTED_EDGE('',*,*,#5480,.T.);
#7972=ORIENTED_EDGE('',*,*,#5454,.T.);
#7973=ORIENTED_EDGE('',*,*,#5669,.F.);
#7974=ORIENTED_EDGE('',*,*,#5697,.F.);
#7975=ORIENTED_EDGE('',*,*,#5698,.F.);
#7976=ORIENTED_EDGE('',*,*,#5699,.F.);
#7977=ORIENTED_EDGE('',*,*,#5700,.F.);
#7978=ORIENTED_EDGE('',*,*,#5668,.F.);
#7979=ORIENTED_EDGE('',*,*,#5653,.F.);
#7980=ORIENTED_EDGE('',*,*,#5701,.F.);
#7981=ORIENTED_EDGE('',*,*,#5702,.T.);
#7982=ORIENTED_EDGE('',*,*,#5703,.F.);
#7983=ORIENTED_EDGE('',*,*,#5701,.T.);
#7984=ORIENTED_EDGE('',*,*,#5663,.T.);
#7985=ORIENTED_EDGE('',*,*,#5698,.T.);
#7986=ORIENTED_EDGE('',*,*,#5704,.T.);
#7987=ORIENTED_EDGE('',*,*,#5705,.T.);
#7988=ORIENTED_EDGE('',*,*,#5706,.F.);
#7989=ORIENTED_EDGE('',*,*,#5645,.F.);
#7990=ORIENTED_EDGE('',*,*,#5707,.F.);
#7991=ORIENTED_EDGE('',*,*,#5649,.F.);
#7992=ORIENTED_EDGE('',*,*,#5708,.F.);
#7993=ORIENTED_EDGE('',*,*,#5709,.T.);
#7994=ORIENTED_EDGE('',*,*,#5710,.F.);
#7995=ORIENTED_EDGE('',*,*,#5711,.T.);
#7996=ORIENTED_EDGE('',*,*,#5712,.F.);
#7997=ORIENTED_EDGE('',*,*,#5640,.F.);
#7998=ORIENTED_EDGE('',*,*,#5713,.F.);
#7999=ORIENTED_EDGE('',*,*,#5713,.T.);
#8000=ORIENTED_EDGE('',*,*,#5657,.T.);
#8001=ORIENTED_EDGE('',*,*,#5700,.T.);
#8002=ORIENTED_EDGE('',*,*,#5714,.T.);
#8003=ORIENTED_EDGE('',*,*,#5626,.F.);
#8004=ORIENTED_EDGE('',*,*,#5715,.F.);
#8005=ORIENTED_EDGE('',*,*,#5716,.F.);
#8006=ORIENTED_EDGE('',*,*,#5715,.T.);
#8007=ORIENTED_EDGE('',*,*,#5636,.T.);
#8008=ORIENTED_EDGE('',*,*,#5703,.T.);
#8009=ORIENTED_EDGE('',*,*,#5717,.T.);
#8010=ORIENTED_EDGE('',*,*,#5718,.F.);
#8011=ORIENTED_EDGE('',*,*,#5719,.F.);
#8012=ORIENTED_EDGE('',*,*,#5720,.F.);
#8013=ORIENTED_EDGE('',*,*,#5719,.T.);
#8014=ORIENTED_EDGE('',*,*,#5721,.T.);
#8015=ORIENTED_EDGE('',*,*,#5707,.T.);
#8016=ORIENTED_EDGE('',*,*,#5696,.T.);
#8017=ORIENTED_EDGE('',*,*,#5621,.F.);
#8018=ORIENTED_EDGE('',*,*,#5722,.F.);
#8019=ORIENTED_EDGE('',*,*,#5723,.F.);
#8020=ORIENTED_EDGE('',*,*,#5724,.F.);
#8021=ORIENTED_EDGE('',*,*,#5725,.F.);
#8022=ORIENTED_EDGE('',*,*,#5726,.F.);
#8023=ORIENTED_EDGE('',*,*,#5712,.T.);
#8024=ORIENTED_EDGE('',*,*,#5727,.T.);
#8025=ORIENTED_EDGE('',*,*,#5725,.T.);
#8026=ORIENTED_EDGE('',*,*,#5694,.T.);
#8027=ORIENTED_EDGE('',*,*,#5619,.F.);
#8028=ORIENTED_EDGE('',*,*,#5728,.F.);
#8029=ORIENTED_EDGE('',*,*,#5729,.F.);
#8030=ORIENTED_EDGE('',*,*,#5728,.T.);
#8031=ORIENTED_EDGE('',*,*,#5692,.T.);
#8032=ORIENTED_EDGE('',*,*,#5716,.T.);
#8033=ORIENTED_EDGE('',*,*,#5730,.T.);
#8034=ORIENTED_EDGE('',*,*,#5731,.F.);
#8035=ORIENTED_EDGE('',*,*,#5732,.F.);
#8036=ORIENTED_EDGE('',*,*,#5733,.F.);
#8037=ORIENTED_EDGE('',*,*,#5732,.T.);
#8038=ORIENTED_EDGE('',*,*,#5734,.T.);
#8039=ORIENTED_EDGE('',*,*,#5718,.T.);
#8040=ORIENTED_EDGE('',*,*,#5735,.T.);
#8041=ORIENTED_EDGE('',*,*,#5615,.F.);
#8042=ORIENTED_EDGE('',*,*,#5736,.F.);
#8043=ORIENTED_EDGE('',*,*,#5737,.F.);
#8044=ORIENTED_EDGE('',*,*,#5738,.F.);
#8045=ORIENTED_EDGE('',*,*,#5739,.F.);
#8046=ORIENTED_EDGE('',*,*,#5740,.F.);
#8047=ORIENTED_EDGE('',*,*,#5739,.T.);
#8048=ORIENTED_EDGE('',*,*,#5741,.T.);
#8049=ORIENTED_EDGE('',*,*,#5726,.T.);
#8050=ORIENTED_EDGE('',*,*,#5742,.T.);
#8051=ORIENTED_EDGE('',*,*,#5606,.F.);
#8052=ORIENTED_EDGE('',*,*,#5743,.F.);
#8053=ORIENTED_EDGE('',*,*,#5744,.T.);
#8054=ORIENTED_EDGE('',*,*,#5745,.F.);
#8055=ORIENTED_EDGE('',*,*,#5743,.T.);
#8056=ORIENTED_EDGE('',*,*,#5609,.T.);
#8057=ORIENTED_EDGE('',*,*,#5729,.T.);
#8058=ORIENTED_EDGE('',*,*,#5746,.T.);
#8059=ORIENTED_EDGE('',*,*,#5747,.F.);
#8060=ORIENTED_EDGE('',*,*,#5748,.F.);
#8061=ORIENTED_EDGE('',*,*,#5749,.F.);
#8062=ORIENTED_EDGE('',*,*,#5602,.F.);
#8063=ORIENTED_EDGE('',*,*,#5750,.F.);
#8064=ORIENTED_EDGE('',*,*,#5751,.T.);
#8065=ORIENTED_EDGE('',*,*,#5752,.F.);
#8066=ORIENTED_EDGE('',*,*,#5753,.F.);
#8067=ORIENTED_EDGE('',*,*,#5754,.F.);
#8068=ORIENTED_EDGE('',*,*,#5755,.F.);
#8069=ORIENTED_EDGE('',*,*,#5689,.F.);
#8070=ORIENTED_EDGE('',*,*,#5756,.F.);
#8071=ORIENTED_EDGE('',*,*,#5757,.F.);
#8072=ORIENTED_EDGE('',*,*,#5756,.T.);
#8073=ORIENTED_EDGE('',*,*,#5408,.T.);
#8074=ORIENTED_EDGE('',*,*,#5745,.T.);
#8075=ORIENTED_EDGE('',*,*,#5758,.T.);
#8076=ORIENTED_EDGE('',*,*,#5759,.F.);
#8077=ORIENTED_EDGE('',*,*,#5760,.F.);
#8078=ORIENTED_EDGE('',*,*,#5761,.F.);
#8079=ORIENTED_EDGE('',*,*,#5422,.F.);
#8080=ORIENTED_EDGE('',*,*,#5762,.F.);
#8081=ORIENTED_EDGE('',*,*,#5763,.F.);
#8082=ORIENTED_EDGE('',*,*,#5764,.F.);
#8083=ORIENTED_EDGE('',*,*,#5765,.F.);
#8084=ORIENTED_EDGE('',*,*,#5766,.F.);
#8085=ORIENTED_EDGE('',*,*,#5680,.F.);
#8086=ORIENTED_EDGE('',*,*,#5767,.F.);
#8087=ORIENTED_EDGE('',*,*,#5768,.T.);
#8088=ORIENTED_EDGE('',*,*,#5769,.F.);
#8089=ORIENTED_EDGE('',*,*,#5767,.T.);
#8090=ORIENTED_EDGE('',*,*,#5685,.T.);
#8091=ORIENTED_EDGE('',*,*,#5757,.T.);
#8092=ORIENTED_EDGE('',*,*,#5770,.T.);
#8093=ORIENTED_EDGE('',*,*,#5769,.T.);
#8094=ORIENTED_EDGE('',*,*,#5771,.T.);
#8095=ORIENTED_EDGE('',*,*,#5761,.T.);
#8096=ORIENTED_EDGE('',*,*,#5675,.T.);
#8097=ORIENTED_EDGE('',*,*,#5426,.F.);
#8098=ORIENTED_EDGE('',*,*,#5772,.F.);
#8099=ORIENTED_EDGE('',*,*,#5773,.T.);
#8100=ORIENTED_EDGE('',*,*,#5774,.F.);
#8101=ORIENTED_EDGE('',*,*,#5765,.T.);
#8102=ORIENTED_EDGE('',*,*,#5775,.T.);
#8103=ORIENTED_EDGE('',*,*,#5772,.T.);
#8104=ORIENTED_EDGE('',*,*,#5677,.T.);
#8105=ORIENTED_EDGE('',*,*,#5762,.T.);
#8106=ORIENTED_EDGE('',*,*,#5424,.T.);
#8107=ORIENTED_EDGE('',*,*,#5774,.T.);
#8108=ORIENTED_EDGE('',*,*,#5776,.T.);
#8109=ORIENTED_EDGE('',*,*,#5760,.T.);
#8110=ORIENTED_EDGE('',*,*,#5777,.T.);
#8111=ORIENTED_EDGE('',*,*,#5766,.T.);
#8112=ORIENTED_EDGE('',*,*,#5676,.T.);
#8113=ORIENTED_EDGE('',*,*,#5754,.T.);
#8114=ORIENTED_EDGE('',*,*,#5778,.T.);
#8115=ORIENTED_EDGE('',*,*,#5764,.T.);
#8116=ORIENTED_EDGE('',*,*,#5779,.T.);
#8117=ORIENTED_EDGE('',*,*,#5750,.T.);
#8118=ORIENTED_EDGE('',*,*,#5398,.T.);
#8119=ORIENTED_EDGE('',*,*,#5763,.T.);
#8120=ORIENTED_EDGE('',*,*,#5780,.T.);
#8121=ORIENTED_EDGE('',*,*,#5435,.T.);
#8122=ORIENTED_EDGE('',*,*,#5781,.T.);
#8123=ORIENTED_EDGE('',*,*,#5483,.T.);
#8124=ORIENTED_EDGE('',*,*,#5414,.T.);
#8125=ORIENTED_EDGE('',*,*,#5748,.T.);
#8126=ORIENTED_EDGE('',*,*,#5782,.T.);
#8127=ORIENTED_EDGE('',*,*,#5759,.T.);
#8128=ORIENTED_EDGE('',*,*,#5783,.T.);
#8129=ORIENTED_EDGE('',*,*,#5747,.T.);
#8130=ORIENTED_EDGE('',*,*,#5784,.T.);
#8131=ORIENTED_EDGE('',*,*,#5755,.T.);
#8132=ORIENTED_EDGE('',*,*,#5785,.T.);
#8133=ORIENTED_EDGE('',*,*,#5753,.T.);
#8134=ORIENTED_EDGE('',*,*,#5786,.T.);
#8135=ORIENTED_EDGE('',*,*,#5740,.T.);
#8136=ORIENTED_EDGE('',*,*,#5787,.T.);
#8137=ORIENTED_EDGE('',*,*,#5736,.T.);
#8138=ORIENTED_EDGE('',*,*,#5611,.T.);
#8139=ORIENTED_EDGE('',*,*,#5752,.T.);
#8140=ORIENTED_EDGE('',*,*,#5788,.T.);
#8141=ORIENTED_EDGE('',*,*,#5731,.T.);
#8142=ORIENTED_EDGE('',*,*,#5789,.T.);
#8143=ORIENTED_EDGE('',*,*,#5749,.T.);
#8144=ORIENTED_EDGE('',*,*,#5790,.T.);
#8145=ORIENTED_EDGE('',*,*,#5738,.T.);
#8146=ORIENTED_EDGE('',*,*,#5791,.T.);
#8147=ORIENTED_EDGE('',*,*,#5733,.T.);
#8148=ORIENTED_EDGE('',*,*,#5792,.T.);
#8149=ORIENTED_EDGE('',*,*,#5722,.T.);
#8150=ORIENTED_EDGE('',*,*,#5691,.T.);
#8151=ORIENTED_EDGE('',*,*,#5737,.T.);
#8152=ORIENTED_EDGE('',*,*,#5793,.T.);
#8153=ORIENTED_EDGE('',*,*,#5450,.T.);
#8154=ORIENTED_EDGE('',*,*,#5794,.T.);
#8155=ORIENTED_EDGE('',*,*,#5458,.T.);
#8156=ORIENTED_EDGE('',*,*,#5690,.T.);
#8157=ORIENTED_EDGE('',*,*,#5724,.T.);
#8158=ORIENTED_EDGE('',*,*,#5795,.T.);
#8159=ORIENTED_EDGE('',*,*,#5720,.T.);
#8160=ORIENTED_EDGE('',*,*,#5695,.T.);
#8161=ORIENTED_EDGE('',*,*,#5708,.T.);
#8162=ORIENTED_EDGE('',*,*,#5632,.T.);
#8163=ORIENTED_EDGE('',*,*,#5723,.T.);
#8164=ORIENTED_EDGE('',*,*,#5796,.T.);
#8165=ORIENTED_EDGE('',*,*,#5516,.T.);
#8166=ORIENTED_EDGE('',*,*,#5797,.T.);
#8167=ORIENTED_EDGE('',*,*,#5566,.T.);
#8168=ORIENTED_EDGE('',*,*,#5693,.T.);
#8169=ORIENTED_EDGE('',*,*,#5699,.T.);
#8170=ORIENTED_EDGE('',*,*,#5664,.T.);
#8171=ORIENTED_EDGE('',*,*,#5710,.T.);
#8172=ORIENTED_EDGE('',*,*,#5798,.T.);
#8173=ORIENTED_EDGE('',*,*,#5697,.T.);
#8174=ORIENTED_EDGE('',*,*,#5659,.T.);
#8175=ORIENTED_EDGE('',*,*,#5706,.T.);
#8176=ORIENTED_EDGE('',*,*,#5799,.T.);
#8177=ORIENTED_EDGE('',*,*,#5514,.T.);
#8178=ORIENTED_EDGE('',*,*,#5800,.T.);
#8179=ORIENTED_EDGE('',*,*,#5568,.T.);
#8180=ORIENTED_EDGE('',*,*,#5801,.T.);
#8181=ORIENTED_EDGE('',*,*,#5711,.F.);
#8182=ORIENTED_EDGE('',*,*,#5714,.F.);
#8183=ORIENTED_EDGE('',*,*,#5798,.F.);
#8184=ORIENTED_EDGE('',*,*,#5709,.F.);
#8185=ORIENTED_EDGE('',*,*,#5796,.F.);
#8186=ORIENTED_EDGE('',*,*,#5793,.F.);
#8187=ORIENTED_EDGE('',*,*,#5788,.F.);
#8188=ORIENTED_EDGE('',*,*,#5751,.F.);
#8189=ORIENTED_EDGE('',*,*,#5780,.F.);
#8190=ORIENTED_EDGE('',*,*,#5776,.F.);
#8191=ORIENTED_EDGE('',*,*,#5773,.F.);
#8192=ORIENTED_EDGE('',*,*,#5775,.F.);
#8193=ORIENTED_EDGE('',*,*,#5778,.F.);
#8194=ORIENTED_EDGE('',*,*,#5787,.F.);
#8195=ORIENTED_EDGE('',*,*,#5742,.F.);
#8196=ORIENTED_EDGE('',*,*,#5727,.F.);
#8197=ORIENTED_EDGE('',*,*,#5515,.T.);
#8198=ORIENTED_EDGE('',*,*,#5801,.F.);
#8199=ORIENTED_EDGE('',*,*,#5567,.T.);
#8200=ORIENTED_EDGE('',*,*,#5797,.F.);
#8201=ORIENTED_EDGE('',*,*,#5741,.F.);
#8202=ORIENTED_EDGE('',*,*,#5792,.F.);
#8203=ORIENTED_EDGE('',*,*,#5735,.F.);
#8204=ORIENTED_EDGE('',*,*,#5795,.F.);
#8205=ORIENTED_EDGE('',*,*,#5434,.T.);
#8206=ORIENTED_EDGE('',*,*,#5683,.F.);
#8207=ORIENTED_EDGE('',*,*,#5484,.T.);
#8208=ORIENTED_EDGE('',*,*,#5781,.F.);
#8209=ORIENTED_EDGE('',*,*,#5777,.F.);
#8210=ORIENTED_EDGE('',*,*,#5782,.F.);
#8211=ORIENTED_EDGE('',*,*,#5785,.F.);
#8212=ORIENTED_EDGE('',*,*,#5779,.F.);
#8213=ORIENTED_EDGE('',*,*,#5784,.F.);
#8214=ORIENTED_EDGE('',*,*,#5789,.F.);
#8215=ORIENTED_EDGE('',*,*,#5791,.F.);
#8216=ORIENTED_EDGE('',*,*,#5786,.F.);
#8217=ORIENTED_EDGE('',*,*,#5427,.T.);
#8218=ORIENTED_EDGE('',*,*,#5436,.T.);
#8219=ORIENTED_EDGE('',*,*,#5439,.T.);
#8220=ORIENTED_EDGE('',*,*,#5442,.T.);
#8221=ORIENTED_EDGE('',*,*,#5452,.T.);
#8222=ORIENTED_EDGE('',*,*,#5455,.T.);
#8223=ORIENTED_EDGE('',*,*,#5465,.T.);
#8224=ORIENTED_EDGE('',*,*,#5468,.T.);
#8225=ORIENTED_EDGE('',*,*,#5478,.T.);
#8226=ORIENTED_EDGE('',*,*,#5481,.T.);
#8227=ORIENTED_EDGE('',*,*,#5490,.T.);
#8228=ORIENTED_EDGE('',*,*,#5493,.T.);
#8229=ORIENTED_EDGE('',*,*,#5503,.T.);
#8230=ORIENTED_EDGE('',*,*,#5522,.T.);
#8231=ORIENTED_EDGE('',*,*,#5532,.T.);
#8232=ORIENTED_EDGE('',*,*,#5551,.T.);
#8233=ORIENTED_EDGE('',*,*,#5570,.T.);
#8234=ORIENTED_EDGE('',*,*,#5589,.T.);
#8235=ORIENTED_EDGE('',*,*,#5592,.T.);
#8236=ORIENTED_EDGE('',*,*,#5386,.T.);
#8237=ORIENTED_EDGE('',*,*,#5383,.T.);
#8238=ORIENTED_EDGE('',*,*,#5449,.T.);
#8239=ORIENTED_EDGE('',*,*,#5607,.F.);
#8240=ORIENTED_EDGE('',*,*,#5459,.T.);
#8241=ORIENTED_EDGE('',*,*,#5794,.F.);
#8242=ORIENTED_EDGE('',*,*,#5513,.T.);
#8243=ORIENTED_EDGE('',*,*,#5655,.F.);
#8244=ORIENTED_EDGE('',*,*,#5553,.T.);
#8245=ORIENTED_EDGE('',*,*,#5569,.T.);
#8246=ORIENTED_EDGE('',*,*,#5800,.F.);
#8247=ORIENTED_EDGE('',*,*,#5705,.F.);
#8248=ORIENTED_EDGE('',*,*,#5721,.F.);
#8249=ORIENTED_EDGE('',*,*,#5734,.F.);
#8250=ORIENTED_EDGE('',*,*,#5790,.F.);
#8251=ORIENTED_EDGE('',*,*,#5783,.F.);
#8252=ORIENTED_EDGE('',*,*,#5771,.F.);
#8253=ORIENTED_EDGE('',*,*,#5768,.F.);
#8254=ORIENTED_EDGE('',*,*,#5770,.F.);
#8255=ORIENTED_EDGE('',*,*,#5758,.F.);
#8256=ORIENTED_EDGE('',*,*,#5744,.F.);
#8257=ORIENTED_EDGE('',*,*,#5746,.F.);
#8258=ORIENTED_EDGE('',*,*,#5730,.F.);
#8259=ORIENTED_EDGE('',*,*,#5717,.F.);
#8260=ORIENTED_EDGE('',*,*,#5702,.F.);
#8261=ORIENTED_EDGE('',*,*,#5704,.F.);
#8262=ORIENTED_EDGE('',*,*,#5799,.F.);
#8946=PLANE('',#10408);
#8947=PLANE('',#10422);
#8948=PLANE('',#10518);
#8949=PLANE('',#10519);
#8950=PLANE('',#10520);
#8951=PLANE('',#10521);
#8952=PLANE('',#10535);
#8953=PLANE('',#10536);
#8954=PLANE('',#10537);
#8955=PLANE('',#10538);
#8956=PLANE('',#10539);
#8957=PLANE('',#10553);
#8958=PLANE('',#10554);
#8959=PLANE('',#10555);
#8960=PLANE('',#10556);
#8961=PLANE('',#10557);
#8962=PLANE('',#10558);
#8963=PLANE('',#10559);
#8964=PLANE('',#10560);
#8965=PLANE('',#10567);
#8966=PLANE('',#10574);
#8967=PLANE('',#10575);
#8968=PLANE('',#10576);
#8969=PLANE('',#10577);
#8970=PLANE('',#10583);
#8971=PLANE('',#10584);
#8972=PLANE('',#10705);
#8973=PLANE('',#10706);
#8974=PLANE('',#10707);
#8975=PLANE('',#10708);
#8976=PLANE('',#10709);
#8977=PLANE('',#10710);
#8978=PLANE('',#10711);
#8979=PLANE('',#10712);
#8980=PLANE('',#10713);
#9330=ADVANCED_FACE('',(#2343),#478,.F.);
#9331=ADVANCED_FACE('',(#2344),#479,.F.);
#9332=ADVANCED_FACE('',(#2345),#8946,.T.);
#9333=ADVANCED_FACE('',(#2346),#480,.T.);
#9334=ADVANCED_FACE('',(#2347),#8947,.T.);
#9335=ADVANCED_FACE('',(#2348),#481,.F.);
#9336=ADVANCED_FACE('',(#2349),#482,.F.);
#9337=ADVANCED_FACE('',(#2350),#483,.F.);
#9338=ADVANCED_FACE('',(#2351),#484,.F.);
#9339=ADVANCED_FACE('',(#2352),#485,.F.);
#9340=ADVANCED_FACE('',(#2353),#486,.F.);
#9341=ADVANCED_FACE('',(#2354),#487,.F.);
#9342=ADVANCED_FACE('',(#2355),#488,.F.);
#9343=ADVANCED_FACE('',(#2356),#489,.F.);
#9344=ADVANCED_FACE('',(#2357),#490,.F.);
#9345=ADVANCED_FACE('',(#2358),#491,.F.);
#9346=ADVANCED_FACE('',(#2359),#492,.F.);
#9347=ADVANCED_FACE('',(#2360),#493,.F.);
#9348=ADVANCED_FACE('',(#2361),#494,.F.);
#9349=ADVANCED_FACE('',(#2362),#495,.F.);
#9350=ADVANCED_FACE('',(#2363),#496,.F.);
#9351=ADVANCED_FACE('',(#2364),#497,.F.);
#9352=ADVANCED_FACE('',(#2365),#498,.F.);
#9353=ADVANCED_FACE('',(#2366),#499,.F.);
#9354=ADVANCED_FACE('',(#2367),#500,.F.);
#9355=ADVANCED_FACE('',(#2368),#501,.F.);
#9356=ADVANCED_FACE('',(#2369),#502,.F.);
#9357=ADVANCED_FACE('',(#2370),#503,.F.);
#9358=ADVANCED_FACE('',(#2371),#504,.F.);
#9359=ADVANCED_FACE('',(#2372),#505,.F.);
#9360=ADVANCED_FACE('',(#2373),#8948,.T.);
#9361=ADVANCED_FACE('',(#2374),#8949,.T.);
#9362=ADVANCED_FACE('',(#2375),#8950,.T.);
#9363=ADVANCED_FACE('',(#2376),#8951,.T.);
#9364=ADVANCED_FACE('',(#2377),#506,.T.);
#9365=ADVANCED_FACE('',(#2378),#507,.T.);
#9366=ADVANCED_FACE('',(#2379),#508,.T.);
#9367=ADVANCED_FACE('',(#2380),#509,.T.);
#9368=ADVANCED_FACE('',(#2381),#510,.T.);
#9369=ADVANCED_FACE('',(#2382),#511,.T.);
#9370=ADVANCED_FACE('',(#2383),#512,.T.);
#9371=ADVANCED_FACE('',(#2384),#513,.T.);
#9372=ADVANCED_FACE('',(#2385),#514,.T.);
#9373=ADVANCED_FACE('',(#2386),#8952,.T.);
#9374=ADVANCED_FACE('',(#2387),#8953,.T.);
#9375=ADVANCED_FACE('',(#2388),#8954,.T.);
#9376=ADVANCED_FACE('',(#2389),#8955,.T.);
#9377=ADVANCED_FACE('',(#2390),#8956,.T.);
#9378=ADVANCED_FACE('',(#2391),#515,.F.);
#9379=ADVANCED_FACE('',(#2392),#516,.F.);
#9380=ADVANCED_FACE('',(#2393),#517,.F.);
#9381=ADVANCED_FACE('',(#2394),#518,.F.);
#9382=ADVANCED_FACE('',(#2395),#519,.F.);
#9383=ADVANCED_FACE('',(#2396),#520,.F.);
#9384=ADVANCED_FACE('',(#2397),#521,.F.);
#9385=ADVANCED_FACE('',(#2398),#522,.F.);
#9386=ADVANCED_FACE('',(#2399),#523,.F.);
#9387=ADVANCED_FACE('',(#2400),#8957,.T.);
#9388=ADVANCED_FACE('',(#2401),#8958,.T.);
#9389=ADVANCED_FACE('',(#2402),#8959,.T.);
#9390=ADVANCED_FACE('',(#2403),#8960,.T.);
#9391=ADVANCED_FACE('',(#2404),#8961,.T.);
#9392=ADVANCED_FACE('',(#2405),#8962,.T.);
#9393=ADVANCED_FACE('',(#2406),#8963,.T.);
#9394=ADVANCED_FACE('',(#2407),#8964,.T.);
#9395=ADVANCED_FACE('',(#2408),#524,.T.);
#9396=ADVANCED_FACE('',(#2409),#525,.T.);
#9397=ADVANCED_FACE('',(#2410),#526,.T.);
#9398=ADVANCED_FACE('',(#2411),#527,.T.);
#9399=ADVANCED_FACE('',(#2412),#8965,.F.);
#9400=ADVANCED_FACE('',(#2413),#528,.F.);
#9401=ADVANCED_FACE('',(#2414),#529,.F.);
#9402=ADVANCED_FACE('',(#2415),#530,.F.);
#9403=ADVANCED_FACE('',(#2416),#531,.F.);
#9404=ADVANCED_FACE('',(#2417),#532,.F.);
#9405=ADVANCED_FACE('',(#2418),#8966,.T.);
#9406=ADVANCED_FACE('',(#2419),#8967,.T.);
#9407=ADVANCED_FACE('',(#2420),#8968,.T.);
#9408=ADVANCED_FACE('',(#2421),#8969,.T.);
#9409=ADVANCED_FACE('',(#2422),#533,.T.);
#9410=ADVANCED_FACE('',(#2423),#534,.T.);
#9411=ADVANCED_FACE('',(#2424),#535,.T.);
#9412=ADVANCED_FACE('',(#2425),#536,.T.);
#9413=ADVANCED_FACE('',(#2426,#1991,#1992,#1993),#8970,.T.);
#9414=ADVANCED_FACE('',(#2427,#1994,#1995,#1996,#1997,#1998),#8971,.F.);
#9415=ADVANCED_FACE('',(#2428),#171,.T.);
#9416=ADVANCED_FACE('',(#2429),#172,.T.);
#9417=ADVANCED_FACE('',(#2430),#241,.T.);
#9418=ADVANCED_FACE('',(#2431),#537,.T.);
#9419=ADVANCED_FACE('',(#2432),#242,.T.);
#9420=ADVANCED_FACE('',(#2433),#243,.T.);
#9421=ADVANCED_FACE('',(#2434),#244,.T.);
#9422=ADVANCED_FACE('',(#2435),#538,.T.);
#9423=ADVANCED_FACE('',(#2436),#173,.T.);
#9424=ADVANCED_FACE('',(#2437),#539,.T.);
#9425=ADVANCED_FACE('',(#2438),#174,.T.);
#9426=ADVANCED_FACE('',(#2439),#540,.T.);
#9427=ADVANCED_FACE('',(#2440),#175,.T.);
#9428=ADVANCED_FACE('',(#2441),#176,.T.);
#9429=ADVANCED_FACE('',(#2442),#541,.T.);
#9430=ADVANCED_FACE('',(#2443),#177,.T.);
#9431=ADVANCED_FACE('',(#2444),#542,.T.);
#9432=ADVANCED_FACE('',(#2445),#178,.T.);
#9433=ADVANCED_FACE('',(#2446),#543,.T.);
#9434=ADVANCED_FACE('',(#2447),#179,.T.);
#9435=ADVANCED_FACE('',(#2448),#180,.T.);
#9436=ADVANCED_FACE('',(#2449),#544,.T.);
#9437=ADVANCED_FACE('',(#2450),#245,.T.);
#9438=ADVANCED_FACE('',(#2451),#545,.T.);
#9439=ADVANCED_FACE('',(#2452),#181,.T.);
#9440=ADVANCED_FACE('',(#2453),#246,.T.);
#9441=ADVANCED_FACE('',(#2454),#182,.T.);
#9442=ADVANCED_FACE('',(#2455),#183,.T.);
#9443=ADVANCED_FACE('',(#2456),#546,.T.);
#9444=ADVANCED_FACE('',(#2457),#184,.T.);
#9445=ADVANCED_FACE('',(#2458),#185,.T.);
#9446=ADVANCED_FACE('',(#2459),#186,.T.);
#9447=ADVANCED_FACE('',(#2460),#247,.T.);
#9448=ADVANCED_FACE('',(#2461),#547,.T.);
#9449=ADVANCED_FACE('',(#2462),#548,.T.);
#9450=ADVANCED_FACE('',(#2463),#248,.T.);
#9451=ADVANCED_FACE('',(#2464),#549,.T.);
#9452=ADVANCED_FACE('',(#2465),#550,.T.);
#9453=ADVANCED_FACE('',(#2466),#551,.T.);
#9454=ADVANCED_FACE('',(#2467),#552,.T.);
#9455=ADVANCED_FACE('',(#2468),#553,.T.);
#9456=ADVANCED_FACE('',(#2469),#554,.T.);
#9457=ADVANCED_FACE('',(#2470),#555,.T.);
#9458=ADVANCED_FACE('',(#2471),#556,.T.);
#9459=ADVANCED_FACE('',(#2472),#557,.T.);
#9460=ADVANCED_FACE('',(#2473),#558,.T.);
#9461=ADVANCED_FACE('',(#2474),#559,.T.);
#9462=ADVANCED_FACE('',(#2475),#560,.T.);
#9463=ADVANCED_FACE('',(#2476),#561,.T.);
#9464=ADVANCED_FACE('',(#2477),#562,.T.);
#9465=ADVANCED_FACE('',(#2478),#563,.T.);
#9466=ADVANCED_FACE('',(#2479),#564,.T.);
#9467=ADVANCED_FACE('',(#2480),#565,.F.);
#9468=ADVANCED_FACE('',(#2481),#566,.T.);
#9469=ADVANCED_FACE('',(#2482),#567,.T.);
#9470=ADVANCED_FACE('',(#2483),#568,.T.);
#9471=ADVANCED_FACE('',(#2484),#8972,.T.);
#9472=ADVANCED_FACE('',(#2485),#8973,.T.);
#9473=ADVANCED_FACE('',(#2486),#8974,.T.);
#9474=ADVANCED_FACE('',(#2487),#8975,.T.);
#9475=ADVANCED_FACE('',(#2488),#8976,.T.);
#9476=ADVANCED_FACE('',(#2489,#1999,#2000,#2001,#2002,#2003,#2004,#2005,
#2006,#2007,#2008,#2009,#2010,#2011,#2012,#2013,#2014,#2015,#2016,#2017,
#2018,#2019),#8977,.T.);
#9477=ADVANCED_FACE('',(#2490),#8978,.T.);
#9478=ADVANCED_FACE('',(#2491),#8979,.T.);
#9479=ADVANCED_FACE('',(#2492),#8980,.T.);
#9633=CLOSED_SHELL('',(#9330,#9331,#9332,#9333,#9334,#9335,#9336,#9337,
#9338,#9339,#9340,#9341,#9342,#9343,#9344,#9345,#9346,#9347,#9348,#9349,
#9350,#9351,#9352,#9353,#9354,#9355,#9356,#9357,#9358,#9359,#9360,#9361,
#9362,#9363,#9364,#9365,#9366,#9367,#9368,#9369,#9370,#9371,#9372,#9373,
#9374,#9375,#9376,#9377,#9378,#9379,#9380,#9381,#9382,#9383,#9384,#9385,
#9386,#9387,#9388,#9389,#9390,#9391,#9392,#9393,#9394,#9395,#9396,#9397,
#9398,#9399,#9400,#9401,#9402,#9403,#9404,#9405,#9406,#9407,#9408,#9409,
#9410,#9411,#9412,#9413,#9414,#9415,#9416,#9417,#9418,#9419,#9420,#9421,
#9422,#9423,#9424,#9425,#9426,#9427,#9428,#9429,#9430,#9431,#9432,#9433,
#9434,#9435,#9436,#9437,#9438,#9439,#9440,#9441,#9442,#9443,#9444,#9445,
#9446,#9447,#9448,#9449,#9450,#9451,#9452,#9453,#9454,#9455,#9456,#9457,
#9458,#9459,#9460,#9461,#9462,#9463,#9464,#9465,#9466,#9467,#9468,#9469,
#9470,#9471,#9472,#9473,#9474,#9475,#9476,#9477,#9478,#9479));
#10399=AXIS2_PLACEMENT_3D('',#15612,#12665,#12666);
#10400=AXIS2_PLACEMENT_3D('',#15613,#12667,#12668);
#10401=AXIS2_PLACEMENT_3D('',#15615,#12669,#12670);
#10402=AXIS2_PLACEMENT_3D('',#15618,#12672,#12673);
#10403=AXIS2_PLACEMENT_3D('',#15619,#12674,#12675);
#10404=AXIS2_PLACEMENT_3D('',#15621,#12676,#12677);
#10405=AXIS2_PLACEMENT_3D('',#15625,#12679,#12680);
#10406=AXIS2_PLACEMENT_3D('',#15651,#12682,#12683);
#10407=AXIS2_PLACEMENT_3D('',#15676,#12685,#12686);
#10408=AXIS2_PLACEMENT_3D('',#15677,#12687,#12688);
#10409=AXIS2_PLACEMENT_3D('',#15685,#12692,#12693);
#10410=AXIS2_PLACEMENT_3D('',#15689,#12695,#12696);
#10411=AXIS2_PLACEMENT_3D('',#15693,#12698,#12699);
#10412=AXIS2_PLACEMENT_3D('',#15697,#12701,#12702);
#10413=AXIS2_PLACEMENT_3D('',#15705,#12706,#12707);
#10414=AXIS2_PLACEMENT_3D('',#15709,#12709,#12710);
#10415=AXIS2_PLACEMENT_3D('',#15711,#12711,#12712);
#10416=AXIS2_PLACEMENT_3D('',#15715,#12714,#12715);
#10417=AXIS2_PLACEMENT_3D('',#15717,#12716,#12717);
#10418=AXIS2_PLACEMENT_3D('',#15721,#12719,#12720);
#10419=AXIS2_PLACEMENT_3D('',#15723,#12721,#12722);
#10420=AXIS2_PLACEMENT_3D('',#15725,#12724,#12725);
#10421=AXIS2_PLACEMENT_3D('',#15728,#12727,#12728);
#10422=AXIS2_PLACEMENT_3D('',#15729,#12729,#12730);
#10423=AXIS2_PLACEMENT_3D('',#15733,#12733,#12734);
#10424=AXIS2_PLACEMENT_3D('',#15736,#12736,#12737);
#10425=AXIS2_PLACEMENT_3D('',#15737,#12738,#12739);
#10426=AXIS2_PLACEMENT_3D('',#15739,#12740,#12741);
#10427=AXIS2_PLACEMENT_3D('',#15766,#12744,#12745);
#10428=AXIS2_PLACEMENT_3D('',#15790,#12747,#12748);
#10429=AXIS2_PLACEMENT_3D('',#15792,#12749,#12750);
#10430=AXIS2_PLACEMENT_3D('',#15795,#12752,#12753);
#10431=AXIS2_PLACEMENT_3D('',#15796,#12754,#12755);
#10432=AXIS2_PLACEMENT_3D('',#15798,#12756,#12757);
#10433=AXIS2_PLACEMENT_3D('',#15801,#12759,#12760);
#10434=AXIS2_PLACEMENT_3D('',#15802,#12761,#12762);
#10435=AXIS2_PLACEMENT_3D('',#15804,#12763,#12764);
#10436=AXIS2_PLACEMENT_3D('',#15808,#12766,#12767);
#10437=AXIS2_PLACEMENT_3D('',#15856,#12770,#12771);
#10438=AXIS2_PLACEMENT_3D('',#15857,#12772,#12773);
#10439=AXIS2_PLACEMENT_3D('',#15859,#12774,#12775);
#10440=AXIS2_PLACEMENT_3D('',#15862,#12777,#12778);
#10441=AXIS2_PLACEMENT_3D('',#15863,#12779,#12780);
#10442=AXIS2_PLACEMENT_3D('',#15865,#12781,#12782);
#10443=AXIS2_PLACEMENT_3D('',#15869,#12784,#12785);
#10444=AXIS2_PLACEMENT_3D('',#15917,#12788,#12789);
#10445=AXIS2_PLACEMENT_3D('',#15918,#12790,#12791);
#10446=AXIS2_PLACEMENT_3D('',#15920,#12792,#12793);
#10447=AXIS2_PLACEMENT_3D('',#15923,#12795,#12796);
#10448=AXIS2_PLACEMENT_3D('',#15924,#12797,#12798);
#10449=AXIS2_PLACEMENT_3D('',#15926,#12799,#12800);
#10450=AXIS2_PLACEMENT_3D('',#15930,#12802,#12803);
#10451=AXIS2_PLACEMENT_3D('',#15978,#12806,#12807);
#10452=AXIS2_PLACEMENT_3D('',#15979,#12808,#12809);
#10453=AXIS2_PLACEMENT_3D('',#15981,#12810,#12811);
#10454=AXIS2_PLACEMENT_3D('',#15984,#12813,#12814);
#10455=AXIS2_PLACEMENT_3D('',#15985,#12815,#12816);
#10456=AXIS2_PLACEMENT_3D('',#15987,#12817,#12818);
#10457=AXIS2_PLACEMENT_3D('',#16014,#12821,#12822);
#10458=AXIS2_PLACEMENT_3D('',#16038,#12824,#12825);
#10459=AXIS2_PLACEMENT_3D('',#16040,#12826,#12827);
#10460=AXIS2_PLACEMENT_3D('',#16043,#12829,#12830);
#10461=AXIS2_PLACEMENT_3D('',#16044,#12831,#12832);
#10462=AXIS2_PLACEMENT_3D('',#16046,#12833,#12834);
#10463=AXIS2_PLACEMENT_3D('',#16050,#12836,#12837);
#10464=AXIS2_PLACEMENT_3D('',#16098,#12840,#12841);
#10465=AXIS2_PLACEMENT_3D('',#16099,#12842,#12843);
#10466=AXIS2_PLACEMENT_3D('',#16101,#12844,#12845);
#10467=AXIS2_PLACEMENT_3D('',#16105,#12847,#12848);
#10468=AXIS2_PLACEMENT_3D('',#16131,#12850,#12851);
#10469=AXIS2_PLACEMENT_3D('',#16157,#12853,#12854);
#10470=AXIS2_PLACEMENT_3D('',#16181,#12855,#12856);
#10471=AXIS2_PLACEMENT_3D('',#16200,#12857,#12858);
#10472=AXIS2_PLACEMENT_3D('',#16219,#12859,#12860);
#10473=AXIS2_PLACEMENT_3D('',#16242,#12861,#12862);
#10474=AXIS2_PLACEMENT_3D('',#16243,#12863,#12864);
#10475=AXIS2_PLACEMENT_3D('',#16245,#12865,#12866);
#10476=AXIS2_PLACEMENT_3D('',#16249,#12868,#12869);
#10477=AXIS2_PLACEMENT_3D('',#16297,#12872,#12873);
#10478=AXIS2_PLACEMENT_3D('',#16298,#12874,#12875);
#10479=AXIS2_PLACEMENT_3D('',#16300,#12876,#12877);
#10480=AXIS2_PLACEMENT_3D('',#16304,#12879,#12880);
#10481=AXIS2_PLACEMENT_3D('',#16330,#12882,#12883);
#10482=AXIS2_PLACEMENT_3D('',#16356,#12885,#12886);
#10483=AXIS2_PLACEMENT_3D('',#16380,#12887,#12888);
#10484=AXIS2_PLACEMENT_3D('',#16399,#12889,#12890);
#10485=AXIS2_PLACEMENT_3D('',#16418,#12891,#12892);
#10486=AXIS2_PLACEMENT_3D('',#16441,#12893,#12894);
#10487=AXIS2_PLACEMENT_3D('',#16442,#12895,#12896);
#10488=AXIS2_PLACEMENT_3D('',#16444,#12897,#12898);
#10489=AXIS2_PLACEMENT_3D('',#16448,#12900,#12901);
#10490=AXIS2_PLACEMENT_3D('',#16474,#12903,#12904);
#10491=AXIS2_PLACEMENT_3D('',#16500,#12906,#12907);
#10492=AXIS2_PLACEMENT_3D('',#16524,#12908,#12909);
#10493=AXIS2_PLACEMENT_3D('',#16543,#12910,#12911);
#10494=AXIS2_PLACEMENT_3D('',#16562,#12912,#12913);
#10495=AXIS2_PLACEMENT_3D('',#16585,#12914,#12915);
#10496=AXIS2_PLACEMENT_3D('',#16586,#12916,#12917);
#10497=AXIS2_PLACEMENT_3D('',#16588,#12918,#12919);
#10498=AXIS2_PLACEMENT_3D('',#16592,#12921,#12922);
#10499=AXIS2_PLACEMENT_3D('',#16618,#12924,#12925);
#10500=AXIS2_PLACEMENT_3D('',#16644,#12927,#12928);
#10501=AXIS2_PLACEMENT_3D('',#16668,#12929,#12930);
#10502=AXIS2_PLACEMENT_3D('',#16687,#12931,#12932);
#10503=AXIS2_PLACEMENT_3D('',#16706,#12933,#12934);
#10504=AXIS2_PLACEMENT_3D('',#16729,#12935,#12936);
#10505=AXIS2_PLACEMENT_3D('',#16730,#12937,#12938);
#10506=AXIS2_PLACEMENT_3D('',#16732,#12939,#12940);
#10507=AXIS2_PLACEMENT_3D('',#16735,#12942,#12943);
#10508=AXIS2_PLACEMENT_3D('',#16736,#12944,#12945);
#10509=AXIS2_PLACEMENT_3D('',#16738,#12946,#12947);
#10510=AXIS2_PLACEMENT_3D('',#16765,#12950,#12951);
#10511=AXIS2_PLACEMENT_3D('',#16789,#12953,#12954);
#10512=AXIS2_PLACEMENT_3D('',#16791,#12956,#12957);
#10513=AXIS2_PLACEMENT_3D('',#16793,#12958,#12959);
#10514=AXIS2_PLACEMENT_3D('',#16795,#12961,#12962);
#10515=AXIS2_PLACEMENT_3D('',#16797,#12964,#12965);
#10516=AXIS2_PLACEMENT_3D('',#16800,#12967,#12968);
#10517=AXIS2_PLACEMENT_3D('',#16801,#12969,#12970);
#10518=AXIS2_PLACEMENT_3D('',#16803,#12972,#12973);
#10519=AXIS2_PLACEMENT_3D('',#16807,#12976,#12977);
#10520=AXIS2_PLACEMENT_3D('',#16809,#12979,#12980);
#10521=AXIS2_PLACEMENT_3D('',#16813,#12983,#12984);
#10522=AXIS2_PLACEMENT_3D('',#16815,#12986,#12987);
#10523=AXIS2_PLACEMENT_3D('',#16817,#12989,#12990);
#10524=AXIS2_PLACEMENT_3D('',#16819,#12991,#12992);
#10525=AXIS2_PLACEMENT_3D('',#16821,#12994,#12995);
#10526=AXIS2_PLACEMENT_3D('',#16823,#12997,#12998);
#10527=AXIS2_PLACEMENT_3D('',#16826,#13000,#13001);
#10528=AXIS2_PLACEMENT_3D('',#16827,#13002,#13003);
#10529=AXIS2_PLACEMENT_3D('',#16831,#13005,#13006);
#10530=AXIS2_PLACEMENT_3D('',#16833,#13008,#13009);
#10531=AXIS2_PLACEMENT_3D('',#16836,#13012,#13013);
#10532=AXIS2_PLACEMENT_3D('',#16840,#13015,#13016);
#10533=AXIS2_PLACEMENT_3D('',#16842,#13018,#13019);
#10534=AXIS2_PLACEMENT_3D('',#16845,#13022,#13023);
#10535=AXIS2_PLACEMENT_3D('',#16848,#13026,#13027);
#10536=AXIS2_PLACEMENT_3D('',#16852,#13030,#13031);
#10537=AXIS2_PLACEMENT_3D('',#16854,#13033,#13034);
#10538=AXIS2_PLACEMENT_3D('',#16858,#13037,#13038);
#10539=AXIS2_PLACEMENT_3D('',#16860,#13040,#13041);
#10540=AXIS2_PLACEMENT_3D('',#16862,#13043,#13044);
#10541=AXIS2_PLACEMENT_3D('',#16866,#13046,#13047);
#10542=AXIS2_PLACEMENT_3D('',#16868,#13049,#13050);
#10543=AXIS2_PLACEMENT_3D('',#16871,#13053,#13054);
#10544=AXIS2_PLACEMENT_3D('',#16875,#13056,#13057);
#10545=AXIS2_PLACEMENT_3D('',#16877,#13059,#13060);
#10546=AXIS2_PLACEMENT_3D('',#16880,#13063,#13064);
#10547=AXIS2_PLACEMENT_3D('',#16882,#13065,#13066);
#10548=AXIS2_PLACEMENT_3D('',#16884,#13068,#13069);
#10549=AXIS2_PLACEMENT_3D('',#16886,#13071,#13072);
#10550=AXIS2_PLACEMENT_3D('',#16889,#13074,#13075);
#10551=AXIS2_PLACEMENT_3D('',#16890,#13076,#13077);
#10552=AXIS2_PLACEMENT_3D('',#16892,#13079,#13080);
#10553=AXIS2_PLACEMENT_3D('',#16894,#13082,#13083);
#10554=AXIS2_PLACEMENT_3D('',#16898,#13086,#13087);
#10555=AXIS2_PLACEMENT_3D('',#16900,#13089,#13090);
#10556=AXIS2_PLACEMENT_3D('',#16904,#13093,#13094);
#10557=AXIS2_PLACEMENT_3D('',#16906,#13096,#13097);
#10558=AXIS2_PLACEMENT_3D('',#16910,#13100,#13101);
#10559=AXIS2_PLACEMENT_3D('',#16914,#13104,#13105);
#10560=AXIS2_PLACEMENT_3D('',#16916,#13107,#13108);
#10561=AXIS2_PLACEMENT_3D('',#16918,#13110,#13111);
#10562=AXIS2_PLACEMENT_3D('',#16919,#13112,#13113);
#10563=AXIS2_PLACEMENT_3D('',#16920,#13114,#13115);
#10564=AXIS2_PLACEMENT_3D('',#16921,#13116,#13117);
#10565=AXIS2_PLACEMENT_3D('',#16922,#13118,#13119);
#10566=AXIS2_PLACEMENT_3D('',#16923,#13120,#13121);
#10567=AXIS2_PLACEMENT_3D('',#16924,#13122,#13123);
#10568=AXIS2_PLACEMENT_3D('',#16936,#13132,#13133);
#10569=AXIS2_PLACEMENT_3D('',#16938,#13135,#13136);
#10570=AXIS2_PLACEMENT_3D('',#16941,#13138,#13139);
#10571=AXIS2_PLACEMENT_3D('',#16942,#13140,#13141);
#10572=AXIS2_PLACEMENT_3D('',#16944,#13143,#13144);
#10573=AXIS2_PLACEMENT_3D('',#16946,#13146,#13147);
#10574=AXIS2_PLACEMENT_3D('',#16948,#13149,#13150);
#10575=AXIS2_PLACEMENT_3D('',#16952,#13153,#13154);
#10576=AXIS2_PLACEMENT_3D('',#16954,#13156,#13157);
#10577=AXIS2_PLACEMENT_3D('',#16956,#13159,#13160);
#10578=AXIS2_PLACEMENT_3D('',#16958,#13162,#13163);
#10579=AXIS2_PLACEMENT_3D('',#16959,#13164,#13165);
#10580=AXIS2_PLACEMENT_3D('',#16960,#13166,#13167);
#10581=AXIS2_PLACEMENT_3D('',#16961,#13168,#13169);
#10582=AXIS2_PLACEMENT_3D('',#16962,#13170,#13171);
#10583=AXIS2_PLACEMENT_3D('',#16963,#13172,#13173);
#10584=AXIS2_PLACEMENT_3D('',#16967,#13177,#13178);
#10585=AXIS2_PLACEMENT_3D('',#16974,#13183,#13184);
#10586=AXIS2_PLACEMENT_3D('',#16976,#13185,#13186);
#10587=AXIS2_PLACEMENT_3D('',#16977,#13187,#13188);
#10588=AXIS2_PLACEMENT_3D('',#16978,#13189,#13190);
#10589=AXIS2_PLACEMENT_3D('',#16980,#13191,#13192);
#10590=AXIS2_PLACEMENT_3D('',#16981,#13193,#13194);
#10591=AXIS2_PLACEMENT_3D('',#16982,#13195,#13196);
#10592=AXIS2_PLACEMENT_3D('',#16984,#13197,#13198);
#10593=AXIS2_PLACEMENT_3D('',#16986,#13199,#13200);
#10594=AXIS2_PLACEMENT_3D('',#16987,#13201,#13202);
#10595=AXIS2_PLACEMENT_3D('',#16988,#13203,#13204);
#10596=AXIS2_PLACEMENT_3D('',#16990,#13206,#13207);
#10597=AXIS2_PLACEMENT_3D('',#16993,#13208,#13209);
#10598=AXIS2_PLACEMENT_3D('',#16994,#13210,#13211);
#10599=AXIS2_PLACEMENT_3D('',#16995,#13212,#13213);
#10600=AXIS2_PLACEMENT_3D('',#16996,#13214,#13215);
#10601=AXIS2_PLACEMENT_3D('',#16998,#13216,#13217);
#10602=AXIS2_PLACEMENT_3D('',#17000,#13218,#13219);
#10603=AXIS2_PLACEMENT_3D('',#17001,#13220,#13221);
#10604=AXIS2_PLACEMENT_3D('',#17002,#13222,#13223);
#10605=AXIS2_PLACEMENT_3D('',#17005,#13224,#13225);
#10606=AXIS2_PLACEMENT_3D('',#17006,#13226,#13227);
#10607=AXIS2_PLACEMENT_3D('',#17007,#13228,#13229);
#10608=AXIS2_PLACEMENT_3D('',#17008,#13230,#13231);
#10609=AXIS2_PLACEMENT_3D('',#17010,#13233,#13234);
#10610=AXIS2_PLACEMENT_3D('',#17012,#13235,#13236);
#10611=AXIS2_PLACEMENT_3D('',#17013,#13237,#13238);
#10612=AXIS2_PLACEMENT_3D('',#17014,#13239,#13240);
#10613=AXIS2_PLACEMENT_3D('',#17016,#13242,#13243);
#10614=AXIS2_PLACEMENT_3D('',#17019,#13244,#13245);
#10615=AXIS2_PLACEMENT_3D('',#17020,#13246,#13247);
#10616=AXIS2_PLACEMENT_3D('',#17021,#13248,#13249);
#10617=AXIS2_PLACEMENT_3D('',#17022,#13250,#13251);
#10618=AXIS2_PLACEMENT_3D('',#17024,#13253,#13254);
#10619=AXIS2_PLACEMENT_3D('',#17026,#13255,#13256);
#10620=AXIS2_PLACEMENT_3D('',#17027,#13257,#13258);
#10621=AXIS2_PLACEMENT_3D('',#17028,#13259,#13260);
#10622=AXIS2_PLACEMENT_3D('',#17030,#13261,#13262);
#10623=AXIS2_PLACEMENT_3D('',#17032,#13263,#13264);
#10624=AXIS2_PLACEMENT_3D('',#17033,#13265,#13266);
#10625=AXIS2_PLACEMENT_3D('',#17034,#13267,#13268);
#10626=AXIS2_PLACEMENT_3D('',#17036,#13270,#13271);
#10627=AXIS2_PLACEMENT_3D('',#17038,#13272,#13273);
#10628=AXIS2_PLACEMENT_3D('',#17039,#13274,#13275);
#10629=AXIS2_PLACEMENT_3D('',#17040,#13276,#13277);
#10630=AXIS2_PLACEMENT_3D('',#17042,#13279,#13280);
#10631=AXIS2_PLACEMENT_3D('',#17045,#13281,#13282);
#10632=AXIS2_PLACEMENT_3D('',#17047,#13283,#13284);
#10633=AXIS2_PLACEMENT_3D('',#17048,#13285,#13286);
#10634=AXIS2_PLACEMENT_3D('',#17049,#13287,#13288);
#10635=AXIS2_PLACEMENT_3D('',#17052,#13291,#13292);
#10636=AXIS2_PLACEMENT_3D('',#17054,#13293,#13294);
#10637=AXIS2_PLACEMENT_3D('',#17055,#13295,#13296);
#10638=AXIS2_PLACEMENT_3D('',#17056,#13297,#13298);
#10639=AXIS2_PLACEMENT_3D('',#17059,#13299,#13300);
#10640=AXIS2_PLACEMENT_3D('',#17061,#13301,#13302);
#10641=AXIS2_PLACEMENT_3D('',#17062,#13303,#13304);
#10642=AXIS2_PLACEMENT_3D('',#17063,#13305,#13306);
#10643=AXIS2_PLACEMENT_3D('',#17066,#13309,#13310);
#10644=AXIS2_PLACEMENT_3D('',#17068,#13311,#13312);
#10645=AXIS2_PLACEMENT_3D('',#17070,#13313,#13314);
#10646=AXIS2_PLACEMENT_3D('',#17071,#13315,#13316);
#10647=AXIS2_PLACEMENT_3D('',#17072,#13317,#13318);
#10648=AXIS2_PLACEMENT_3D('',#17074,#13320,#13321);
#10649=AXIS2_PLACEMENT_3D('',#17077,#13322,#13323);
#10650=AXIS2_PLACEMENT_3D('',#17079,#13324,#13325);
#10651=AXIS2_PLACEMENT_3D('',#17080,#13326,#13327);
#10652=AXIS2_PLACEMENT_3D('',#17081,#13328,#13329);
#10653=AXIS2_PLACEMENT_3D('',#17083,#13330,#13331);
#10654=AXIS2_PLACEMENT_3D('',#17085,#13332,#13333);
#10655=AXIS2_PLACEMENT_3D('',#17086,#13334,#13335);
#10656=AXIS2_PLACEMENT_3D('',#17087,#13336,#13337);
#10657=AXIS2_PLACEMENT_3D('',#17090,#13338,#13339);
#10658=AXIS2_PLACEMENT_3D('',#17092,#13340,#13341);
#10659=AXIS2_PLACEMENT_3D('',#17093,#13342,#13343);
#10660=AXIS2_PLACEMENT_3D('',#17094,#13344,#13345);
#10661=AXIS2_PLACEMENT_3D('',#17096,#13346,#13347);
#10662=AXIS2_PLACEMENT_3D('',#17097,#13348,#13349);
#10663=AXIS2_PLACEMENT_3D('',#17098,#13350,#13351);
#10664=AXIS2_PLACEMENT_3D('',#17100,#13353,#13354);
#10665=AXIS2_PLACEMENT_3D('',#17103,#13355,#13356);
#10666=AXIS2_PLACEMENT_3D('',#17104,#13357,#13358);
#10667=AXIS2_PLACEMENT_3D('',#17105,#13359,#13360);
#10668=AXIS2_PLACEMENT_3D('',#17106,#13361,#13362);
#10669=AXIS2_PLACEMENT_3D('',#17108,#13363,#13364);
#10670=AXIS2_PLACEMENT_3D('',#17109,#13365,#13366);
#10671=AXIS2_PLACEMENT_3D('',#17110,#13367,#13368);
#10672=AXIS2_PLACEMENT_3D('',#17113,#13369,#13370);
#10673=AXIS2_PLACEMENT_3D('',#17114,#13371,#13372);
#10674=AXIS2_PLACEMENT_3D('',#17115,#13373,#13374);
#10675=AXIS2_PLACEMENT_3D('',#17116,#13375,#13376);
#10676=AXIS2_PLACEMENT_3D('',#17118,#13377,#13378);
#10677=AXIS2_PLACEMENT_3D('',#17120,#13379,#13380);
#10678=AXIS2_PLACEMENT_3D('',#17121,#13381,#13382);
#10679=AXIS2_PLACEMENT_3D('',#17122,#13383,#13384);
#10680=AXIS2_PLACEMENT_3D('',#17124,#13386,#13387);
#10681=AXIS2_PLACEMENT_3D('',#17126,#13389,#13390);
#10682=AXIS2_PLACEMENT_3D('',#17128,#13391,#13392);
#10683=AXIS2_PLACEMENT_3D('',#17130,#13393,#13394);
#10684=AXIS2_PLACEMENT_3D('',#17131,#13395,#13396);
#10685=AXIS2_PLACEMENT_3D('',#17132,#13397,#13398);
#10686=AXIS2_PLACEMENT_3D('',#17134,#13400,#13401);
#10687=AXIS2_PLACEMENT_3D('',#17136,#13403,#13404);
#10688=AXIS2_PLACEMENT_3D('',#17138,#13406,#13407);
#10689=AXIS2_PLACEMENT_3D('',#17141,#13410,#13411);
#10690=AXIS2_PLACEMENT_3D('',#17143,#13413,#13414);
#10691=AXIS2_PLACEMENT_3D('',#17145,#13416,#13417);
#10692=AXIS2_PLACEMENT_3D('',#17148,#13420,#13421);
#10693=AXIS2_PLACEMENT_3D('',#17151,#13424,#13425);
#10694=AXIS2_PLACEMENT_3D('',#17154,#13428,#13429);
#10695=AXIS2_PLACEMENT_3D('',#17156,#13431,#13432);
#10696=AXIS2_PLACEMENT_3D('',#17159,#13435,#13436);
#10697=AXIS2_PLACEMENT_3D('',#17162,#13439,#13440);
#10698=AXIS2_PLACEMENT_3D('',#17164,#13442,#13443);
#10699=AXIS2_PLACEMENT_3D('',#17166,#13445,#13446);
#10700=AXIS2_PLACEMENT_3D('',#17168,#13448,#13449);
#10701=AXIS2_PLACEMENT_3D('',#17170,#13451,#13452);
#10702=AXIS2_PLACEMENT_3D('',#17172,#13454,#13455);
#10703=AXIS2_PLACEMENT_3D('',#17174,#13457,#13458);
#10704=AXIS2_PLACEMENT_3D('',#17176,#13460,#13461);
#10705=AXIS2_PLACEMENT_3D('',#17179,#13464,#13465);
#10706=AXIS2_PLACEMENT_3D('',#17180,#13466,#13467);
#10707=AXIS2_PLACEMENT_3D('',#17181,#13468,#13469);
#10708=AXIS2_PLACEMENT_3D('',#17182,#13470,#13471);
#10709=AXIS2_PLACEMENT_3D('',#17183,#13472,#13473);
#10710=AXIS2_PLACEMENT_3D('',#17184,#13474,#13475);
#10711=AXIS2_PLACEMENT_3D('',#17185,#13476,#13477);
#10712=AXIS2_PLACEMENT_3D('',#17186,#13478,#13479);
#10713=AXIS2_PLACEMENT_3D('',#17187,#13480,#13481);
#12665=DIRECTION('axis',(0.,0.,1.));
#12666=DIRECTION('refdir',(1.,0.,0.));
#12667=DIRECTION('center_axis',(0.,0.,-1.));
#12668=DIRECTION('ref_axis',(-1.,0.,0.));
#12669=DIRECTION('center_axis',(0.,0.,-1.));
#12670=DIRECTION('ref_axis',(-1.,0.,0.));
#12671=DIRECTION('',(0.,0.,-1.));
#12672=DIRECTION('center_axis',(0.,0.,1.));
#12673=DIRECTION('ref_axis',(-1.,0.,0.));
#12674=DIRECTION('center_axis',(0.,0.,-1.));
#12675=DIRECTION('ref_axis',(-1.,0.,0.));
#12676=DIRECTION('center_axis',(0.,0.,-1.));
#12677=DIRECTION('ref_axis',(-1.,0.,0.));
#12678=DIRECTION('',(0.,0.,-1.));
#12679=DIRECTION('center_axis',(0.,0.,1.));
#12680=DIRECTION('ref_axis',(-1.,0.,0.));
#12681=DIRECTION('',(0.,0.,1.));
#12682=DIRECTION('center_axis',(0.,0.,1.));
#12683=DIRECTION('ref_axis',(-1.,0.,0.));
#12684=DIRECTION('',(0.,0.,-1.));
#12685=DIRECTION('center_axis',(0.,0.,1.));
#12686=DIRECTION('ref_axis',(-1.,0.,0.));
#12687=DIRECTION('center_axis',(0.,0.,-1.));
#12688=DIRECTION('ref_axis',(-2.22044604925031E-16,-1.,0.));
#12689=DIRECTION('',(1.,-2.22044604925031E-16,0.));
#12690=DIRECTION('',(-2.22044604925031E-16,-1.,0.));
#12691=DIRECTION('',(-1.,2.22044604925031E-16,0.));
#12692=DIRECTION('center_axis',(0.,0.,1.));
#12693=DIRECTION('ref_axis',(-1.,0.,0.));
#12694=DIRECTION('',(-1.,2.22044604925031E-16,0.));
#12695=DIRECTION('center_axis',(0.,0.,1.));
#12696=DIRECTION('ref_axis',(-1.,0.,0.));
#12697=DIRECTION('',(-1.,2.22044604925031E-16,0.));
#12698=DIRECTION('center_axis',(0.,0.,1.));
#12699=DIRECTION('ref_axis',(-1.,0.,0.));
#12700=DIRECTION('',(-1.,2.22044604925031E-16,0.));
#12701=DIRECTION('center_axis',(0.,0.,1.));
#12702=DIRECTION('ref_axis',(-1.,0.,0.));
#12703=DIRECTION('',(-1.,2.22044604925031E-16,0.));
#12704=DIRECTION('',(2.22044604925031E-16,1.,0.));
#12705=DIRECTION('',(1.,-2.22044604925031E-16,0.));
#12706=DIRECTION('center_axis',(0.,0.,1.));
#12707=DIRECTION('ref_axis',(-1.,0.,0.));
#12708=DIRECTION('',(1.,-2.22044604925031E-16,0.));
#12709=DIRECTION('center_axis',(0.,0.,1.));
#12710=DIRECTION('ref_axis',(-1.,0.,0.));
#12711=DIRECTION('center_axis',(0.,0.,1.));
#12712=DIRECTION('ref_axis',(-1.,0.,0.));
#12713=DIRECTION('',(1.,-2.22044604925031E-16,0.));
#12714=DIRECTION('center_axis',(0.,0.,1.));
#12715=DIRECTION('ref_axis',(-1.,0.,0.));
#12716=DIRECTION('center_axis',(0.,0.,1.));
#12717=DIRECTION('ref_axis',(-1.,0.,0.));
#12718=DIRECTION('',(1.,-2.22044604925031E-16,0.));
#12719=DIRECTION('center_axis',(0.,0.,1.));
#12720=DIRECTION('ref_axis',(-1.,0.,0.));
#12721=DIRECTION('center_axis',(0.,0.,1.));
#12722=DIRECTION('ref_axis',(-1.,0.,0.));
#12723=DIRECTION('',(1.,-2.22044604925031E-16,0.));
#12724=DIRECTION('center_axis',(-1.,2.22044604925031E-16,0.));
#12725=DIRECTION('ref_axis',(-1.57009245868376E-16,-0.707106781186541,-0.707106781186554));
#12726=DIRECTION('',(-1.,2.22044604925031E-16,0.));
#12727=DIRECTION('center_axis',(-1.,2.22044604925031E-16,0.));
#12728=DIRECTION('ref_axis',(-2.22044604925031E-16,-1.,0.));
#12729=DIRECTION('center_axis',(-2.22044604925031E-16,-1.,0.));
#12730=DIRECTION('ref_axis',(0.,0.,1.));
#12731=DIRECTION('',(1.,-2.22044604925031E-16,0.));
#12732=DIRECTION('',(0.,0.,1.));
#12733=DIRECTION('center_axis',(1.,-2.22044604925031E-16,0.));
#12734=DIRECTION('ref_axis',(1.57009245868376E-16,0.707106781186541,0.707106781186554));
#12735=DIRECTION('',(-1.,2.22044604925031E-16,0.));
#12736=DIRECTION('center_axis',(1.,-2.22044604925031E-16,0.));
#12737=DIRECTION('ref_axis',(0.,0.,1.));
#12738=DIRECTION('center_axis',(0.,0.,-1.));
#12739=DIRECTION('ref_axis',(-1.,0.,0.));
#12740=DIRECTION('center_axis',(0.,0.,-1.));
#12741=DIRECTION('ref_axis',(-1.,0.,0.));
#12742=DIRECTION('',(0.,0.,-1.));
#12743=DIRECTION('',(0.,0.,-1.));
#12744=DIRECTION('center_axis',(0.,0.,1.));
#12745=DIRECTION('ref_axis',(-1.,0.,0.));
#12746=DIRECTION('',(0.,0.,1.));
#12747=DIRECTION('center_axis',(0.,0.,-1.));
#12748=DIRECTION('ref_axis',(-1.,0.,0.));
#12749=DIRECTION('center_axis',(0.,0.,-1.));
#12750=DIRECTION('ref_axis',(-1.,0.,0.));
#12751=DIRECTION('',(0.,0.,-1.));
#12752=DIRECTION('center_axis',(0.,0.,1.));
#12753=DIRECTION('ref_axis',(-1.,0.,0.));
#12754=DIRECTION('center_axis',(0.,0.,-1.));
#12755=DIRECTION('ref_axis',(-1.,0.,0.));
#12756=DIRECTION('center_axis',(0.,0.,-1.));
#12757=DIRECTION('ref_axis',(-1.,0.,0.));
#12758=DIRECTION('',(0.,0.,-1.));
#12759=DIRECTION('center_axis',(0.,0.,1.));
#12760=DIRECTION('ref_axis',(-1.,0.,0.));
#12761=DIRECTION('center_axis',(0.,0.,-1.));
#12762=DIRECTION('ref_axis',(-1.,0.,0.));
#12763=DIRECTION('center_axis',(0.,0.,-1.));
#12764=DIRECTION('ref_axis',(-1.,0.,0.));
#12765=DIRECTION('',(0.,0.,-1.));
#12766=DIRECTION('center_axis',(0.,0.,1.));
#12767=DIRECTION('ref_axis',(-1.,0.,0.));
#12768=DIRECTION('',(0.,0.,-1.));
#12769=DIRECTION('',(0.,0.,1.));
#12770=DIRECTION('center_axis',(0.,0.,1.));
#12771=DIRECTION('ref_axis',(-1.,0.,0.));
#12772=DIRECTION('center_axis',(0.,0.,-1.));
#12773=DIRECTION('ref_axis',(-1.,0.,0.));
#12774=DIRECTION('center_axis',(0.,0.,-1.));
#12775=DIRECTION('ref_axis',(-1.,0.,0.));
#12776=DIRECTION('',(0.,0.,-1.));
#12777=DIRECTION('center_axis',(0.,0.,1.));
#12778=DIRECTION('ref_axis',(-1.,0.,0.));
#12779=DIRECTION('center_axis',(0.,0.,-1.));
#12780=DIRECTION('ref_axis',(-1.,0.,0.));
#12781=DIRECTION('center_axis',(0.,0.,-1.));
#12782=DIRECTION('ref_axis',(-1.,0.,0.));
#12783=DIRECTION('',(0.,0.,-1.));
#12784=DIRECTION('center_axis',(0.,0.,1.));
#12785=DIRECTION('ref_axis',(-1.,0.,0.));
#12786=DIRECTION('',(0.,0.,-1.));
#12787=DIRECTION('',(0.,0.,1.));
#12788=DIRECTION('center_axis',(0.,0.,1.));
#12789=DIRECTION('ref_axis',(-1.,0.,0.));
#12790=DIRECTION('center_axis',(0.,0.,-1.));
#12791=DIRECTION('ref_axis',(-1.,0.,0.));
#12792=DIRECTION('center_axis',(0.,0.,-1.));
#12793=DIRECTION('ref_axis',(-1.,0.,0.));
#12794=DIRECTION('',(0.,0.,-1.));
#12795=DIRECTION('center_axis',(0.,0.,1.));
#12796=DIRECTION('ref_axis',(-1.,0.,0.));
#12797=DIRECTION('center_axis',(0.,0.,-1.));
#12798=DIRECTION('ref_axis',(-1.,0.,0.));
#12799=DIRECTION('center_axis',(0.,0.,-1.));
#12800=DIRECTION('ref_axis',(-1.,0.,0.));
#12801=DIRECTION('',(0.,0.,-1.));
#12802=DIRECTION('center_axis',(0.,0.,1.));
#12803=DIRECTION('ref_axis',(-1.,0.,0.));
#12804=DIRECTION('',(0.,0.,-1.));
#12805=DIRECTION('',(0.,0.,1.));
#12806=DIRECTION('center_axis',(0.,0.,1.));
#12807=DIRECTION('ref_axis',(-1.,0.,0.));
#12808=DIRECTION('center_axis',(0.,0.,-1.));
#12809=DIRECTION('ref_axis',(-1.,0.,0.));
#12810=DIRECTION('center_axis',(0.,0.,-1.));
#12811=DIRECTION('ref_axis',(-1.,0.,0.));
#12812=DIRECTION('',(0.,0.,-1.));
#12813=DIRECTION('center_axis',(0.,0.,1.));
#12814=DIRECTION('ref_axis',(-1.,0.,0.));
#12815=DIRECTION('center_axis',(0.,0.,-1.));
#12816=DIRECTION('ref_axis',(-1.,0.,0.));
#12817=DIRECTION('center_axis',(0.,0.,-1.));
#12818=DIRECTION('ref_axis',(-1.,0.,0.));
#12819=DIRECTION('',(0.,0.,-1.));
#12820=DIRECTION('',(0.,0.,-1.));
#12821=DIRECTION('center_axis',(0.,0.,1.));
#12822=DIRECTION('ref_axis',(-1.,0.,0.));
#12823=DIRECTION('',(0.,0.,1.));
#12824=DIRECTION('center_axis',(0.,0.,-1.));
#12825=DIRECTION('ref_axis',(-1.,0.,0.));
#12826=DIRECTION('center_axis',(0.,0.,-1.));
#12827=DIRECTION('ref_axis',(-1.,0.,0.));
#12828=DIRECTION('',(0.,0.,-1.));
#12829=DIRECTION('center_axis',(0.,0.,1.));
#12830=DIRECTION('ref_axis',(-1.,0.,0.));
#12831=DIRECTION('center_axis',(0.,0.,-1.));
#12832=DIRECTION('ref_axis',(-1.,0.,0.));
#12833=DIRECTION('center_axis',(0.,0.,-1.));
#12834=DIRECTION('ref_axis',(-1.,0.,0.));
#12835=DIRECTION('',(0.,0.,-1.));
#12836=DIRECTION('center_axis',(0.,0.,1.));
#12837=DIRECTION('ref_axis',(-1.,0.,0.));
#12838=DIRECTION('',(0.,0.,-1.));
#12839=DIRECTION('',(0.,0.,1.));
#12840=DIRECTION('center_axis',(0.,0.,1.));
#12841=DIRECTION('ref_axis',(-1.,0.,0.));
#12842=DIRECTION('center_axis',(0.,0.,-1.));
#12843=DIRECTION('ref_axis',(-1.,0.,0.));
#12844=DIRECTION('center_axis',(0.,0.,-1.));
#12845=DIRECTION('ref_axis',(-1.,0.,0.));
#12846=DIRECTION('',(0.,0.,-1.));
#12847=DIRECTION('center_axis',(0.,0.,1.));
#12848=DIRECTION('ref_axis',(-1.,0.,0.));
#12849=DIRECTION('',(0.,0.,1.));
#12850=DIRECTION('center_axis',(0.,0.,1.));
#12851=DIRECTION('ref_axis',(-1.,0.,0.));
#12852=DIRECTION('',(0.,0.,-1.));
#12853=DIRECTION('center_axis',(0.,0.,1.));
#12854=DIRECTION('ref_axis',(-1.,0.,0.));
#12855=DIRECTION('center_axis',(-1.57009245868377E-16,-0.707106781186548,
-0.707106781186548));
#12856=DIRECTION('ref_axis',(0.,0.707106781186547,-0.707106781186547));
#12857=DIRECTION('center_axis',(0.,0.,1.));
#12858=DIRECTION('ref_axis',(-1.,0.,0.));
#12859=DIRECTION('center_axis',(-1.57009245868377E-16,-0.707106781186548,
-0.707106781186548));
#12860=DIRECTION('ref_axis',(0.,0.707106781186547,-0.707106781186547));
#12861=DIRECTION('center_axis',(0.,0.,1.));
#12862=DIRECTION('ref_axis',(-1.,0.,0.));
#12863=DIRECTION('center_axis',(0.,0.,-1.));
#12864=DIRECTION('ref_axis',(-1.,0.,0.));
#12865=DIRECTION('center_axis',(0.,0.,-1.));
#12866=DIRECTION('ref_axis',(-1.,0.,0.));
#12867=DIRECTION('',(0.,0.,-1.));
#12868=DIRECTION('center_axis',(0.,0.,1.));
#12869=DIRECTION('ref_axis',(-1.,0.,0.));
#12870=DIRECTION('',(0.,0.,1.));
#12871=DIRECTION('',(0.,0.,-1.));
#12872=DIRECTION('center_axis',(0.,0.,1.));
#12873=DIRECTION('ref_axis',(-1.,0.,0.));
#12874=DIRECTION('center_axis',(0.,0.,-1.));
#12875=DIRECTION('ref_axis',(-1.,0.,0.));
#12876=DIRECTION('center_axis',(0.,0.,-1.));
#12877=DIRECTION('ref_axis',(-1.,0.,0.));
#12878=DIRECTION('',(0.,0.,-1.));
#12879=DIRECTION('center_axis',(0.,0.,1.));
#12880=DIRECTION('ref_axis',(-1.,0.,0.));
#12881=DIRECTION('',(0.,0.,1.));
#12882=DIRECTION('center_axis',(0.,0.,1.));
#12883=DIRECTION('ref_axis',(-1.,0.,0.));
#12884=DIRECTION('',(0.,0.,-1.));
#12885=DIRECTION('center_axis',(0.,0.,1.));
#12886=DIRECTION('ref_axis',(-1.,0.,0.));
#12887=DIRECTION('center_axis',(-1.57009245868377E-16,-0.707106781186548,
-0.707106781186548));
#12888=DIRECTION('ref_axis',(0.,0.707106781186547,-0.707106781186547));
#12889=DIRECTION('center_axis',(0.,0.,1.));
#12890=DIRECTION('ref_axis',(-1.,0.,0.));
#12891=DIRECTION('center_axis',(-1.57009245868377E-16,-0.707106781186548,
-0.707106781186548));
#12892=DIRECTION('ref_axis',(0.,0.707106781186547,-0.707106781186547));
#12893=DIRECTION('center_axis',(0.,0.,1.));
#12894=DIRECTION('ref_axis',(-1.,0.,0.));
#12895=DIRECTION('center_axis',(0.,0.,-1.));
#12896=DIRECTION('ref_axis',(-1.,0.,0.));
#12897=DIRECTION('center_axis',(0.,0.,-1.));
#12898=DIRECTION('ref_axis',(-1.,0.,0.));
#12899=DIRECTION('',(0.,0.,-1.));
#12900=DIRECTION('center_axis',(0.,0.,1.));
#12901=DIRECTION('ref_axis',(-1.,0.,0.));
#12902=DIRECTION('',(0.,0.,1.));
#12903=DIRECTION('center_axis',(0.,0.,1.));
#12904=DIRECTION('ref_axis',(-1.,0.,0.));
#12905=DIRECTION('',(0.,0.,-1.));
#12906=DIRECTION('center_axis',(0.,0.,1.));
#12907=DIRECTION('ref_axis',(-1.,0.,0.));
#12908=DIRECTION('center_axis',(-1.57009245868377E-16,-0.707106781186548,
-0.707106781186548));
#12909=DIRECTION('ref_axis',(0.,0.707106781186547,-0.707106781186547));
#12910=DIRECTION('center_axis',(0.,0.,1.));
#12911=DIRECTION('ref_axis',(-1.,0.,0.));
#12912=DIRECTION('center_axis',(-1.57009245868377E-16,-0.707106781186548,
-0.707106781186548));
#12913=DIRECTION('ref_axis',(0.,0.707106781186547,-0.707106781186547));
#12914=DIRECTION('center_axis',(0.,0.,1.));
#12915=DIRECTION('ref_axis',(-1.,0.,0.));
#12916=DIRECTION('center_axis',(0.,0.,-1.));
#12917=DIRECTION('ref_axis',(-1.,0.,0.));
#12918=DIRECTION('center_axis',(0.,0.,-1.));
#12919=DIRECTION('ref_axis',(-1.,0.,0.));
#12920=DIRECTION('',(0.,0.,-1.));
#12921=DIRECTION('center_axis',(0.,0.,1.));
#12922=DIRECTION('ref_axis',(-1.,0.,0.));
#12923=DIRECTION('',(0.,0.,1.));
#12924=DIRECTION('center_axis',(0.,0.,1.));
#12925=DIRECTION('ref_axis',(-1.,0.,0.));
#12926=DIRECTION('',(0.,0.,-1.));
#12927=DIRECTION('center_axis',(0.,0.,1.));
#12928=DIRECTION('ref_axis',(-1.,0.,0.));
#12929=DIRECTION('center_axis',(-1.57009245868377E-16,-0.707106781186548,
-0.707106781186548));
#12930=DIRECTION('ref_axis',(0.,0.707106781186547,-0.707106781186547));
#12931=DIRECTION('center_axis',(0.,0.,1.));
#12932=DIRECTION('ref_axis',(-1.,0.,0.));
#12933=DIRECTION('center_axis',(-1.57009245868377E-16,-0.707106781186548,
-0.707106781186548));
#12934=DIRECTION('ref_axis',(0.,0.707106781186547,-0.707106781186547));
#12935=DIRECTION('center_axis',(0.,0.,1.));
#12936=DIRECTION('ref_axis',(-1.,0.,0.));
#12937=DIRECTION('center_axis',(0.,0.,-1.));
#12938=DIRECTION('ref_axis',(-1.,0.,0.));
#12939=DIRECTION('center_axis',(0.,0.,-1.));
#12940=DIRECTION('ref_axis',(-1.,0.,0.));
#12941=DIRECTION('',(0.,0.,-1.));
#12942=DIRECTION('center_axis',(0.,0.,1.));
#12943=DIRECTION('ref_axis',(-1.,0.,0.));
#12944=DIRECTION('center_axis',(0.,0.,-1.));
#12945=DIRECTION('ref_axis',(-1.,0.,0.));
#12946=DIRECTION('center_axis',(0.,0.,-1.));
#12947=DIRECTION('ref_axis',(-1.,0.,0.));
#12948=DIRECTION('',(0.,0.,-1.));
#12949=DIRECTION('',(0.,0.,-1.));
#12950=DIRECTION('center_axis',(0.,0.,1.));
#12951=DIRECTION('ref_axis',(-1.,0.,0.));
#12952=DIRECTION('',(0.,0.,1.));
#12953=DIRECTION('center_axis',(-1.,2.22044604925031E-16,0.));
#12954=DIRECTION('ref_axis',(1.57009245868377E-16,0.707106781186544,0.707106781186551));
#12955=DIRECTION('',(1.,-2.22044604925031E-16,0.));
#12956=DIRECTION('center_axis',(-1.,2.22044604925031E-16,0.));
#12957=DIRECTION('ref_axis',(1.57009245868377E-16,0.707106781186544,0.707106781186551));
#12958=DIRECTION('center_axis',(1.,-2.22044604925031E-16,0.));
#12959=DIRECTION('ref_axis',(0.,0.,1.));
#12960=DIRECTION('',(1.,-2.22044604925031E-16,0.));
#12961=DIRECTION('center_axis',(-1.,2.22044604925031E-16,0.));
#12962=DIRECTION('ref_axis',(1.57009245868377E-16,0.707106781186544,0.707106781186551));
#12963=DIRECTION('',(1.,-2.22044604925031E-16,0.));
#12964=DIRECTION('center_axis',(-1.,2.22044604925031E-16,0.));
#12965=DIRECTION('ref_axis',(1.57009245868377E-16,0.707106781186544,0.707106781186551));
#12966=DIRECTION('',(1.,-2.22044604925031E-16,0.));
#12967=DIRECTION('center_axis',(-1.,2.22044604925031E-16,0.));
#12968=DIRECTION('ref_axis',(2.22044604925031E-16,1.,0.));
#12969=DIRECTION('center_axis',(-1.,2.22044604925031E-16,0.));
#12970=DIRECTION('ref_axis',(1.57009245868377E-16,0.707106781186544,0.707106781186551));
#12971=DIRECTION('',(1.,-2.22044604925031E-16,0.));
#12972=DIRECTION('center_axis',(-2.22044604925031E-16,-1.,0.));
#12973=DIRECTION('ref_axis',(0.,0.,1.));
#12974=DIRECTION('',(-1.,2.22044604925031E-16,0.));
#12975=DIRECTION('',(0.,0.,-1.));
#12976=DIRECTION('center_axis',(-2.22044604925031E-16,-1.,0.));
#12977=DIRECTION('ref_axis',(0.,0.,1.));
#12978=DIRECTION('',(-1.,2.22044604925031E-16,0.));
#12979=DIRECTION('center_axis',(-2.22044604925031E-16,-1.,0.));
#12980=DIRECTION('ref_axis',(0.,0.,1.));
#12981=DIRECTION('',(0.,0.,1.));
#12982=DIRECTION('',(-1.,2.22044604925031E-16,0.));
#12983=DIRECTION('center_axis',(-2.22044604925031E-16,-1.,0.));
#12984=DIRECTION('ref_axis',(0.,0.,1.));
#12985=DIRECTION('',(-1.,2.22044604925031E-16,0.));
#12986=DIRECTION('center_axis',(-1.,2.22044604925031E-16,0.));
#12987=DIRECTION('ref_axis',(-1.57009245868377E-16,-0.707106781186546,-0.707106781186549));
#12988=DIRECTION('',(1.,-2.22044604925031E-16,0.));
#12989=DIRECTION('center_axis',(-1.,2.22044604925031E-16,0.));
#12990=DIRECTION('ref_axis',(-1.57009245868377E-16,-0.707106781186546,-0.707106781186549));
#12991=DIRECTION('center_axis',(-1.,2.22044604925031E-16,0.));
#12992=DIRECTION('ref_axis',(-2.22044604925031E-16,-1.,0.));
#12993=DIRECTION('',(1.,-2.22044604925031E-16,0.));
#12994=DIRECTION('center_axis',(-1.,2.22044604925031E-16,0.));
#12995=DIRECTION('ref_axis',(-1.57009245868377E-16,-0.707106781186546,-0.707106781186549));
#12996=DIRECTION('',(1.,-2.22044604925031E-16,0.));
#12997=DIRECTION('center_axis',(-1.,2.22044604925031E-16,0.));
#12998=DIRECTION('ref_axis',(-1.57009245868377E-16,-0.707106781186546,-0.707106781186549));
#12999=DIRECTION('',(1.,-2.22044604925031E-16,0.));
#13000=DIRECTION('center_axis',(1.,-2.22044604925031E-16,0.));
#13001=DIRECTION('ref_axis',(0.,0.,-1.));
#13002=DIRECTION('center_axis',(-1.,2.22044604925031E-16,0.));
#13003=DIRECTION('ref_axis',(1.57009245868377E-16,0.707106781186547,-0.707106781186548));
#13004=DIRECTION('',(-1.,2.22044604925031E-16,0.));
#13005=DIRECTION('center_axis',(-1.,2.22044604925031E-16,0.));
#13006=DIRECTION('ref_axis',(0.,0.,-1.));
#13007=DIRECTION('',(1.,-2.22044604925031E-16,0.));
#13008=DIRECTION('center_axis',(-1.,2.22044604925031E-16,0.));
#13009=DIRECTION('ref_axis',(1.57009245868377E-16,0.707106781186547,-0.707106781186548));
#13010=DIRECTION('',(-1.,2.22044604925031E-16,0.));
#13011=DIRECTION('',(1.,-2.22044604925031E-16,0.));
#13012=DIRECTION('center_axis',(-1.,2.22044604925031E-16,0.));
#13013=DIRECTION('ref_axis',(1.57009245868377E-16,0.707106781186547,-0.707106781186548));
#13014=DIRECTION('',(1.,-2.22044604925031E-16,0.));
#13015=DIRECTION('center_axis',(1.,-2.22044604925031E-16,0.));
#13016=DIRECTION('ref_axis',(2.22044604925031E-16,1.,0.));
#13017=DIRECTION('',(-1.,2.22044604925031E-16,0.));
#13018=DIRECTION('center_axis',(-1.,2.22044604925031E-16,0.));
#13019=DIRECTION('ref_axis',(1.57009245868377E-16,0.707106781186547,-0.707106781186548));
#13020=DIRECTION('',(1.,-2.22044604925031E-16,0.));
#13021=DIRECTION('',(-1.,2.22044604925031E-16,0.));
#13022=DIRECTION('center_axis',(-1.,2.22044604925031E-16,0.));
#13023=DIRECTION('ref_axis',(1.57009245868377E-16,0.707106781186547,-0.707106781186548));
#13024=DIRECTION('',(-1.,2.22044604925031E-16,0.));
#13025=DIRECTION('',(1.,-2.22044604925031E-16,0.));
#13026=DIRECTION('center_axis',(2.22044604925031E-16,1.,0.));
#13027=DIRECTION('ref_axis',(0.,0.,-1.));
#13028=DIRECTION('',(0.,0.,-1.));
#13029=DIRECTION('',(-1.,2.22044604925031E-16,0.));
#13030=DIRECTION('center_axis',(2.22044604925031E-16,1.,0.));
#13031=DIRECTION('ref_axis',(0.,0.,-1.));
#13032=DIRECTION('',(-1.,2.22044604925031E-16,0.));
#13033=DIRECTION('center_axis',(2.22044604925031E-16,1.,0.));
#13034=DIRECTION('ref_axis',(0.,0.,-1.));
#13035=DIRECTION('',(-1.,2.22044604925031E-16,0.));
#13036=DIRECTION('',(0.,0.,1.));
#13037=DIRECTION('center_axis',(2.22044604925031E-16,1.,0.));
#13038=DIRECTION('ref_axis',(0.,0.,-1.));
#13039=DIRECTION('',(-1.,2.22044604925031E-16,0.));
#13040=DIRECTION('center_axis',(2.22044604925031E-16,1.,0.));
#13041=DIRECTION('ref_axis',(0.,0.,-1.));
#13042=DIRECTION('',(-1.,2.22044604925031E-16,0.));
#13043=DIRECTION('center_axis',(-1.,2.22044604925031E-16,0.));
#13044=DIRECTION('ref_axis',(-2.05142465794791E-16,-0.923879532511288,0.382683432365088));
#13045=DIRECTION('',(-1.,2.22044604925031E-16,0.));
#13046=DIRECTION('center_axis',(1.,-2.22044604925031E-16,0.));
#13047=DIRECTION('ref_axis',(-1.57009245868377E-16,-0.707106781186548,-0.707106781186548));
#13048=DIRECTION('',(1.,-2.22044604925031E-16,0.));
#13049=DIRECTION('center_axis',(-1.,2.22044604925031E-16,0.));
#13050=DIRECTION('ref_axis',(-2.05142465794791E-16,-0.923879532511288,0.382683432365088));
#13051=DIRECTION('',(-1.,2.22044604925031E-16,0.));
#13052=DIRECTION('',(1.,-2.22044604925031E-16,0.));
#13053=DIRECTION('center_axis',(-1.,2.22044604925031E-16,0.));
#13054=DIRECTION('ref_axis',(-2.05142465794791E-16,-0.923879532511288,0.382683432365088));
#13055=DIRECTION('',(1.,-2.22044604925031E-16,0.));
#13056=DIRECTION('center_axis',(-1.,5.04650032828059E-14,0.));
#13057=DIRECTION('ref_axis',(0.,0.,1.));
#13058=DIRECTION('',(-1.,2.22044604925031E-16,0.));
#13059=DIRECTION('center_axis',(-1.,2.22044604925031E-16,0.));
#13060=DIRECTION('ref_axis',(-2.05142465794791E-16,-0.923879532511288,0.382683432365088));
#13061=DIRECTION('',(1.,-2.22044604925031E-16,0.));
#13062=DIRECTION('',(-1.,2.22044604925031E-16,0.));
#13063=DIRECTION('center_axis',(-1.,2.22044604925031E-16,0.));
#13064=DIRECTION('ref_axis',(-1.57009245868377E-16,-0.707106781186548,0.707106781186548));
#13065=DIRECTION('center_axis',(1.,-2.22044604925031E-16,0.));
#13066=DIRECTION('ref_axis',(-2.22044604925031E-16,-1.,0.));
#13067=DIRECTION('',(1.,-2.22044604925031E-16,0.));
#13068=DIRECTION('center_axis',(-1.,2.22044604925031E-16,0.));
#13069=DIRECTION('ref_axis',(-1.57009245868377E-16,-0.707106781186548,0.707106781186548));
#13070=DIRECTION('',(1.,-2.22044604925031E-16,0.));
#13071=DIRECTION('center_axis',(-1.,2.22044604925031E-16,0.));
#13072=DIRECTION('ref_axis',(-1.57009245868377E-16,-0.707106781186548,0.707106781186548));
#13073=DIRECTION('',(1.,-2.22044604925031E-16,0.));
#13074=DIRECTION('center_axis',(-1.,2.22044604925031E-16,0.));
#13075=DIRECTION('ref_axis',(0.,0.,1.));
#13076=DIRECTION('center_axis',(-1.,2.22044604925031E-16,0.));
#13077=DIRECTION('ref_axis',(-1.57009245868377E-16,-0.707106781186548,0.707106781186548));
#13078=DIRECTION('',(1.,-2.22044604925031E-16,0.));
#13079=DIRECTION('center_axis',(-1.,2.22044604925031E-16,0.));
#13080=DIRECTION('ref_axis',(-1.57009245868377E-16,-0.707106781186548,0.707106781186548));
#13081=DIRECTION('',(1.,-2.22044604925031E-16,0.));
#13082=DIRECTION('center_axis',(1.57009245868377E-16,0.707106781186548,
0.707106781186548));
#13083=DIRECTION('ref_axis',(1.57009245868377E-16,0.707106781186548,-0.707106781186548));
#13084=DIRECTION('',(1.,-2.22044604925031E-16,0.));
#13085=DIRECTION('',(1.57009245868377E-16,0.707106781186548,-0.707106781186548));
#13086=DIRECTION('center_axis',(1.57009245868377E-16,0.707106781186548,
0.707106781186548));
#13087=DIRECTION('ref_axis',(1.57009245868377E-16,0.707106781186548,-0.707106781186548));
#13088=DIRECTION('',(1.,-2.22044604925031E-16,0.));
#13089=DIRECTION('center_axis',(1.57009245868377E-16,0.707106781186548,
0.707106781186548));
#13090=DIRECTION('ref_axis',(1.57009245868377E-16,0.707106781186548,-0.707106781186548));
#13091=DIRECTION('',(-1.57009245868377E-16,-0.707106781186548,0.707106781186548));
#13092=DIRECTION('',(1.,-2.22044604925031E-16,0.));
#13093=DIRECTION('center_axis',(1.57009245868377E-16,0.707106781186548,
0.707106781186548));
#13094=DIRECTION('ref_axis',(1.57009245868377E-16,0.707106781186548,-0.707106781186548));
#13095=DIRECTION('',(1.,-2.22044604925031E-16,0.));
#13096=DIRECTION('center_axis',(0.,0.,-1.));
#13097=DIRECTION('ref_axis',(-2.22044604925031E-16,-1.,0.));
#13098=DIRECTION('',(-1.,2.22044604925031E-16,0.));
#13099=DIRECTION('',(2.22044604925031E-16,1.,0.));
#13100=DIRECTION('center_axis',(0.,0.,-1.));
#13101=DIRECTION('ref_axis',(-2.22044604925031E-16,-1.,0.));
#13102=DIRECTION('',(-2.22044604925031E-16,-1.,0.));
#13103=DIRECTION('',(-1.,2.22044604925031E-16,0.));
#13104=DIRECTION('center_axis',(0.,0.,-1.));
#13105=DIRECTION('ref_axis',(-2.22044604925031E-16,-1.,0.));
#13106=DIRECTION('',(-1.,2.22044604925031E-16,0.));
#13107=DIRECTION('center_axis',(0.,0.,-1.));
#13108=DIRECTION('ref_axis',(-2.22044604925031E-16,-1.,0.));
#13109=DIRECTION('',(-1.,2.22044604925031E-16,0.));
#13110=DIRECTION('center_axis',(-1.,2.22044604925031E-16,0.));
#13111=DIRECTION('ref_axis',(2.05142465794791E-16,0.923879532511283,-0.382683432365098));
#13112=DIRECTION('center_axis',(-1.,2.22044604925031E-16,0.));
#13113=DIRECTION('ref_axis',(0.,0.,-1.));
#13114=DIRECTION('center_axis',(-1.,2.22044604925031E-16,0.));
#13115=DIRECTION('ref_axis',(2.05142465794791E-16,0.923879532511283,-0.382683432365098));
#13116=DIRECTION('center_axis',(-1.,2.22044604925031E-16,0.));
#13117=DIRECTION('ref_axis',(2.05142465794791E-16,0.923879532511283,-0.382683432365098));
#13118=DIRECTION('center_axis',(1.,-7.1276318180935E-14,7.105427357601E-14));
#13119=DIRECTION('ref_axis',(1.57009245868377E-16,0.707106781186548,0.707106781186548));
#13120=DIRECTION('center_axis',(-1.,2.22044604925031E-16,0.));
#13121=DIRECTION('ref_axis',(2.05142465794791E-16,0.923879532511283,-0.382683432365098));
#13122=DIRECTION('center_axis',(0.,0.,1.));
#13123=DIRECTION('ref_axis',(2.22044604925031E-16,1.,0.));
#13124=DIRECTION('',(-1.,2.22044604925031E-16,0.));
#13125=DIRECTION('',(-1.,2.22044604925031E-16,0.));
#13126=DIRECTION('',(-1.,2.22044604925031E-16,0.));
#13127=DIRECTION('',(-1.,2.22044604925031E-16,0.));
#13128=DIRECTION('',(-1.,2.22044604925031E-16,0.));
#13129=DIRECTION('',(2.22044604925031E-16,1.,0.));
#13130=DIRECTION('',(1.,-2.22044604925031E-16,0.));
#13131=DIRECTION('',(-2.22044604925031E-16,-1.,0.));
#13132=DIRECTION('center_axis',(1.,-2.22044604925031E-16,0.));
#13133=DIRECTION('ref_axis',(1.57009245868376E-16,0.707106781186541,0.707106781186554));
#13134=DIRECTION('',(1.,-2.22044604925031E-16,0.));
#13135=DIRECTION('center_axis',(1.,-2.22044604925031E-16,0.));
#13136=DIRECTION('ref_axis',(1.57009245868376E-16,0.707106781186541,0.707106781186554));
#13137=DIRECTION('',(1.,-2.22044604925031E-16,0.));
#13138=DIRECTION('center_axis',(-1.,2.22044604925031E-16,0.));
#13139=DIRECTION('ref_axis',(2.22044604925031E-16,1.,0.));
#13140=DIRECTION('center_axis',(1.,-2.22044604925031E-16,0.));
#13141=DIRECTION('ref_axis',(1.57009245868376E-16,0.707106781186541,0.707106781186554));
#13142=DIRECTION('',(1.,-2.22044604925031E-16,0.));
#13143=DIRECTION('center_axis',(1.,-2.22044604925031E-16,0.));
#13144=DIRECTION('ref_axis',(1.57009245868376E-16,0.707106781186541,0.707106781186554));
#13145=DIRECTION('',(1.,-2.22044604925031E-16,0.));
#13146=DIRECTION('center_axis',(1.,-2.22044604925031E-16,0.));
#13147=DIRECTION('ref_axis',(1.57009245868376E-16,0.707106781186541,0.707106781186554));
#13148=DIRECTION('',(1.,-2.22044604925031E-16,0.));
#13149=DIRECTION('center_axis',(-2.22044604925031E-16,-1.,0.));
#13150=DIRECTION('ref_axis',(0.,0.,1.));
#13151=DIRECTION('',(-1.,2.22044604925031E-16,0.));
#13152=DIRECTION('',(0.,0.,-1.));
#13153=DIRECTION('center_axis',(-2.22044604925031E-16,-1.,0.));
#13154=DIRECTION('ref_axis',(0.,0.,1.));
#13155=DIRECTION('',(-1.,2.22044604925031E-16,0.));
#13156=DIRECTION('center_axis',(-2.22044604925031E-16,-1.,0.));
#13157=DIRECTION('ref_axis',(0.,0.,1.));
#13158=DIRECTION('',(-1.,2.22044604925031E-16,0.));
#13159=DIRECTION('center_axis',(-2.22044604925031E-16,-1.,0.));
#13160=DIRECTION('ref_axis',(0.,0.,1.));
#13161=DIRECTION('',(-1.,2.22044604925031E-16,0.));
#13162=DIRECTION('center_axis',(-1.,2.22044604925031E-16,0.));
#13163=DIRECTION('ref_axis',(-1.57009245868376E-16,-0.707106781186541,-0.707106781186554));
#13164=DIRECTION('center_axis',(-1.,2.22044604925031E-16,0.));
#13165=DIRECTION('ref_axis',(-1.57009245868376E-16,-0.707106781186541,-0.707106781186554));
#13166=DIRECTION('center_axis',(1.,-2.22044604925031E-16,0.));
#13167=DIRECTION('ref_axis',(0.,0.,-1.));
#13168=DIRECTION('center_axis',(-1.,2.22044604925031E-16,0.));
#13169=DIRECTION('ref_axis',(-1.57009245868376E-16,-0.707106781186541,-0.707106781186554));
#13170=DIRECTION('center_axis',(-1.,2.22044604925031E-16,0.));
#13171=DIRECTION('ref_axis',(-1.57009245868376E-16,-0.707106781186541,-0.707106781186554));
#13172=DIRECTION('center_axis',(0.,0.,-1.));
#13173=DIRECTION('ref_axis',(-2.22044604925031E-16,-1.,0.));
#13174=DIRECTION('',(1.,-2.22044604925031E-16,0.));
#13175=DIRECTION('',(-2.22044604925031E-16,-1.,0.));
#13176=DIRECTION('',(2.22044604925031E-16,1.,0.));
#13177=DIRECTION('center_axis',(0.,0.,1.));
#13178=DIRECTION('ref_axis',(2.22044604925031E-16,1.,0.));
#13179=DIRECTION('',(1.,-2.22044604925031E-16,0.));
#13180=DIRECTION('',(-2.22044604925031E-16,-1.,0.));
#13181=DIRECTION('',(-1.,2.22044604925031E-16,0.));
#13182=DIRECTION('',(2.22044604925031E-16,1.,0.));
#13183=DIRECTION('center_axis',(-0.538877990790891,0.827465426020391,0.15783370927044));
#13184=DIRECTION('ref_axis',(0.79410448776086,0.561516668266297,-0.232587819494442));
#13185=DIRECTION('center_axis',(1.57009245868378E-16,0.707106781186552,
-0.707106781186543));
#13186=DIRECTION('ref_axis',(1.,-2.22044604925031E-16,0.));
#13187=DIRECTION('center_axis',(2.22044604925031E-16,1.,0.));
#13188=DIRECTION('ref_axis',(0.,0.,-1.));
#13189=DIRECTION('center_axis',(0.53887799079092,0.827465426020364,0.157833709270477));
#13190=DIRECTION('ref_axis',(-0.794104487760813,0.561516668266353,-0.232587819494468));
#13191=DIRECTION('center_axis',(2.22044604925031E-16,1.,0.));
#13192=DIRECTION('ref_axis',(-1.,2.22044604925031E-16,0.));
#13193=DIRECTION('center_axis',(1.57009245868377E-16,0.707106781186548,
-0.707106781186548));
#13194=DIRECTION('ref_axis',(1.57009245868378E-16,0.707106781186548,0.707106781186548));
#13195=DIRECTION('center_axis',(-1.,2.22044604925031E-16,0.));
#13196=DIRECTION('ref_axis',(0.,0.,-1.));
#13197=DIRECTION('center_axis',(2.22044604925031E-16,1.,0.));
#13198=DIRECTION('ref_axis',(1.,-2.22044604925031E-16,0.));
#13199=DIRECTION('center_axis',(1.,-2.22044604925031E-16,0.));
#13200=DIRECTION('ref_axis',(-1.57009245868378E-16,-0.707106781186549,0.707106781186546));
#13201=DIRECTION('center_axis',(0.,0.,-1.));
#13202=DIRECTION('ref_axis',(2.22044604925031E-16,1.,0.));
#13203=DIRECTION('center_axis',(-2.22044604925031E-16,-1.,0.));
#13204=DIRECTION('ref_axis',(0.707106781186554,-1.57009245868379E-16,-0.707106781186541));
#13205=DIRECTION('',(-2.22044604925031E-16,-1.,0.));
#13206=DIRECTION('center_axis',(-1.,2.22044604925031E-16,3.5527136788003E-14));
#13207=DIRECTION('ref_axis',(-2.84217094304039E-14,0.,-1.));
#13208=DIRECTION('center_axis',(1.,-2.22044604925031E-16,0.));
#13209=DIRECTION('ref_axis',(-2.05142465794791E-16,-0.923879532511286,0.382683432365093));
#13210=DIRECTION('center_axis',(-2.49644700930708E-14,0.707106781186543,
-0.707106781186552));
#13211=DIRECTION('ref_axis',(1.57009245868378E-16,0.707106781186552,0.707106781186543));
#13212=DIRECTION('center_axis',(2.22044604925031E-16,1.,0.));
#13213=DIRECTION('ref_axis',(1.,-2.22044604925031E-16,0.));
#13214=DIRECTION('center_axis',(1.,-2.22044604925031E-16,0.));
#13215=DIRECTION('ref_axis',(0.,0.,1.));
#13216=DIRECTION('center_axis',(0.,0.,-1.));
#13217=DIRECTION('ref_axis',(-1.,2.22044604925031E-16,0.));
#13218=DIRECTION('center_axis',(-1.,2.22044604925031E-16,0.));
#13219=DIRECTION('ref_axis',(-1.57009245868378E-16,-0.707106781186549,0.707106781186546));
#13220=DIRECTION('center_axis',(2.22044604925031E-16,1.,0.));
#13221=DIRECTION('ref_axis',(0.,0.,-1.));
#13222=DIRECTION('center_axis',(1.,-2.22044604925031E-16,0.));
#13223=DIRECTION('ref_axis',(0.,0.,1.));
#13224=DIRECTION('center_axis',(-1.,2.22044604925031E-16,0.));
#13225=DIRECTION('ref_axis',(-2.05142465794794E-16,-0.9238795325113,0.382683432365059));
#13226=DIRECTION('center_axis',(2.22044604925031E-16,1.,0.));
#13227=DIRECTION('ref_axis',(0.,0.,-1.));
#13228=DIRECTION('center_axis',(1.57009245868376E-16,0.707106781186539,
-0.707106781186556));
#13229=DIRECTION('ref_axis',(-1.,2.22044604925031E-16,0.));
#13230=DIRECTION('center_axis',(-1.57009245868377E-16,-0.707106781186548,
0.707106781186548));
#13231=DIRECTION('ref_axis',(-0.707106781186551,0.499999999999995,0.500000000000001));
#13232=DIRECTION('',(-1.57009245868377E-16,-0.707106781186548,0.707106781186548));
#13233=DIRECTION('center_axis',(-0.408248290463856,0.816496580927733,0.408248290463856));
#13234=DIRECTION('ref_axis',(0.577350269189638,0.577350269189616,-0.577350269189623));
#13235=DIRECTION('center_axis',(0.,0.,-1.));
#13236=DIRECTION('ref_axis',(1.,-2.22044604925031E-16,0.));
#13237=DIRECTION('center_axis',(2.22044604925031E-16,1.,0.));
#13238=DIRECTION('ref_axis',(0.,0.,-1.));
#13239=DIRECTION('center_axis',(0.,0.,-1.));
#13240=DIRECTION('ref_axis',(0.707106781186554,0.707106781186541,0.));
#13241=DIRECTION('',(0.,0.,-1.));
#13242=DIRECTION('center_axis',(-0.408248290463858,-0.408248290463858,-0.816496580927731));
#13243=DIRECTION('ref_axis',(0.577350269189631,0.577350269189631,-0.577350269189616));
#13244=DIRECTION('center_axis',(0.,0.,-1.));
#13245=DIRECTION('ref_axis',(1.,-2.22044604925031E-16,0.));
#13246=DIRECTION('center_axis',(2.22044604925031E-16,1.,0.));
#13247=DIRECTION('ref_axis',(0.,0.,-1.));
#13248=DIRECTION('center_axis',(1.,-2.22044604925031E-16,0.));
#13249=DIRECTION('ref_axis',(2.22044604925031E-16,1.,0.));
#13250=DIRECTION('center_axis',(2.22044604925031E-16,1.,0.));
#13251=DIRECTION('ref_axis',(0.707106781186554,-1.57009245868379E-16,-0.707106781186541));
#13252=DIRECTION('',(-2.22044604925031E-16,-1.,0.));
#13253=DIRECTION('center_axis',(0.408248290463856,0.816496580927733,0.408248290463856));
#13254=DIRECTION('ref_axis',(-0.577350269189638,0.577350269189616,-0.577350269189623));
#13255=DIRECTION('center_axis',(2.22044604925031E-16,1.,0.));
#13256=DIRECTION('ref_axis',(-1.,2.22044604925031E-16,0.));
#13257=DIRECTION('center_axis',(0.,0.,-1.));
#13258=DIRECTION('ref_axis',(2.22044604925031E-16,1.,0.));
#13259=DIRECTION('center_axis',(0.408248290463854,-0.408248290463854,-0.816496580927736));
#13260=DIRECTION('ref_axis',(-0.577350269189616,0.577350269189645,-0.577350269189616));
#13261=DIRECTION('center_axis',(-1.,2.22044604925031E-16,0.));
#13262=DIRECTION('ref_axis',(0.,0.,-1.));
#13263=DIRECTION('center_axis',(2.22044604925031E-16,1.,1.77635683940026E-14));
#13264=DIRECTION('ref_axis',(-1.,2.22044604925031E-16,0.));
#13265=DIRECTION('center_axis',(0.,0.,-1.));
#13266=DIRECTION('ref_axis',(2.22044604925031E-16,1.,0.));
#13267=DIRECTION('center_axis',(-2.22044604925031E-16,-1.,0.));
#13268=DIRECTION('ref_axis',(-0.707106781186554,1.57009245868379E-16,-0.707106781186541));
#13269=DIRECTION('',(2.22044604925031E-16,1.,0.));
#13270=DIRECTION('center_axis',(0.408248290463856,0.816496580927733,-0.408248290463856));
#13271=DIRECTION('ref_axis',(0.577350269189638,-0.577350269189616,-0.577350269189623));
#13272=DIRECTION('center_axis',(-2.22044604925031E-16,-1.,0.));
#13273=DIRECTION('ref_axis',(1.,-2.22044604925031E-16,0.));
#13274=DIRECTION('center_axis',(-2.22044604925028E-15,4.93038065763125E-31,
-1.));
#13275=DIRECTION('ref_axis',(-2.22044604925031E-16,-1.,0.));
#13276=DIRECTION('center_axis',(-2.22044604925031E-16,-1.,0.));
#13277=DIRECTION('ref_axis',(0.707106781186553,-1.57009245868379E-16,-0.707106781186542));
#13278=DIRECTION('',(-2.22044604925031E-16,-1.,0.));
#13279=DIRECTION('center_axis',(-0.408248290463875,0.816496580927721,-0.408248290463861));
#13280=DIRECTION('ref_axis',(0.577350269189635,0.577350269189635,0.577350269189607));
#13281=DIRECTION('center_axis',(2.22044604925031E-16,1.,0.));
#13282=DIRECTION('ref_axis',(1.,-2.22044604925031E-16,0.));
#13283=DIRECTION('center_axis',(0.,0.,1.));
#13284=DIRECTION('ref_axis',(2.22044604925031E-16,1.,0.));
#13285=DIRECTION('center_axis',(1.,-2.22044604925031E-16,0.));
#13286=DIRECTION('ref_axis',(0.,0.,1.));
#13287=DIRECTION('center_axis',(0.,0.,1.));
#13288=DIRECTION('ref_axis',(0.707106781186548,0.707106781186547,0.));
#13289=DIRECTION('',(0.,0.,-1.));
#13290=DIRECTION('',(0.,0.,1.));
#13291=DIRECTION('center_axis',(-0.408248290463856,0.816496580927733,-0.408248290463856));
#13292=DIRECTION('ref_axis',(-0.577350269189638,-0.577350269189616,-0.577350269189623));
#13293=DIRECTION('center_axis',(-4.93038065763134E-31,-2.22044604925032E-15,
-1.));
#13294=DIRECTION('ref_axis',(-1.,2.22044604925031E-16,0.));
#13295=DIRECTION('center_axis',(-2.22044604925031E-16,-1.,0.));
#13296=DIRECTION('ref_axis',(0.,0.,-1.));
#13297=DIRECTION('center_axis',(-0.408248290463854,0.408248290463854,-0.816496580927736));
#13298=DIRECTION('ref_axis',(-0.577350269189616,0.577350269189645,0.577350269189616));
#13299=DIRECTION('center_axis',(-1.,2.22044604925031E-16,0.));
#13300=DIRECTION('ref_axis',(2.22044604925031E-16,1.,0.));
#13301=DIRECTION('center_axis',(0.,0.,1.));
#13302=DIRECTION('ref_axis',(-1.,2.22044604925031E-16,0.));
#13303=DIRECTION('center_axis',(-1.75415237890772E-14,1.,0.));
#13304=DIRECTION('ref_axis',(0.,0.,1.));
#13305=DIRECTION('center_axis',(0.,0.,1.));
#13306=DIRECTION('ref_axis',(-0.707106781186547,0.707106781186548,0.));
#13307=DIRECTION('',(0.,0.,-1.));
#13308=DIRECTION('',(0.,0.,1.));
#13309=DIRECTION('center_axis',(-1.,2.22044604925031E-16,0.));
#13310=DIRECTION('ref_axis',(0.,0.,-1.));
#13311=DIRECTION('center_axis',(0.,0.,-1.));
#13312=DIRECTION('ref_axis',(1.,-2.22044604925031E-16,0.));
#13313=DIRECTION('center_axis',(1.,-2.22044604925031E-16,0.));
#13314=DIRECTION('ref_axis',(1.57009245868377E-16,0.707106781186546,0.707106781186549));
#13315=DIRECTION('center_axis',(-2.22044604925031E-16,-1.,0.));
#13316=DIRECTION('ref_axis',(0.,0.,-1.));
#13317=DIRECTION('center_axis',(0.,0.,1.));
#13318=DIRECTION('ref_axis',(0.707106781186554,-0.707106781186541,0.));
#13319=DIRECTION('',(0.,0.,1.));
#13320=DIRECTION('center_axis',(0.408248290463854,-0.408248290463854,-0.816496580927736));
#13321=DIRECTION('ref_axis',(0.577350269189616,-0.577350269189645,0.577350269189616));
#13322=DIRECTION('center_axis',(1.,-2.22044604925031E-16,0.));
#13323=DIRECTION('ref_axis',(-2.22044604925031E-16,-1.,0.));
#13324=DIRECTION('center_axis',(0.,0.,1.));
#13325=DIRECTION('ref_axis',(1.,-2.22044604925031E-16,0.));
#13326=DIRECTION('center_axis',(1.75415237890772E-14,-1.,0.));
#13327=DIRECTION('ref_axis',(0.,0.,1.));
#13328=DIRECTION('center_axis',(1.,-2.22044604925031E-16,0.));
#13329=DIRECTION('ref_axis',(0.,0.,1.));
#13330=DIRECTION('center_axis',(-2.22044604925031E-16,-1.,0.));
#13331=DIRECTION('ref_axis',(-1.,2.22044604925031E-16,0.));
#13332=DIRECTION('center_axis',(-1.,2.22044604925031E-16,0.));
#13333=DIRECTION('ref_axis',(1.57009245868378E-16,0.707106781186549,0.707106781186546));
#13334=DIRECTION('center_axis',(0.,0.,-1.));
#13335=DIRECTION('ref_axis',(-2.22044604925031E-16,-1.,0.));
#13336=DIRECTION('center_axis',(-0.408248290463875,0.816496580927721,0.408248290463861));
#13337=DIRECTION('ref_axis',(-0.577350269189635,-0.577350269189635,0.577350269189607));
#13338=DIRECTION('center_axis',(-2.22044604925031E-16,-1.,0.));
#13339=DIRECTION('ref_axis',(-1.,2.22044604925031E-16,0.));
#13340=DIRECTION('center_axis',(0.,0.,1.));
#13341=DIRECTION('ref_axis',(-2.22044604925031E-16,-1.,0.));
#13342=DIRECTION('center_axis',(-1.,2.22044604925031E-16,0.));
#13343=DIRECTION('ref_axis',(0.,0.,1.));
#13344=DIRECTION('center_axis',(-0.408248290463854,0.408248290463854,-0.816496580927736));
#13345=DIRECTION('ref_axis',(0.577350269189616,-0.577350269189645,-0.577350269189616));
#13346=DIRECTION('center_axis',(-2.22044604925031E-16,-1.,1.77635683940026E-14));
#13347=DIRECTION('ref_axis',(1.,-2.22044604925031E-16,0.));
#13348=DIRECTION('center_axis',(0.,0.,-1.));
#13349=DIRECTION('ref_axis',(-2.22044604925031E-16,-1.,0.));
#13350=DIRECTION('center_axis',(-2.22044604925031E-16,-1.,0.));
#13351=DIRECTION('ref_axis',(0.707106781186554,-1.57009245868379E-16,-0.707106781186541));
#13352=DIRECTION('',(-2.22044604925031E-16,-1.,0.));
#13353=DIRECTION('center_axis',(0.408248290463865,0.816496580927731,-0.408248290463851));
#13354=DIRECTION('ref_axis',(0.577350269189626,-0.577350269189626,-0.577350269189626));
#13355=DIRECTION('center_axis',(0.,0.,-1.));
#13356=DIRECTION('ref_axis',(-2.22044604925031E-16,-1.,0.));
#13357=DIRECTION('center_axis',(1.,-2.22044604925031E-16,0.));
#13358=DIRECTION('ref_axis',(0.,0.,-1.));
#13359=DIRECTION('center_axis',(-2.22044604925031E-16,-1.,1.77635683940026E-14));
#13360=DIRECTION('ref_axis',(1.,-2.22044604925031E-16,0.));
#13361=DIRECTION('center_axis',(0.408248290463854,0.408248290463854,-0.816496580927736));
#13362=DIRECTION('ref_axis',(-0.577350269189616,-0.577350269189645,-0.577350269189616));
#13363=DIRECTION('center_axis',(0.,0.,-1.));
#13364=DIRECTION('ref_axis',(-1.,2.22044604925031E-16,0.));
#13365=DIRECTION('center_axis',(-2.22044604925031E-16,-1.,0.));
#13366=DIRECTION('ref_axis',(0.,0.,-1.));
#13367=DIRECTION('center_axis',(0.408248290463858,0.408248290463858,-0.816496580927731));
#13368=DIRECTION('ref_axis',(-0.577350269189631,-0.577350269189631,-0.577350269189616));
#13369=DIRECTION('center_axis',(0.,0.,-1.));
#13370=DIRECTION('ref_axis',(-1.,2.22044604925031E-16,0.));
#13371=DIRECTION('center_axis',(-2.22044604925031E-16,-1.,0.));
#13372=DIRECTION('ref_axis',(0.,0.,-1.));
#13373=DIRECTION('center_axis',(-1.,2.22044604925031E-16,0.));
#13374=DIRECTION('ref_axis',(-2.22044604925031E-16,-1.,0.));
#13375=DIRECTION('center_axis',(-1.,2.22044604925031E-16,0.));
#13376=DIRECTION('ref_axis',(0.,0.,-1.));
#13377=DIRECTION('center_axis',(0.,0.,-1.));
#13378=DIRECTION('ref_axis',(1.,-2.22044604925031E-16,0.));
#13379=DIRECTION('center_axis',(1.,-2.22044604925031E-16,0.));
#13380=DIRECTION('ref_axis',(1.57009245868377E-16,0.707106781186548,0.707106781186548));
#13381=DIRECTION('center_axis',(-2.22044604925031E-16,-1.,0.));
#13382=DIRECTION('ref_axis',(0.,0.,-1.));
#13383=DIRECTION('center_axis',(0.,0.,1.));
#13384=DIRECTION('ref_axis',(0.707106781186547,-0.707106781186548,0.));
#13385=DIRECTION('',(0.,0.,1.));
#13386=DIRECTION('center_axis',(2.22044604925031E-16,1.,0.));
#13387=DIRECTION('ref_axis',(0.707106781186554,-1.57009245868379E-16,-0.707106781186541));
#13388=DIRECTION('',(-2.22044604925031E-16,-1.,0.));
#13389=DIRECTION('center_axis',(1.,-2.22044604925031E-16,0.));
#13390=DIRECTION('ref_axis',(0.,0.,1.));
#13391=DIRECTION('center_axis',(-2.22044604925031E-16,-1.,0.));
#13392=DIRECTION('ref_axis',(-1.,2.22044604925031E-16,0.));
#13393=DIRECTION('center_axis',(-1.,2.22044604925031E-16,0.));
#13394=DIRECTION('ref_axis',(1.57009245868377E-16,0.707106781186548,0.707106781186548));
#13395=DIRECTION('center_axis',(0.,0.,-1.));
#13396=DIRECTION('ref_axis',(-2.22044604925031E-16,-1.,0.));
#13397=DIRECTION('center_axis',(-2.22044604925031E-16,-1.,0.));
#13398=DIRECTION('ref_axis',(-0.707106781186554,1.57009245868379E-16,-0.707106781186541));
#13399=DIRECTION('',(2.22044604925031E-16,1.,0.));
#13400=DIRECTION('center_axis',(0.,0.,-1.));
#13401=DIRECTION('ref_axis',(-0.707106781186548,-0.707106781186547,0.));
#13402=DIRECTION('',(0.,0.,-1.));
#13403=DIRECTION('center_axis',(1.,-2.22044604925031E-16,0.));
#13404=DIRECTION('ref_axis',(-1.57009245868376E-16,-0.707106781186541,-0.707106781186554));
#13405=DIRECTION('',(-1.,2.22044604925031E-16,0.));
#13406=DIRECTION('center_axis',(0.,0.,1.));
#13407=DIRECTION('ref_axis',(-0.707106781186548,-0.707106781186547,0.));
#13408=DIRECTION('',(0.,0.,-1.));
#13409=DIRECTION('',(0.,0.,1.));
#13410=DIRECTION('center_axis',(2.22044604925031E-16,1.,0.));
#13411=DIRECTION('ref_axis',(-0.707106781186554,1.57009245868379E-16,-0.707106781186541));
#13412=DIRECTION('',(2.22044604925031E-16,1.,0.));
#13413=DIRECTION('center_axis',(-1.,2.22044604925031E-16,0.));
#13414=DIRECTION('ref_axis',(-1.57009245868376E-16,-0.707106781186541,-0.707106781186554));
#13415=DIRECTION('',(-1.,2.22044604925031E-16,0.));
#13416=DIRECTION('center_axis',(0.,0.,1.));
#13417=DIRECTION('ref_axis',(0.707106781186547,-0.707106781186548,0.));
#13418=DIRECTION('',(0.,0.,-1.));
#13419=DIRECTION('',(0.,0.,1.));
#13420=DIRECTION('center_axis',(1.,-2.22044604925031E-16,0.));
#13421=DIRECTION('ref_axis',(-1.57009245868376E-16,-0.707106781186541,0.707106781186554));
#13422=DIRECTION('',(-1.,2.22044604925031E-16,0.));
#13423=DIRECTION('',(1.,-2.22044604925031E-16,0.));
#13424=DIRECTION('center_axis',(-2.22044604925031E-16,-1.,0.));
#13425=DIRECTION('ref_axis',(-0.707106781186554,1.57009245868379E-16,0.707106781186541));
#13426=DIRECTION('',(2.22044604925031E-16,1.,0.));
#13427=DIRECTION('',(-2.22044604925031E-16,-1.,0.));
#13428=DIRECTION('center_axis',(0.,0.,-1.));
#13429=DIRECTION('ref_axis',(-0.707106781186554,-0.707106781186541,0.));
#13430=DIRECTION('',(0.,0.,-1.));
#13431=DIRECTION('center_axis',(2.22044604925031E-16,1.,0.));
#13432=DIRECTION('ref_axis',(0.707106781186554,-1.57009245868379E-16,0.707106781186541));
#13433=DIRECTION('',(-2.22044604925031E-16,-1.,0.));
#13434=DIRECTION('',(2.22044604925031E-16,1.,0.));
#13435=DIRECTION('center_axis',(-1.,2.22044604925031E-16,0.));
#13436=DIRECTION('ref_axis',(1.57009245868376E-16,0.707106781186541,0.707106781186554));
#13437=DIRECTION('',(1.,-2.22044604925031E-16,0.));
#13438=DIRECTION('',(-1.,2.22044604925031E-16,0.));
#13439=DIRECTION('center_axis',(2.22044604925031E-16,1.,0.));
#13440=DIRECTION('ref_axis',(-0.707106781186553,1.57009245868379E-16,-0.707106781186542));
#13441=DIRECTION('',(2.22044604925031E-16,1.,0.));
#13442=DIRECTION('center_axis',(-1.,2.22044604925031E-16,0.));
#13443=DIRECTION('ref_axis',(-1.57009245868377E-16,-0.707106781186546,-0.707106781186549));
#13444=DIRECTION('',(-1.,2.22044604925031E-16,0.));
#13445=DIRECTION('center_axis',(-1.,2.22044604925031E-16,0.));
#13446=DIRECTION('ref_axis',(1.57009245868376E-16,0.707106781186541,-0.707106781186554));
#13447=DIRECTION('',(1.,-2.22044604925031E-16,0.));
#13448=DIRECTION('center_axis',(0.,0.,1.));
#13449=DIRECTION('ref_axis',(-0.707106781186554,0.707106781186541,0.));
#13450=DIRECTION('',(0.,0.,1.));
#13451=DIRECTION('center_axis',(-1.,2.22044604925031E-16,0.));
#13452=DIRECTION('ref_axis',(-2.05142465794791E-16,-0.923879532511288,0.382683432365088));
#13453=DIRECTION('',(-1.,2.22044604925031E-16,0.));
#13454=DIRECTION('center_axis',(2.22044604925031E-16,1.,0.));
#13455=DIRECTION('ref_axis',(-0.707106781186554,1.57009245868379E-16,-0.707106781186541));
#13456=DIRECTION('',(2.22044604925031E-16,1.,0.));
#13457=DIRECTION('center_axis',(1.57009245868377E-16,0.707106781186548,
-0.707106781186548));
#13458=DIRECTION('ref_axis',(0.707106781186553,0.499999999999997,0.499999999999996));
#13459=DIRECTION('',(1.57009245868377E-16,0.707106781186548,-0.707106781186548));
#13460=DIRECTION('center_axis',(-1.,2.22044604925031E-16,0.));
#13461=DIRECTION('ref_axis',(2.05142465794791E-16,0.923879532511283,-0.382683432365098));
#13462=DIRECTION('',(-1.,2.22044604925031E-16,0.));
#13463=DIRECTION('',(1.,-2.22044604925031E-16,0.));
#13464=DIRECTION('center_axis',(-1.,2.22044604925031E-16,0.));
#13465=DIRECTION('ref_axis',(-2.22044604925031E-16,-1.,0.));
#13466=DIRECTION('center_axis',(1.57009245868377E-16,0.707106781186548,
0.707106781186548));
#13467=DIRECTION('ref_axis',(1.57009245868377E-16,0.707106781186548,-0.707106781186548));
#13468=DIRECTION('center_axis',(2.22044604925031E-16,1.,0.));
#13469=DIRECTION('ref_axis',(-1.,2.22044604925031E-16,0.));
#13470=DIRECTION('center_axis',(-2.22044604925031E-16,-1.,0.));
#13471=DIRECTION('ref_axis',(0.,0.,1.));
#13472=DIRECTION('center_axis',(-2.22044604925031E-16,-1.,0.));
#13473=DIRECTION('ref_axis',(1.,-2.22044604925031E-16,0.));
#13474=DIRECTION('center_axis',(0.,0.,1.));
#13475=DIRECTION('ref_axis',(-2.22044604925031E-16,-1.,0.));
#13476=DIRECTION('center_axis',(-2.22044604925031E-16,-1.,0.));
#13477=DIRECTION('ref_axis',(0.,0.,1.));
#13478=DIRECTION('center_axis',(0.,0.,-1.));
#13479=DIRECTION('ref_axis',(-2.22044604925031E-16,-1.,0.));
#13480=DIRECTION('center_axis',(1.,-2.22044604925031E-16,0.));
#13481=DIRECTION('ref_axis',(2.22044604925031E-16,1.,0.));
#15612=CARTESIAN_POINT('',(0.,0.,0.));
#15613=CARTESIAN_POINT('Origin',(-71.2994615223724,45.9821613702938,64.));
#15614=CARTESIAN_POINT('',(-58.7994615223724,45.9821613702938,64.));
#15615=CARTESIAN_POINT('Origin',(-71.2994615223724,45.9821613702938,64.));
#15616=CARTESIAN_POINT('',(-58.7994615223724,45.9821613702938,52.));
#15617=CARTESIAN_POINT('',(-58.7994615223724,45.9821613702938,64.));
#15618=CARTESIAN_POINT('Origin',(-71.2994615223724,45.9821613702938,52.));
#15619=CARTESIAN_POINT('Origin',(-71.2994615223724,-45.9821613702938,64.));
#15620=CARTESIAN_POINT('',(-58.7994615223724,-45.9821613702938,64.));
#15621=CARTESIAN_POINT('Origin',(-71.2994615223724,-45.9821613702938,64.));
#15622=CARTESIAN_POINT('',(-58.7994615223724,-45.9821613702938,52.));
#15623=CARTESIAN_POINT('',(-58.7994615223724,-45.9821613702938,64.));
#15624=CARTESIAN_POINT('',(-83.7822941402435,-45.3272645584124,52.));
#15625=CARTESIAN_POINT('Origin',(-71.2994615223724,-45.9821613702938,52.));
#15626=CARTESIAN_POINT('',(-83.745995712817,-44.8272645584124,51.5));
#15627=CARTESIAN_POINT('Ctrl Pts',(-83.745995712817,-44.8272645584124,51.5));
#15628=CARTESIAN_POINT('Ctrl Pts',(-83.745995712817,-44.8272645584124,51.5628289407498));
#15629=CARTESIAN_POINT('Ctrl Pts',(-83.747181725005,-44.83983109791,51.6298216562663));
#15630=CARTESIAN_POINT('Ctrl Pts',(-83.7517608175057,-44.8908782000976,
51.7530059059081));
#15631=CARTESIAN_POINT('Ctrl Pts',(-83.7551262217237,-44.9293569823107,
51.8091992050848));
#15632=CARTESIAN_POINT('Ctrl Pts',(-83.762309793067,-45.0181089553366,51.8979511781107));
#15633=CARTESIAN_POINT('Ctrl Pts',(-83.7666038574713,-45.0743219277052,
51.936421701237));
#15634=CARTESIAN_POINT('Ctrl Pts',(-83.7749619719384,-45.1974964800649,
51.9874465324277));
#15635=CARTESIAN_POINT('Ctrl Pts',(-83.7789991865087,-45.264460227701,52.));
#15636=CARTESIAN_POINT('Ctrl Pts',(-83.7822941402435,-45.3272645584124,
52.));
#15637=CARTESIAN_POINT('',(-83.745995712817,-44.8272645584124,48.1978257430375));
#15638=CARTESIAN_POINT('',(-83.745995712817,-44.8272645584124,64.));
#15639=CARTESIAN_POINT('',(-83.6894299057874,-44.3272645584124,47.6978257430375));
#15640=CARTESIAN_POINT('Ctrl Pts',(-83.6894299057874,-44.3272645584124,
47.6978257430375));
#15641=CARTESIAN_POINT('Ctrl Pts',(-83.6977893835036,-44.3898507353037,
47.6978257430375));
#15642=CARTESIAN_POINT('Ctrl Pts',(-83.7061896428019,-44.4567282803348,
47.7102969796753));
#15643=CARTESIAN_POINT('Ctrl Pts',(-83.7207197517911,-44.5799514130651,
47.7612544377797));
#15644=CARTESIAN_POINT('Ctrl Pts',(-83.7268763359328,-44.636291625979,47.7997460294175));
#15645=CARTESIAN_POINT('Ctrl Pts',(-83.7361763124954,-44.7251367458781,
47.8885911493166));
#15646=CARTESIAN_POINT('Ctrl Pts',(-83.7399528718684,-44.7636241839714,
47.9447717029639));
#15647=CARTESIAN_POINT('Ctrl Pts',(-83.7448488457163,-44.8146887744293,
48.0679654140368));
#15648=CARTESIAN_POINT('Ctrl Pts',(-83.745995712817,-44.8272645584124,48.1349780461073));
#15649=CARTESIAN_POINT('Ctrl Pts',(-83.745995712817,-44.8272645584124,48.1978257430375));
#15650=CARTESIAN_POINT('',(-58.9094931389573,-44.3272645584124,47.6978257430375));
#15651=CARTESIAN_POINT('Origin',(-71.2994615223724,-45.9821613702938,47.6978257430375));
#15652=CARTESIAN_POINT('',(-58.8529273319278,-44.8272645584124,48.1978257430375));
#15653=CARTESIAN_POINT('Ctrl Pts',(-58.8529273319278,-44.8272645584124,
48.1978257430375));
#15654=CARTESIAN_POINT('Ctrl Pts',(-58.8529273319278,-44.8272645584124,
48.1349780461073));
#15655=CARTESIAN_POINT('Ctrl Pts',(-58.8540741990285,-44.8146887744293,
48.0679654140368));
#15656=CARTESIAN_POINT('Ctrl Pts',(-58.8589701728764,-44.7636241839714,
47.9447717029639));
#15657=CARTESIAN_POINT('Ctrl Pts',(-58.8627467322493,-44.7251367458781,
47.8885911493166));
#15658=CARTESIAN_POINT('Ctrl Pts',(-58.872046708812,-44.636291625979,47.7997460294175));
#15659=CARTESIAN_POINT('Ctrl Pts',(-58.8782032929536,-44.5799514130651,
47.7612544377797));
#15660=CARTESIAN_POINT('Ctrl Pts',(-58.8927334019429,-44.4567282803348,
47.7102969796753));
#15661=CARTESIAN_POINT('Ctrl Pts',(-58.9011336612412,-44.3898507353037,
47.6978257430375));
#15662=CARTESIAN_POINT('Ctrl Pts',(-58.9094931389573,-44.3272645584124,
47.6978257430375));
#15663=CARTESIAN_POINT('',(-58.8529273319278,-44.8272645584124,51.5));
#15664=CARTESIAN_POINT('',(-58.8529273319278,-44.8272645584124,64.));
#15665=CARTESIAN_POINT('',(-58.8166289045013,-45.3272645584124,52.));
#15666=CARTESIAN_POINT('Ctrl Pts',(-58.8166289045013,-45.3272645584124,
52.));
#15667=CARTESIAN_POINT('Ctrl Pts',(-58.8199238582361,-45.264460227701,52.));
#15668=CARTESIAN_POINT('Ctrl Pts',(-58.8239610728064,-45.1974964800649,
51.9874465324277));
#15669=CARTESIAN_POINT('Ctrl Pts',(-58.8323191872735,-45.0743219277052,
51.9364217012371));
#15670=CARTESIAN_POINT('Ctrl Pts',(-58.8366132516778,-45.0181089553366,
51.8979511781107));
#15671=CARTESIAN_POINT('Ctrl Pts',(-58.8437968230211,-44.9293569823107,
51.8091992050848));
#15672=CARTESIAN_POINT('Ctrl Pts',(-58.847162227239,-44.8908782000976,51.7530059059082));
#15673=CARTESIAN_POINT('Ctrl Pts',(-58.8517413197398,-44.83983109791,51.6298216562663));
#15674=CARTESIAN_POINT('Ctrl Pts',(-58.8529273319278,-44.8272645584124,
51.5628289407498));
#15675=CARTESIAN_POINT('Ctrl Pts',(-58.8529273319278,-44.8272645584124,
51.5));
#15676=CARTESIAN_POINT('Origin',(-71.2994615223724,-45.9821613702938,52.));
#15677=CARTESIAN_POINT('Origin',(-90.,-21.5741207385023,47.6978257430375));
#15678=CARTESIAN_POINT('',(-89.5,-44.3272645584124,47.6978257430375));
#15679=CARTESIAN_POINT('',(-90.,-44.3272645584124,47.6978257430375));
#15680=CARTESIAN_POINT('',(-89.5,-22.0741207385023,47.6978257430375));
#15681=CARTESIAN_POINT('',(-89.5,21.7129396307488,47.6978257430375));
#15682=CARTESIAN_POINT('',(-59.5720117555674,-22.0741207385024,47.6978257430375));
#15683=CARTESIAN_POINT('',(-90.,-22.0741207385023,47.6978257430375));
#15684=CARTESIAN_POINT('',(-49.8290651996878,-22.0741207385024,47.6978257430375));
#15685=CARTESIAN_POINT('Origin',(-54.7005384776276,-20.9477335482704,47.6978257430375));
#15686=CARTESIAN_POINT('',(-17.5720117555674,-22.0741207385024,47.6978257430375));
#15687=CARTESIAN_POINT('',(-90.,-22.0741207385023,47.6978257430375));
#15688=CARTESIAN_POINT('',(-7.82906519968783,-22.0741207385024,47.6978257430375));
#15689=CARTESIAN_POINT('Origin',(-12.7005384776276,-20.9477335482704,47.6978257430375));
#15690=CARTESIAN_POINT('',(24.4279882444326,-22.0741207385024,47.6978257430375));
#15691=CARTESIAN_POINT('',(-90.,-22.0741207385023,47.6978257430375));
#15692=CARTESIAN_POINT('',(34.1709348003122,-22.0741207385024,47.6978257430375));
#15693=CARTESIAN_POINT('Origin',(29.2994615223724,-20.9477335482704,47.6978257430375));
#15694=CARTESIAN_POINT('',(66.4279882444326,-22.0741207385024,47.6978257430375));
#15695=CARTESIAN_POINT('',(-90.,-22.0741207385023,47.6978257430375));
#15696=CARTESIAN_POINT('',(76.1709348003122,-22.0741207385024,47.6978257430375));
#15697=CARTESIAN_POINT('Origin',(71.2994615223724,-20.9477335482704,47.6978257430375));
#15698=CARTESIAN_POINT('',(89.5,-22.0741207385024,47.6978257430375));
#15699=CARTESIAN_POINT('',(-90.,-22.0741207385023,47.6978257430375));
#15700=CARTESIAN_POINT('',(89.5,-44.3272645584125,47.6978257430375));
#15701=CARTESIAN_POINT('',(89.5,-43.2870603692512,47.6978257430375));
#15702=CARTESIAN_POINT('',(83.6894299057875,-44.3272645584125,47.6978257430375));
#15703=CARTESIAN_POINT('',(-90.,-44.3272645584124,47.6978257430375));
#15704=CARTESIAN_POINT('',(58.9094931389573,-44.3272645584125,47.6978257430375));
#15705=CARTESIAN_POINT('Origin',(71.2994615223724,-45.9821613702938,47.6978257430375));
#15706=CARTESIAN_POINT('',(54.6969417294651,-44.3272645584125,47.6978257430375));
#15707=CARTESIAN_POINT('',(-90.,-44.3272645584124,47.6978257430375));
#15708=CARTESIAN_POINT('',(55.2994615223724,-41.9477335482704,47.6978257430375));
#15709=CARTESIAN_POINT('Origin',(50.2994615223724,-41.9477335482704,47.6978257430375));
#15710=CARTESIAN_POINT('',(45.9019813152797,-44.3272645584125,47.6978257430375));
#15711=CARTESIAN_POINT('Origin',(50.2994615223724,-41.9477335482704,47.6978257430375));
#15712=CARTESIAN_POINT('',(12.6969417294651,-44.3272645584125,47.6978257430375));
#15713=CARTESIAN_POINT('',(-90.,-44.3272645584124,47.6978257430375));
#15714=CARTESIAN_POINT('',(13.2994615223724,-41.9477335482704,47.6978257430375));
#15715=CARTESIAN_POINT('Origin',(8.29946152237238,-41.9477335482704,47.6978257430375));
#15716=CARTESIAN_POINT('',(3.90198131527965,-44.3272645584125,47.6978257430375));
#15717=CARTESIAN_POINT('Origin',(8.29946152237238,-41.9477335482704,47.6978257430375));
#15718=CARTESIAN_POINT('',(-29.3030582705349,-44.3272645584125,47.6978257430375));
#15719=CARTESIAN_POINT('',(-90.,-44.3272645584124,47.6978257430375));
#15720=CARTESIAN_POINT('',(-28.7005384776276,-41.9477335482704,47.6978257430375));
#15721=CARTESIAN_POINT('Origin',(-33.7005384776276,-41.9477335482704,47.6978257430375));
#15722=CARTESIAN_POINT('',(-38.0980186847204,-44.3272645584125,47.6978257430375));
#15723=CARTESIAN_POINT('Origin',(-33.7005384776276,-41.9477335482704,47.6978257430375));
#15724=CARTESIAN_POINT('',(-90.,-44.3272645584124,47.6978257430375));
#15725=CARTESIAN_POINT('Origin',(-90.,-44.3272645584124,48.1978257430375));
#15726=CARTESIAN_POINT('',(-89.5,-44.8272645584124,48.1978257430375));
#15727=CARTESIAN_POINT('',(-90.,-44.8272645584124,48.1978257430375));
#15728=CARTESIAN_POINT('Origin',(-89.5,-44.3272645584124,48.1978257430375));
#15729=CARTESIAN_POINT('Origin',(-90.,-44.8272645584124,47.6978257430375));
#15730=CARTESIAN_POINT('',(-89.5,-44.8272645584124,51.5));
#15731=CARTESIAN_POINT('',(-45.,-44.8272645584124,51.5));
#15732=CARTESIAN_POINT('',(-89.5,-44.8272645584124,49.8489128715187));
#15733=CARTESIAN_POINT('Origin',(-45.,-45.3272645584124,51.5));
#15734=CARTESIAN_POINT('',(-89.5,-45.3272645584124,52.));
#15735=CARTESIAN_POINT('',(-45.,-45.3272645584124,52.));
#15736=CARTESIAN_POINT('Origin',(-89.5,-45.3272645584124,51.5));
#15737=CARTESIAN_POINT('Origin',(50.2994615223724,-41.9477335482704,64.));
#15738=CARTESIAN_POINT('',(55.2994615223724,-41.9477335482704,64.));
#15739=CARTESIAN_POINT('Origin',(50.2994615223724,-41.9477335482704,64.));
#15740=CARTESIAN_POINT('',(55.2994615223724,-41.9477335482704,64.));
#15741=CARTESIAN_POINT('',(54.3870404098839,-44.8272645584125,48.1978257430375));
#15742=CARTESIAN_POINT('Ctrl Pts',(54.3870404098839,-44.8272645584125,48.1978257430375));
#15743=CARTESIAN_POINT('Ctrl Pts',(54.3870404098839,-44.8272645584125,48.1321584122493));
#15744=CARTESIAN_POINT('Ctrl Pts',(54.3967984405243,-44.8135380049882,48.0636994127672));
#15745=CARTESIAN_POINT('Ctrl Pts',(54.4328078861395,-44.7613527165995,47.9408836439009));
#15746=CARTESIAN_POINT('Ctrl Pts',(54.4588553021428,-44.7229773515989,47.8864317550374));
#15747=CARTESIAN_POINT('Ctrl Pts',(54.516109620418,-44.6352673224994,47.7987217259379));
#15748=CARTESIAN_POINT('Ctrl Pts',(54.5518807965474,-44.5787128115292,47.7605853033887));
#15749=CARTESIAN_POINT('Ctrl Pts',(54.6254379450942,-44.4559300231492,47.710126421675));
#15750=CARTESIAN_POINT('Ctrl Pts',(54.6631764277562,-44.3896643528756,47.6978257430375));
#15751=CARTESIAN_POINT('Ctrl Pts',(54.6969417294651,-44.3272645584125,47.6978257430375));
#15752=CARTESIAN_POINT('',(54.3870404098839,-44.8272645584125,51.5));
#15753=CARTESIAN_POINT('',(54.3870404098839,-44.8272645584125,64.));
#15754=CARTESIAN_POINT('',(53.9843998056396,-45.3272645584125,52.));
#15755=CARTESIAN_POINT('Ctrl Pts',(53.9843998056396,-45.3272645584125,52.));
#15756=CARTESIAN_POINT('Ctrl Pts',(54.0373751514369,-45.269501845417,52.));
#15757=CARTESIAN_POINT('Ctrl Pts',(54.09337665569,-45.2054409446566,51.9894566895945));
#15758=CARTESIAN_POINT('Ctrl Pts',(54.1960417034407,-45.0819180329636,51.9406971089121));
#15759=CARTESIAN_POINT('Ctrl Pts',(54.2427357823159,-45.0225259231798,51.9023681459539));
#15760=CARTESIAN_POINT('Ctrl Pts',(54.3112071685676,-44.9324583590974,51.8123005818715));
#15761=CARTESIAN_POINT('Ctrl Pts',(54.3393802752971,-44.8939359317371,51.7582688558033));
#15762=CARTESIAN_POINT('Ctrl Pts',(54.377261890984,-44.8412774147571,51.6352518100092));
#15763=CARTESIAN_POINT('Ctrl Pts',(54.3870404098839,-44.8272645584125,51.5662353407203));
#15764=CARTESIAN_POINT('Ctrl Pts',(54.3870404098839,-44.8272645584125,51.5));
#15765=CARTESIAN_POINT('',(46.6145232391052,-45.3272645584125,52.));
#15766=CARTESIAN_POINT('Origin',(50.2994615223724,-41.9477335482704,52.));
#15767=CARTESIAN_POINT('',(46.2118826348608,-44.8272645584125,51.5));
#15768=CARTESIAN_POINT('Ctrl Pts',(46.2118826348608,-44.8272645584125,51.5));
#15769=CARTESIAN_POINT('Ctrl Pts',(46.2118826348608,-44.8272645584125,51.5662353407203));
#15770=CARTESIAN_POINT('Ctrl Pts',(46.2216611537608,-44.8412774147571,51.6352518100092));
#15771=CARTESIAN_POINT('Ctrl Pts',(46.2595427694477,-44.8939359317371,51.7582688558033));
#15772=CARTESIAN_POINT('Ctrl Pts',(46.2877158761771,-44.9324583590974,51.8123005818715));
#15773=CARTESIAN_POINT('Ctrl Pts',(46.3561872624289,-45.0225259231798,51.9023681459539));
#15774=CARTESIAN_POINT('Ctrl Pts',(46.4028813413041,-45.0819180329636,51.9406971089121));
#15775=CARTESIAN_POINT('Ctrl Pts',(46.5055463890548,-45.2054409446566,51.9894566895945));
#15776=CARTESIAN_POINT('Ctrl Pts',(46.5615478933078,-45.269501845417,52.));
#15777=CARTESIAN_POINT('Ctrl Pts',(46.6145232391052,-45.3272645584125,52.));
#15778=CARTESIAN_POINT('',(46.2118826348608,-44.8272645584125,48.1978257430375));
#15779=CARTESIAN_POINT('',(46.2118826348608,-44.8272645584125,64.));
#15780=CARTESIAN_POINT('Ctrl Pts',(45.9019813152797,-44.3272645584125,47.6978257430375));
#15781=CARTESIAN_POINT('Ctrl Pts',(45.9357466169886,-44.3896643528756,47.6978257430375));
#15782=CARTESIAN_POINT('Ctrl Pts',(45.9734850996506,-44.4559300231492,47.710126421675));
#15783=CARTESIAN_POINT('Ctrl Pts',(46.0470422481974,-44.5787128115292,47.7605853033887));
#15784=CARTESIAN_POINT('Ctrl Pts',(46.0828134243267,-44.6352673224994,47.7987217259379));
#15785=CARTESIAN_POINT('Ctrl Pts',(46.140067742602,-44.7229773515989,47.8864317550374));
#15786=CARTESIAN_POINT('Ctrl Pts',(46.1661151586053,-44.7613527165994,47.9408836439009));
#15787=CARTESIAN_POINT('Ctrl Pts',(46.2021246042205,-44.8135380049881,48.0636994127672));
#15788=CARTESIAN_POINT('Ctrl Pts',(46.2118826348608,-44.8272645584125,48.1321584122493));
#15789=CARTESIAN_POINT('Ctrl Pts',(46.2118826348608,-44.8272645584125,48.1978257430375));
#15790=CARTESIAN_POINT('Origin',(-33.7005384776276,-0.052266451729599,64.));
#15791=CARTESIAN_POINT('',(-28.7005384776276,-0.0522664517295984,64.));
#15792=CARTESIAN_POINT('Origin',(-33.7005384776276,-0.052266451729599,64.));
#15793=CARTESIAN_POINT('',(-28.7005384776276,-0.0522664517295984,35.6978257430375));
#15794=CARTESIAN_POINT('',(-28.7005384776276,-0.0522664517295996,64.));
#15795=CARTESIAN_POINT('Origin',(-33.7005384776276,-0.052266451729599,35.6978257430375));
#15796=CARTESIAN_POINT('Origin',(50.2994615223724,-0.052266451729599,64.));
#15797=CARTESIAN_POINT('',(55.2994615223724,-0.0522664517295984,64.));
#15798=CARTESIAN_POINT('Origin',(50.2994615223724,-0.052266451729599,64.));
#15799=CARTESIAN_POINT('',(55.2994615223724,-0.0522664517295984,35.6978257430375));
#15800=CARTESIAN_POINT('',(55.2994615223724,-0.0522664517295996,64.));
#15801=CARTESIAN_POINT('Origin',(50.2994615223724,-0.052266451729599,35.6978257430375));
#15802=CARTESIAN_POINT('Origin',(71.2994615223724,-20.9477335482704,64.));
#15803=CARTESIAN_POINT('',(76.2994615223724,-20.9477335482704,64.));
#15804=CARTESIAN_POINT('Origin',(71.2994615223724,-20.9477335482704,64.));
#15805=CARTESIAN_POINT('',(76.2994615223724,-20.9477335482704,35.6978257430375));
#15806=CARTESIAN_POINT('',(76.2994615223724,-20.9477335482704,64.));
#15807=CARTESIAN_POINT('',(76.2978638949456,-21.0741207385024,35.6978257430375));
#15808=CARTESIAN_POINT('Origin',(71.2994615223724,-20.9477335482704,35.6978257430375));
#15809=CARTESIAN_POINT('',(76.2600702640404,-21.5741207385024,36.1978257430375));
#15810=CARTESIAN_POINT('Ctrl Pts',(76.2600702640404,-21.5741207385024,36.1978257430375));
#15811=CARTESIAN_POINT('Ctrl Pts',(76.2600702640404,-21.5741207385024,36.1349939529891));
#15812=CARTESIAN_POINT('Ctrl Pts',(76.261707444775,-21.5615536728765,36.0680174512863));
#15813=CARTESIAN_POINT('Ctrl Pts',(76.2677518597934,-21.5105397842088,35.9448840917433));
#15814=CARTESIAN_POINT('Ctrl Pts',(76.272089134882,-21.4720964497992,35.8887223643976));
#15815=CARTESIAN_POINT('Ctrl Pts',(76.2806427116048,-21.3834176983908,35.7999882651862));
#15816=CARTESIAN_POINT('Ctrl Pts',(76.285421251069,-21.3272274349036,35.7614956023605));
#15817=CARTESIAN_POINT('Ctrl Pts',(76.2932700900897,-21.2040263789334,35.7104126564947));
#15818=CARTESIAN_POINT('Ctrl Pts',(76.2962737086844,-21.1370099503463,35.6978257430375));
#15819=CARTESIAN_POINT('Ctrl Pts',(76.2978638949456,-21.0741207385024,35.6978257430375));
#15820=CARTESIAN_POINT('',(76.2600702640404,-21.5741207385024,47.1978257430375));
#15821=CARTESIAN_POINT('',(76.2600702640404,-21.5741207385024,64.));
#15822=CARTESIAN_POINT('Ctrl Pts',(76.1709348003122,-22.0741207385024,47.6978257430375));
#15823=CARTESIAN_POINT('Ctrl Pts',(76.1853501219146,-22.0117764091386,47.6978257430375));
#15824=CARTESIAN_POINT('Ctrl Pts',(76.1994330591515,-21.9448505322038,47.685440610641));
#15825=CARTESIAN_POINT('Ctrl Pts',(76.2229851313344,-21.8211627737637,47.6342788519733));
#15826=CARTESIAN_POINT('Ctrl Pts',(76.2325215699319,-21.7644213914886,47.5954836759127));
#15827=CARTESIAN_POINT('Ctrl Pts',(76.2463930261636,-21.6756387909071,47.5061996323312));
#15828=CARTESIAN_POINT('Ctrl Pts',(76.2517358957749,-21.6373959691348,47.4501913374276));
#15829=CARTESIAN_POINT('Ctrl Pts',(76.2585400256461,-21.5866358243642,47.3273455515029));
#15830=CARTESIAN_POINT('Ctrl Pts',(76.2600702640404,-21.5741207385024,47.2605109663339));
#15831=CARTESIAN_POINT('Ctrl Pts',(76.2600702640404,-21.5741207385024,47.1978257430375));
#15832=CARTESIAN_POINT('',(66.3388527807044,-21.5741207385024,47.1978257430375));
#15833=CARTESIAN_POINT('Ctrl Pts',(66.3388527807044,-21.5741207385024,47.1978257430375));
#15834=CARTESIAN_POINT('Ctrl Pts',(66.3388527807044,-21.5741207385024,47.2605109663339));
#15835=CARTESIAN_POINT('Ctrl Pts',(66.3403830190987,-21.5866358243642,47.3273455515029));
#15836=CARTESIAN_POINT('Ctrl Pts',(66.3471871489699,-21.6373959691348,47.4501913374276));
#15837=CARTESIAN_POINT('Ctrl Pts',(66.3525300185812,-21.6756387909071,47.5061996323312));
#15838=CARTESIAN_POINT('Ctrl Pts',(66.3664014748128,-21.7644213914886,47.5954836759127));
#15839=CARTESIAN_POINT('Ctrl Pts',(66.3759379134104,-21.8211627737637,47.6342788519733));
#15840=CARTESIAN_POINT('Ctrl Pts',(66.3994899855933,-21.9448505322038,47.6854406106411));
#15841=CARTESIAN_POINT('Ctrl Pts',(66.4135729228302,-22.0117764091386,47.6978257430375));
#15842=CARTESIAN_POINT('Ctrl Pts',(66.4279882444326,-22.0741207385024,47.6978257430375));
#15843=CARTESIAN_POINT('',(66.3388527807044,-21.5741207385024,36.1978257430375));
#15844=CARTESIAN_POINT('',(66.3388527807044,-21.5741207385024,64.));
#15845=CARTESIAN_POINT('',(66.3010591497992,-21.0741207385024,35.6978257430375));
#15846=CARTESIAN_POINT('Ctrl Pts',(66.3010591497992,-21.0741207385024,35.6978257430375));
#15847=CARTESIAN_POINT('Ctrl Pts',(66.3026493360604,-21.1370099503463,35.6978257430375));
#15848=CARTESIAN_POINT('Ctrl Pts',(66.305652954655,-21.2040263789334,35.7104126564947));
#15849=CARTESIAN_POINT('Ctrl Pts',(66.3135017936757,-21.3272274349036,35.7614956023605));
#15850=CARTESIAN_POINT('Ctrl Pts',(66.31828033314,-21.3834176983908,35.7999882651862));
#15851=CARTESIAN_POINT('Ctrl Pts',(66.3268339098628,-21.4720964497992,35.8887223643976));
#15852=CARTESIAN_POINT('Ctrl Pts',(66.3311711849514,-21.5105397842088,35.9448840917433));
#15853=CARTESIAN_POINT('Ctrl Pts',(66.3372155999698,-21.5615536728765,36.0680174512863));
#15854=CARTESIAN_POINT('Ctrl Pts',(66.3388527807044,-21.5741207385024,36.1349939529891));
#15855=CARTESIAN_POINT('Ctrl Pts',(66.3388527807044,-21.5741207385024,36.1978257430375));
#15856=CARTESIAN_POINT('Origin',(71.2994615223724,-20.9477335482704,35.6978257430375));
#15857=CARTESIAN_POINT('Origin',(71.2994615223724,45.9821613702938,64.));
#15858=CARTESIAN_POINT('',(83.7994615223724,45.9821613702938,64.));
#15859=CARTESIAN_POINT('Origin',(71.2994615223724,45.9821613702938,64.));
#15860=CARTESIAN_POINT('',(83.7994615223724,45.9821613702938,52.));
#15861=CARTESIAN_POINT('',(83.7994615223724,45.9821613702938,64.));
#15862=CARTESIAN_POINT('Origin',(71.2994615223724,45.9821613702938,52.));
#15863=CARTESIAN_POINT('Origin',(29.2994615223724,-20.9477335482704,64.));
#15864=CARTESIAN_POINT('',(34.2994615223724,-20.9477335482704,64.));
#15865=CARTESIAN_POINT('Origin',(29.2994615223724,-20.9477335482704,64.));
#15866=CARTESIAN_POINT('',(34.2994615223724,-20.9477335482704,35.6978257430375));
#15867=CARTESIAN_POINT('',(34.2994615223724,-20.9477335482704,64.));
#15868=CARTESIAN_POINT('',(34.2978638949456,-21.0741207385024,35.6978257430375));
#15869=CARTESIAN_POINT('Origin',(29.2994615223724,-20.9477335482704,35.6978257430375));
#15870=CARTESIAN_POINT('',(34.2600702640404,-21.5741207385024,36.1978257430375));
#15871=CARTESIAN_POINT('Ctrl Pts',(34.2600702640404,-21.5741207385024,36.1978257430375));
#15872=CARTESIAN_POINT('Ctrl Pts',(34.2600702640404,-21.5741207385024,36.1349939529891));
#15873=CARTESIAN_POINT('Ctrl Pts',(34.261707444775,-21.5615536728765,36.0680174512863));
#15874=CARTESIAN_POINT('Ctrl Pts',(34.2677518597934,-21.5105397842088,35.9448840917433));
#15875=CARTESIAN_POINT('Ctrl Pts',(34.272089134882,-21.4720964497992,35.8887223643976));
#15876=CARTESIAN_POINT('Ctrl Pts',(34.2806427116048,-21.3834176983908,35.7999882651862));
#15877=CARTESIAN_POINT('Ctrl Pts',(34.285421251069,-21.3272274349036,35.7614956023605));
#15878=CARTESIAN_POINT('Ctrl Pts',(34.2932700900897,-21.2040263789334,35.7104126564947));
#15879=CARTESIAN_POINT('Ctrl Pts',(34.2962737086844,-21.1370099503463,35.6978257430375));
#15880=CARTESIAN_POINT('Ctrl Pts',(34.2978638949456,-21.0741207385024,35.6978257430375));
#15881=CARTESIAN_POINT('',(34.2600702640404,-21.5741207385024,47.1978257430375));
#15882=CARTESIAN_POINT('',(34.2600702640404,-21.5741207385024,64.));
#15883=CARTESIAN_POINT('Ctrl Pts',(34.1709348003122,-22.0741207385024,47.6978257430375));
#15884=CARTESIAN_POINT('Ctrl Pts',(34.1853501219146,-22.0117764091386,47.6978257430375));
#15885=CARTESIAN_POINT('Ctrl Pts',(34.1994330591515,-21.9448505322038,47.6854406106411));
#15886=CARTESIAN_POINT('Ctrl Pts',(34.2229851313344,-21.8211627737637,47.6342788519733));
#15887=CARTESIAN_POINT('Ctrl Pts',(34.2325215699319,-21.7644213914886,47.5954836759127));
#15888=CARTESIAN_POINT('Ctrl Pts',(34.2463930261636,-21.6756387909071,47.5061996323312));
#15889=CARTESIAN_POINT('Ctrl Pts',(34.2517358957749,-21.6373959691348,47.4501913374276));
#15890=CARTESIAN_POINT('Ctrl Pts',(34.2585400256461,-21.5866358243642,47.3273455515029));
#15891=CARTESIAN_POINT('Ctrl Pts',(34.2600702640404,-21.5741207385024,47.2605109663339));
#15892=CARTESIAN_POINT('Ctrl Pts',(34.2600702640404,-21.5741207385024,47.1978257430375));
#15893=CARTESIAN_POINT('',(24.3388527807044,-21.5741207385024,47.1978257430375));
#15894=CARTESIAN_POINT('Ctrl Pts',(24.3388527807044,-21.5741207385024,47.1978257430375));
#15895=CARTESIAN_POINT('Ctrl Pts',(24.3388527807044,-21.5741207385024,47.2605109663339));
#15896=CARTESIAN_POINT('Ctrl Pts',(24.3403830190987,-21.5866358243642,47.3273455515029));
#15897=CARTESIAN_POINT('Ctrl Pts',(24.3471871489699,-21.6373959691348,47.4501913374276));
#15898=CARTESIAN_POINT('Ctrl Pts',(24.3525300185812,-21.6756387909071,47.5061996323312));
#15899=CARTESIAN_POINT('Ctrl Pts',(24.3664014748128,-21.7644213914886,47.5954836759127));
#15900=CARTESIAN_POINT('Ctrl Pts',(24.3759379134104,-21.8211627737637,47.6342788519733));
#15901=CARTESIAN_POINT('Ctrl Pts',(24.3994899855933,-21.9448505322038,47.6854406106411));
#15902=CARTESIAN_POINT('Ctrl Pts',(24.4135729228302,-22.0117764091386,47.6978257430375));
#15903=CARTESIAN_POINT('Ctrl Pts',(24.4279882444326,-22.0741207385024,47.6978257430375));
#15904=CARTESIAN_POINT('',(24.3388527807044,-21.5741207385024,36.1978257430375));
#15905=CARTESIAN_POINT('',(24.3388527807044,-21.5741207385024,64.));
#15906=CARTESIAN_POINT('',(24.3010591497992,-21.0741207385024,35.6978257430375));
#15907=CARTESIAN_POINT('Ctrl Pts',(24.3010591497992,-21.0741207385024,35.6978257430375));
#15908=CARTESIAN_POINT('Ctrl Pts',(24.3026493360604,-21.1370099503463,35.6978257430375));
#15909=CARTESIAN_POINT('Ctrl Pts',(24.305652954655,-21.2040263789334,35.7104126564947));
#15910=CARTESIAN_POINT('Ctrl Pts',(24.3135017936757,-21.3272274349036,35.7614956023605));
#15911=CARTESIAN_POINT('Ctrl Pts',(24.31828033314,-21.3834176983908,35.7999882651862));
#15912=CARTESIAN_POINT('Ctrl Pts',(24.3268339098628,-21.4720964497992,35.8887223643976));
#15913=CARTESIAN_POINT('Ctrl Pts',(24.3311711849514,-21.5105397842088,35.9448840917433));
#15914=CARTESIAN_POINT('Ctrl Pts',(24.3372155999698,-21.5615536728765,36.0680174512863));
#15915=CARTESIAN_POINT('Ctrl Pts',(24.3388527807044,-21.5741207385024,36.1349939529891));
#15916=CARTESIAN_POINT('Ctrl Pts',(24.3388527807044,-21.5741207385024,36.1978257430375));
#15917=CARTESIAN_POINT('Origin',(29.2994615223724,-20.9477335482704,35.6978257430375));
#15918=CARTESIAN_POINT('Origin',(8.29946152237238,-0.052266451729599,64.));
#15919=CARTESIAN_POINT('',(13.2994615223724,-0.0522664517295984,64.));
#15920=CARTESIAN_POINT('Origin',(8.29946152237238,-0.052266451729599,64.));
#15921=CARTESIAN_POINT('',(13.2994615223724,-0.0522664517295984,35.6978257430375));
#15922=CARTESIAN_POINT('',(13.2994615223724,-0.0522664517295996,64.));
#15923=CARTESIAN_POINT('Origin',(8.29946152237238,-0.052266451729599,35.6978257430375));
#15924=CARTESIAN_POINT('Origin',(-54.7005384776276,-20.9477335482704,64.));
#15925=CARTESIAN_POINT('',(-49.7005384776276,-20.9477335482704,64.));
#15926=CARTESIAN_POINT('Origin',(-54.7005384776276,-20.9477335482704,64.));
#15927=CARTESIAN_POINT('',(-49.7005384776276,-20.9477335482704,35.6978257430375));
#15928=CARTESIAN_POINT('',(-49.7005384776276,-20.9477335482704,64.));
#15929=CARTESIAN_POINT('',(-49.7021361050544,-21.0741207385024,35.6978257430375));
#15930=CARTESIAN_POINT('Origin',(-54.7005384776276,-20.9477335482704,35.6978257430375));
#15931=CARTESIAN_POINT('',(-49.7399297359596,-21.5741207385024,36.1978257430375));
#15932=CARTESIAN_POINT('Ctrl Pts',(-49.7399297359596,-21.5741207385024,
36.1978257430375));
#15933=CARTESIAN_POINT('Ctrl Pts',(-49.7399297359596,-21.5741207385024,
36.1349939529891));
#15934=CARTESIAN_POINT('Ctrl Pts',(-49.738292555225,-21.5615536728765,36.0680174512863));
#15935=CARTESIAN_POINT('Ctrl Pts',(-49.7322481402066,-21.5105397842088,
35.9448840917433));
#15936=CARTESIAN_POINT('Ctrl Pts',(-49.727910865118,-21.4720964497991,35.8887223643976));
#15937=CARTESIAN_POINT('Ctrl Pts',(-49.7193572883952,-21.3834176983908,
35.7999882651862));
#15938=CARTESIAN_POINT('Ctrl Pts',(-49.714578748931,-21.3272274349035,35.7614956023605));
#15939=CARTESIAN_POINT('Ctrl Pts',(-49.7067299099103,-21.2040263789334,
35.7104126564947));
#15940=CARTESIAN_POINT('Ctrl Pts',(-49.7037262913156,-21.1370099503463,
35.6978257430375));
#15941=CARTESIAN_POINT('Ctrl Pts',(-49.7021361050544,-21.0741207385024,
35.6978257430375));
#15942=CARTESIAN_POINT('',(-49.7399297359596,-21.5741207385024,47.1978257430375));
#15943=CARTESIAN_POINT('',(-49.7399297359596,-21.5741207385024,64.));
#15944=CARTESIAN_POINT('Ctrl Pts',(-49.8290651996878,-22.0741207385024,
47.6978257430375));
#15945=CARTESIAN_POINT('Ctrl Pts',(-49.8146498780854,-22.0117764091386,
47.6978257430375));
#15946=CARTESIAN_POINT('Ctrl Pts',(-49.8005669408485,-21.9448505322038,
47.6854406106411));
#15947=CARTESIAN_POINT('Ctrl Pts',(-49.7770148686656,-21.8211627737637,
47.6342788519733));
#15948=CARTESIAN_POINT('Ctrl Pts',(-49.7674784300681,-21.7644213914886,
47.5954836759127));
#15949=CARTESIAN_POINT('Ctrl Pts',(-49.7536069738364,-21.675638790907,47.5061996323312));
#15950=CARTESIAN_POINT('Ctrl Pts',(-49.7482641042251,-21.6373959691347,
47.4501913374276));
#15951=CARTESIAN_POINT('Ctrl Pts',(-49.7414599743539,-21.5866358243642,
47.3273455515029));
#15952=CARTESIAN_POINT('Ctrl Pts',(-49.7399297359596,-21.5741207385024,
47.2605109663339));
#15953=CARTESIAN_POINT('Ctrl Pts',(-49.7399297359596,-21.5741207385024,
47.1978257430375));
#15954=CARTESIAN_POINT('',(-59.6611472192956,-21.5741207385024,47.1978257430375));
#15955=CARTESIAN_POINT('Ctrl Pts',(-59.6611472192956,-21.5741207385024,
47.1978257430375));
#15956=CARTESIAN_POINT('Ctrl Pts',(-59.6611472192956,-21.5741207385024,
47.2605109663339));
#15957=CARTESIAN_POINT('Ctrl Pts',(-59.6596169809013,-21.5866358243642,
47.3273455515029));
#15958=CARTESIAN_POINT('Ctrl Pts',(-59.6528128510301,-21.6373959691347,
47.4501913374276));
#15959=CARTESIAN_POINT('Ctrl Pts',(-59.6474699814188,-21.675638790907,47.5061996323312));
#15960=CARTESIAN_POINT('Ctrl Pts',(-59.6335985251872,-21.7644213914886,
47.5954836759127));
#15961=CARTESIAN_POINT('Ctrl Pts',(-59.6240620865897,-21.8211627737637,
47.6342788519733));
#15962=CARTESIAN_POINT('Ctrl Pts',(-59.6005100144067,-21.9448505322038,
47.6854406106411));
#15963=CARTESIAN_POINT('Ctrl Pts',(-59.5864270771698,-22.0117764091386,
47.6978257430375));
#15964=CARTESIAN_POINT('Ctrl Pts',(-59.5720117555674,-22.0741207385024,
47.6978257430375));
#15965=CARTESIAN_POINT('',(-59.6611472192956,-21.5741207385024,36.1978257430375));
#15966=CARTESIAN_POINT('',(-59.6611472192956,-21.5741207385024,64.));
#15967=CARTESIAN_POINT('',(-59.6989408502008,-21.0741207385024,35.6978257430375));
#15968=CARTESIAN_POINT('Ctrl Pts',(-59.6989408502008,-21.0741207385024,
35.6978257430375));
#15969=CARTESIAN_POINT('Ctrl Pts',(-59.6973506639396,-21.1370099503463,
35.6978257430375));
#15970=CARTESIAN_POINT('Ctrl Pts',(-59.694347045345,-21.2040263789334,35.7104126564947));
#15971=CARTESIAN_POINT('Ctrl Pts',(-59.6864982063243,-21.3272274349035,
35.7614956023605));
#15972=CARTESIAN_POINT('Ctrl Pts',(-59.68171966686,-21.3834176983908,35.7999882651862));
#15973=CARTESIAN_POINT('Ctrl Pts',(-59.6731660901373,-21.4720964497991,
35.8887223643976));
#15974=CARTESIAN_POINT('Ctrl Pts',(-59.6688288150486,-21.5105397842088,
35.9448840917433));
#15975=CARTESIAN_POINT('Ctrl Pts',(-59.6627844000302,-21.5615536728765,
36.0680174512863));
#15976=CARTESIAN_POINT('Ctrl Pts',(-59.6611472192956,-21.5741207385024,
36.1349939529891));
#15977=CARTESIAN_POINT('Ctrl Pts',(-59.6611472192956,-21.5741207385024,
36.1978257430375));
#15978=CARTESIAN_POINT('Origin',(-54.7005384776276,-20.9477335482704,35.6978257430375));
#15979=CARTESIAN_POINT('Origin',(-33.7005384776276,41.9477335482704,64.));
#15980=CARTESIAN_POINT('',(-28.7005384776276,41.9477335482704,64.));
#15981=CARTESIAN_POINT('Origin',(-33.7005384776276,41.9477335482704,64.));
#15982=CARTESIAN_POINT('',(-28.7005384776276,41.9477335482704,52.));
#15983=CARTESIAN_POINT('',(-28.7005384776276,41.9477335482704,64.));
#15984=CARTESIAN_POINT('Origin',(-33.7005384776276,41.9477335482704,52.));
#15985=CARTESIAN_POINT('Origin',(8.29946152237238,-41.9477335482704,64.));
#15986=CARTESIAN_POINT('',(13.2994615223724,-41.9477335482704,64.));
#15987=CARTESIAN_POINT('Origin',(8.29946152237238,-41.9477335482704,64.));
#15988=CARTESIAN_POINT('',(13.2994615223724,-41.9477335482704,64.));
#15989=CARTESIAN_POINT('',(12.387040409884,-44.8272645584125,48.1978257430375));
#15990=CARTESIAN_POINT('Ctrl Pts',(12.3870404098839,-44.8272645584125,48.1978257430375));
#15991=CARTESIAN_POINT('Ctrl Pts',(12.3870404098839,-44.8272645584125,48.1321584122493));
#15992=CARTESIAN_POINT('Ctrl Pts',(12.3967984405243,-44.8135380049881,48.0636994127671));
#15993=CARTESIAN_POINT('Ctrl Pts',(12.4328078861395,-44.7613527165994,47.9408836439009));
#15994=CARTESIAN_POINT('Ctrl Pts',(12.4588553021428,-44.7229773515989,47.8864317550374));
#15995=CARTESIAN_POINT('Ctrl Pts',(12.516109620418,-44.6352673224994,47.7987217259379));
#15996=CARTESIAN_POINT('Ctrl Pts',(12.5518807965474,-44.5787128115292,47.7605853033887));
#15997=CARTESIAN_POINT('Ctrl Pts',(12.6254379450942,-44.4559300231491,47.710126421675));
#15998=CARTESIAN_POINT('Ctrl Pts',(12.6631764277562,-44.3896643528756,47.6978257430375));
#15999=CARTESIAN_POINT('Ctrl Pts',(12.6969417294651,-44.3272645584124,47.6978257430375));
#16000=CARTESIAN_POINT('',(12.3870404098839,-44.8272645584125,51.5));
#16001=CARTESIAN_POINT('',(12.387040409884,-44.8272645584125,64.));
#16002=CARTESIAN_POINT('',(11.9843998056396,-45.3272645584125,52.));
#16003=CARTESIAN_POINT('Ctrl Pts',(11.9843998056396,-45.3272645584125,52.));
#16004=CARTESIAN_POINT('Ctrl Pts',(12.0373751514369,-45.269501845417,52.));
#16005=CARTESIAN_POINT('Ctrl Pts',(12.09337665569,-45.2054409446566,51.9894566895945));
#16006=CARTESIAN_POINT('Ctrl Pts',(12.1960417034407,-45.0819180329636,51.9406971089121));
#16007=CARTESIAN_POINT('Ctrl Pts',(12.2427357823159,-45.0225259231798,51.9023681459539));
#16008=CARTESIAN_POINT('Ctrl Pts',(12.3112071685676,-44.9324583590974,51.8123005818715));
#16009=CARTESIAN_POINT('Ctrl Pts',(12.3393802752971,-44.8939359317371,51.7582688558033));
#16010=CARTESIAN_POINT('Ctrl Pts',(12.377261890984,-44.8412774147571,51.6352518100092));
#16011=CARTESIAN_POINT('Ctrl Pts',(12.387040409884,-44.8272645584125,51.5662353407203));
#16012=CARTESIAN_POINT('Ctrl Pts',(12.387040409884,-44.8272645584125,51.5));
#16013=CARTESIAN_POINT('',(4.61452323910518,-45.3272645584125,52.));
#16014=CARTESIAN_POINT('Origin',(8.29946152237238,-41.9477335482704,52.));
#16015=CARTESIAN_POINT('',(4.21188263486082,-44.8272645584125,51.5));
#16016=CARTESIAN_POINT('Ctrl Pts',(4.21188263486082,-44.8272645584125,51.5));
#16017=CARTESIAN_POINT('Ctrl Pts',(4.21188263486082,-44.8272645584125,51.5662353407203));
#16018=CARTESIAN_POINT('Ctrl Pts',(4.22166115376081,-44.8412774147571,51.6352518100092));
#16019=CARTESIAN_POINT('Ctrl Pts',(4.25954276944767,-44.8939359317371,51.7582688558033));
#16020=CARTESIAN_POINT('Ctrl Pts',(4.28771587617714,-44.9324583590974,51.8123005818715));
#16021=CARTESIAN_POINT('Ctrl Pts',(4.3561872624289,-45.0225259231798,51.9023681459539));
#16022=CARTESIAN_POINT('Ctrl Pts',(4.40288134130409,-45.0819180329636,51.9406971089121));
#16023=CARTESIAN_POINT('Ctrl Pts',(4.50554638905476,-45.2054409446566,51.9894566895945));
#16024=CARTESIAN_POINT('Ctrl Pts',(4.56154789330784,-45.269501845417,52.));
#16025=CARTESIAN_POINT('Ctrl Pts',(4.61452323910518,-45.3272645584125,52.));
#16026=CARTESIAN_POINT('',(4.21188263486082,-44.8272645584125,48.1978257430375));
#16027=CARTESIAN_POINT('',(4.21188263486082,-44.8272645584125,64.));
#16028=CARTESIAN_POINT('Ctrl Pts',(3.90198131527965,-44.3272645584124,47.6978257430375));
#16029=CARTESIAN_POINT('Ctrl Pts',(3.93574661698859,-44.3896643528756,47.6978257430375));
#16030=CARTESIAN_POINT('Ctrl Pts',(3.97348509965058,-44.4559300231491,47.710126421675));
#16031=CARTESIAN_POINT('Ctrl Pts',(4.04704224819734,-44.5787128115292,47.7605853033887));
#16032=CARTESIAN_POINT('Ctrl Pts',(4.08281342432674,-44.6352673224994,47.7987217259379));
#16033=CARTESIAN_POINT('Ctrl Pts',(4.14006774260197,-44.7229773515989,47.8864317550374));
#16034=CARTESIAN_POINT('Ctrl Pts',(4.16611515860529,-44.7613527165994,47.9408836439009));
#16035=CARTESIAN_POINT('Ctrl Pts',(4.20212460422049,-44.8135380049881,48.0636994127672));
#16036=CARTESIAN_POINT('Ctrl Pts',(4.21188263486082,-44.8272645584125,48.1321584122493));
#16037=CARTESIAN_POINT('Ctrl Pts',(4.21188263486082,-44.8272645584125,48.1978257430375));
#16038=CARTESIAN_POINT('Origin',(50.2994615223724,41.9477335482704,64.));
#16039=CARTESIAN_POINT('',(55.2994615223724,41.9477335482704,64.));
#16040=CARTESIAN_POINT('Origin',(50.2994615223724,41.9477335482704,64.));
#16041=CARTESIAN_POINT('',(55.2994615223724,41.9477335482704,52.));
#16042=CARTESIAN_POINT('',(55.2994615223724,41.9477335482704,64.));
#16043=CARTESIAN_POINT('Origin',(50.2994615223724,41.9477335482704,52.));
#16044=CARTESIAN_POINT('Origin',(-12.7005384776276,-20.9477335482704,64.));
#16045=CARTESIAN_POINT('',(-7.70053847762761,-20.9477335482704,64.));
#16046=CARTESIAN_POINT('Origin',(-12.7005384776276,-20.9477335482704,64.));
#16047=CARTESIAN_POINT('',(-7.70053847762761,-20.9477335482704,35.6978257430375));
#16048=CARTESIAN_POINT('',(-7.70053847762761,-20.9477335482704,64.));
#16049=CARTESIAN_POINT('',(-7.70213610505443,-21.0741207385024,35.6978257430375));
#16050=CARTESIAN_POINT('Origin',(-12.7005384776276,-20.9477335482704,35.6978257430375));
#16051=CARTESIAN_POINT('',(-7.73992973595958,-21.5741207385024,36.1978257430375));
#16052=CARTESIAN_POINT('Ctrl Pts',(-7.73992973595958,-21.5741207385024,
36.1978257430375));
#16053=CARTESIAN_POINT('Ctrl Pts',(-7.73992973595958,-21.5741207385024,
36.1349939529891));
#16054=CARTESIAN_POINT('Ctrl Pts',(-7.73829255522502,-21.5615536728765,
36.0680174512863));
#16055=CARTESIAN_POINT('Ctrl Pts',(-7.73224814020658,-21.5105397842088,
35.9448840917433));
#16056=CARTESIAN_POINT('Ctrl Pts',(-7.72791086511798,-21.4720964497992,
35.8887223643976));
#16057=CARTESIAN_POINT('Ctrl Pts',(-7.71935728839523,-21.3834176983908,
35.7999882651862));
#16058=CARTESIAN_POINT('Ctrl Pts',(-7.71457874893097,-21.3272274349035,
35.7614956023605));
#16059=CARTESIAN_POINT('Ctrl Pts',(-7.70672990991027,-21.2040263789334,
35.7104126564947));
#16060=CARTESIAN_POINT('Ctrl Pts',(-7.70372629131563,-21.1370099503463,
35.6978257430375));
#16061=CARTESIAN_POINT('Ctrl Pts',(-7.70213610505443,-21.0741207385024,
35.6978257430375));
#16062=CARTESIAN_POINT('',(-7.73992973595958,-21.5741207385024,47.1978257430375));
#16063=CARTESIAN_POINT('',(-7.73992973595958,-21.5741207385024,64.));
#16064=CARTESIAN_POINT('Ctrl Pts',(-7.82906519968783,-22.0741207385024,
47.6978257430375));
#16065=CARTESIAN_POINT('Ctrl Pts',(-7.81464987808543,-22.0117764091386,
47.6978257430375));
#16066=CARTESIAN_POINT('Ctrl Pts',(-7.80056694084853,-21.9448505322038,
47.6854406106411));
#16067=CARTESIAN_POINT('Ctrl Pts',(-7.77701486866557,-21.8211627737637,
47.6342788519733));
#16068=CARTESIAN_POINT('Ctrl Pts',(-7.76747843006806,-21.7644213914886,
47.5954836759127));
#16069=CARTESIAN_POINT('Ctrl Pts',(-7.7536069738364,-21.675638790907,47.5061996323312));
#16070=CARTESIAN_POINT('Ctrl Pts',(-7.74826410422513,-21.6373959691348,
47.4501913374276));
#16071=CARTESIAN_POINT('Ctrl Pts',(-7.74145997435394,-21.5866358243642,
47.3273455515029));
#16072=CARTESIAN_POINT('Ctrl Pts',(-7.73992973595958,-21.5741207385024,
47.2605109663339));
#16073=CARTESIAN_POINT('Ctrl Pts',(-7.73992973595958,-21.5741207385024,
47.1978257430375));
#16074=CARTESIAN_POINT('',(-17.6611472192956,-21.5741207385024,47.1978257430375));
#16075=CARTESIAN_POINT('Ctrl Pts',(-17.6611472192956,-21.5741207385024,
47.1978257430375));
#16076=CARTESIAN_POINT('Ctrl Pts',(-17.6611472192956,-21.5741207385024,
47.2605109663339));
#16077=CARTESIAN_POINT('Ctrl Pts',(-17.6596169809013,-21.5866358243642,
47.3273455515029));
#16078=CARTESIAN_POINT('Ctrl Pts',(-17.6528128510301,-21.6373959691348,
47.4501913374276));
#16079=CARTESIAN_POINT('Ctrl Pts',(-17.6474699814188,-21.675638790907,47.5061996323312));
#16080=CARTESIAN_POINT('Ctrl Pts',(-17.6335985251872,-21.7644213914886,
47.5954836759127));
#16081=CARTESIAN_POINT('Ctrl Pts',(-17.6240620865897,-21.8211627737637,
47.6342788519733));
#16082=CARTESIAN_POINT('Ctrl Pts',(-17.6005100144067,-21.9448505322038,
47.6854406106411));
#16083=CARTESIAN_POINT('Ctrl Pts',(-17.5864270771698,-22.0117764091386,
47.6978257430375));
#16084=CARTESIAN_POINT('Ctrl Pts',(-17.5720117555674,-22.0741207385024,
47.6978257430375));
#16085=CARTESIAN_POINT('',(-17.6611472192956,-21.5741207385024,36.1978257430375));
#16086=CARTESIAN_POINT('',(-17.6611472192956,-21.5741207385024,64.));
#16087=CARTESIAN_POINT('',(-17.6989408502008,-21.0741207385024,35.6978257430375));
#16088=CARTESIAN_POINT('Ctrl Pts',(-17.6989408502008,-21.0741207385024,
35.6978257430375));
#16089=CARTESIAN_POINT('Ctrl Pts',(-17.6973506639396,-21.1370099503463,
35.6978257430375));
#16090=CARTESIAN_POINT('Ctrl Pts',(-17.694347045345,-21.2040263789334,35.7104126564947));
#16091=CARTESIAN_POINT('Ctrl Pts',(-17.6864982063243,-21.3272274349035,
35.7614956023605));
#16092=CARTESIAN_POINT('Ctrl Pts',(-17.68171966686,-21.3834176983908,35.7999882651862));
#16093=CARTESIAN_POINT('Ctrl Pts',(-17.6731660901372,-21.4720964497992,
35.8887223643976));
#16094=CARTESIAN_POINT('Ctrl Pts',(-17.6688288150486,-21.5105397842088,
35.9448840917433));
#16095=CARTESIAN_POINT('Ctrl Pts',(-17.6627844000302,-21.5615536728765,
36.0680174512863));
#16096=CARTESIAN_POINT('Ctrl Pts',(-17.6611472192956,-21.5741207385024,
36.1349939529891));
#16097=CARTESIAN_POINT('Ctrl Pts',(-17.6611472192956,-21.5741207385024,
36.1978257430375));
#16098=CARTESIAN_POINT('Origin',(-12.7005384776276,-20.9477335482704,35.6978257430375));
#16099=CARTESIAN_POINT('Origin',(29.2994615223724,20.9477335482704,64.));
#16100=CARTESIAN_POINT('',(34.2994615223724,20.9477335482704,64.));
#16101=CARTESIAN_POINT('Origin',(29.2994615223724,20.9477335482704,64.));
#16102=CARTESIAN_POINT('',(34.2994615223724,20.9477335482704,47.6978257430375));
#16103=CARTESIAN_POINT('',(34.2994615223724,20.9477335482704,64.));
#16104=CARTESIAN_POINT('',(34.0987510891795,19.545300072509,47.6978257430375));
#16105=CARTESIAN_POINT('Origin',(29.2994615223724,20.9477335482704,47.6978257430375));
#16106=CARTESIAN_POINT('',(33.9233934931417,19.045300072509,47.1978257430375));
#16107=CARTESIAN_POINT('Ctrl Pts',(33.9233934931417,19.045300072509,47.1978257430375));
#16108=CARTESIAN_POINT('Ctrl Pts',(33.9233934931417,19.045300072509,47.2606262015597));
#16109=CARTESIAN_POINT('Ctrl Pts',(33.9286235220756,19.0578693331568,47.3272049658121));
#16110=CARTESIAN_POINT('Ctrl Pts',(33.9487439245958,19.1079235845375,47.4488825757172));
#16111=CARTESIAN_POINT('Ctrl Pts',(33.9635333627505,19.1453760973014,47.50401144732));
#16112=CARTESIAN_POINT('Ctrl Pts',(33.9963894622215,19.2327496876229,47.5933468507728));
#16113=CARTESIAN_POINT('Ctrl Pts',(34.0169336674918,19.2894923661088,47.6326971370671));
#16114=CARTESIAN_POINT('Ctrl Pts',(34.0588328495999,19.4138848506455,47.6849404681153));
#16115=CARTESIAN_POINT('Ctrl Pts',(34.0801249019844,19.4815591055255,47.6978257430375));
#16116=CARTESIAN_POINT('Ctrl Pts',(34.0987510891795,19.545300072509,47.6978257430375));
#16117=CARTESIAN_POINT('',(33.9233934931417,19.045300072509,36.1978257430375));
#16118=CARTESIAN_POINT('',(33.9233934931417,19.045300072509,64.));
#16119=CARTESIAN_POINT('',(33.6844716015559,18.545300072509,35.6978257430375));
#16120=CARTESIAN_POINT('Ctrl Pts',(33.6844716015559,18.545300072509,35.6978257430375));
#16121=CARTESIAN_POINT('Ctrl Pts',(33.7183437123576,18.6071246969023,35.6978257430375));
#16122=CARTESIAN_POINT('Ctrl Pts',(33.7533284422121,18.6744087742692,35.7099831569546));
#16123=CARTESIAN_POINT('Ctrl Pts',(33.8154443123393,18.800447936422,35.7624419799854));
#16124=CARTESIAN_POINT('Ctrl Pts',(33.8426335478405,18.8591453590194,35.8028130850757));
#16125=CARTESIAN_POINT('Ctrl Pts',(33.8819451449858,18.9470131641942,35.8942412268742));
#16126=CARTESIAN_POINT('Ctrl Pts',(33.8976695801488,18.983759545124,35.9488335262825));
#16127=CARTESIAN_POINT('Ctrl Pts',(33.91835801237,19.0329211748031,36.0694921472959));
#16128=CARTESIAN_POINT('Ctrl Pts',(33.9233934931417,19.045300072509,36.1355610097978));
#16129=CARTESIAN_POINT('Ctrl Pts',(33.9233934931417,19.045300072509,36.1978257430375));
#16130=CARTESIAN_POINT('',(24.9144514431889,18.545300072509,35.6978257430375));
#16131=CARTESIAN_POINT('Origin',(29.2994615223724,20.9477335482704,35.6978257430375));
#16132=CARTESIAN_POINT('',(24.6755295516031,19.045300072509,36.1978257430375));
#16133=CARTESIAN_POINT('Ctrl Pts',(24.6755295516031,19.045300072509,36.1978257430375));
#16134=CARTESIAN_POINT('Ctrl Pts',(24.6755295516031,19.045300072509,36.1355610097978));
#16135=CARTESIAN_POINT('Ctrl Pts',(24.6805650323748,19.0329211748031,36.0694921472959));
#16136=CARTESIAN_POINT('Ctrl Pts',(24.701253464596,18.983759545124,35.9488335262825));
#16137=CARTESIAN_POINT('Ctrl Pts',(24.716977899759,18.9470131641942,35.8942412268742));
#16138=CARTESIAN_POINT('Ctrl Pts',(24.7562894969043,18.8591453590194,35.8028130850757));
#16139=CARTESIAN_POINT('Ctrl Pts',(24.7834787324055,18.800447936422,35.7624419799854));
#16140=CARTESIAN_POINT('Ctrl Pts',(24.8455946025327,18.6744087742692,35.7099831569546));
#16141=CARTESIAN_POINT('Ctrl Pts',(24.8805793323871,18.6071246969023,35.6978257430375));
#16142=CARTESIAN_POINT('Ctrl Pts',(24.9144514431889,18.545300072509,35.6978257430375));
#16143=CARTESIAN_POINT('',(24.6755295516031,19.045300072509,47.1978257430375));
#16144=CARTESIAN_POINT('',(24.6755295516031,19.045300072509,64.));
#16145=CARTESIAN_POINT('',(24.5001719555652,19.545300072509,47.6978257430375));
#16146=CARTESIAN_POINT('Ctrl Pts',(24.5001719555652,19.545300072509,47.6978257430375));
#16147=CARTESIAN_POINT('Ctrl Pts',(24.5187981427604,19.4815591055255,47.6978257430375));
#16148=CARTESIAN_POINT('Ctrl Pts',(24.5400901951449,19.4138848506455,47.6849404681153));
#16149=CARTESIAN_POINT('Ctrl Pts',(24.5819893772529,19.2894923661088,47.6326971370671));
#16150=CARTESIAN_POINT('Ctrl Pts',(24.6025335825232,19.2327496876229,47.5933468507728));
#16151=CARTESIAN_POINT('Ctrl Pts',(24.6353896819943,19.1453760973014,47.50401144732));
#16152=CARTESIAN_POINT('Ctrl Pts',(24.6501791201489,19.1079235845375,47.4488825757172));
#16153=CARTESIAN_POINT('Ctrl Pts',(24.6702995226691,19.0578693331568,47.3272049658121));
#16154=CARTESIAN_POINT('Ctrl Pts',(24.6755295516031,19.045300072509,47.2606262015597));
#16155=CARTESIAN_POINT('Ctrl Pts',(24.6755295516031,19.045300072509,47.1978257430375));
#16156=CARTESIAN_POINT('',(26.2727417324721,24.92755355845,47.6978257430375));
#16157=CARTESIAN_POINT('Origin',(29.2994615223724,20.9477335482704,47.6978257430375));
#16158=CARTESIAN_POINT('',(26.8050928708948,25.2811069490433,48.5513791336308));
#16159=CARTESIAN_POINT('Ctrl Pts',(26.8050928708948,25.2811069490433,48.5513791336308));
#16160=CARTESIAN_POINT('Ctrl Pts',(26.82943543518,25.2951189723872,48.5373671102869));
#16161=CARTESIAN_POINT('Ctrl Pts',(26.8530498914274,25.308437537607,48.5223873647648));
#16162=CARTESIAN_POINT('Ctrl Pts',(26.9248328641831,25.348221870878,48.4716633740189));
#16163=CARTESIAN_POINT('Ctrl Pts',(26.9755840167052,25.3750874905218,48.4276121965828));
#16164=CARTESIAN_POINT('Ctrl Pts',(27.0333153241737,25.4047562084472,48.3496563433172));
#16165=CARTESIAN_POINT('Ctrl Pts',(27.0494846243196,25.4129061770103,48.3217082903646));
#16166=CARTESIAN_POINT('Ctrl Pts',(27.0722400173048,25.4242998143135,48.2623093314405));
#16167=CARTESIAN_POINT('Ctrl Pts',(27.078828127056,25.42755355845,48.2308611312278));
#16168=CARTESIAN_POINT('Ctrl Pts',(27.078828127056,25.42755355845,48.1978257430375));
#16169=CARTESIAN_POINT('Ctrl Pts',(27.078828127056,25.42755355845,48.1647903548472));
#16170=CARTESIAN_POINT('Ctrl Pts',(27.0722400173048,25.4242998143135,48.1333421546345));
#16171=CARTESIAN_POINT('Ctrl Pts',(27.0494846243196,25.4129061770103,48.0739431957104));
#16172=CARTESIAN_POINT('Ctrl Pts',(27.0333153241737,25.4047562084472,48.0459951427578));
#16173=CARTESIAN_POINT('Ctrl Pts',(26.9755840167052,25.3750874905218,47.9680392894922));
#16174=CARTESIAN_POINT('Ctrl Pts',(26.9248328641832,25.348221870878,47.9239881120561));
#16175=CARTESIAN_POINT('Ctrl Pts',(26.7868075959158,25.2717240182291,47.8264553384537));
#16176=CARTESIAN_POINT('Ctrl Pts',(26.6830441955061,25.2103549049237,47.7786797574698));
#16177=CARTESIAN_POINT('Ctrl Pts',(26.4736085973111,25.0744920557659,47.7140189797529));
#16178=CARTESIAN_POINT('Ctrl Pts',(26.3678144401405,24.9998579453427,47.6978257430375));
#16179=CARTESIAN_POINT('Ctrl Pts',(26.2727417324721,24.92755355845,47.6978257430375));
#16180=CARTESIAN_POINT('',(24.6113603597352,22.6860394732673,51.1464466094067));
#16181=CARTESIAN_POINT('Origin',(29.2994615223724,20.9477335482704,52.8847525344037));
#16182=CARTESIAN_POINT('',(24.7580823702008,23.0395928638606,52.));
#16183=CARTESIAN_POINT('Ctrl Pts',(24.7580823702008,23.0395928638606,52.));
#16184=CARTESIAN_POINT('Ctrl Pts',(24.7295403892111,22.9776288701721,52.));
#16185=CARTESIAN_POINT('Ctrl Pts',(24.7003039670753,22.9104700099307,51.9877768144645));
#16186=CARTESIAN_POINT('Ctrl Pts',(24.6488415484994,22.7852096676192,51.9357615493743));
#16187=CARTESIAN_POINT('Ctrl Pts',(24.6265540100987,22.7271564800506,51.8959141016255));
#16188=CARTESIAN_POINT('Ctrl Pts',(24.5939647498949,22.6389806710746,51.8052231982866));
#16189=CARTESIAN_POINT('Ctrl Pts',(24.5808795048891,22.6017210834816,51.7501423324695));
#16190=CARTESIAN_POINT('Ctrl Pts',(24.5637493585117,22.5520157275868,51.6287300770116));
#16191=CARTESIAN_POINT('Ctrl Pts',(24.5596319980784,22.5395928638606,51.5623995455887));
#16192=CARTESIAN_POINT('Ctrl Pts',(24.5596319980784,22.5395928638606,51.4376004544113));
#16193=CARTESIAN_POINT('Ctrl Pts',(24.5637493585117,22.5520157275868,51.3712699229884));
#16194=CARTESIAN_POINT('Ctrl Pts',(24.5808795048891,22.6017210834816,51.2498576675305));
#16195=CARTESIAN_POINT('Ctrl Pts',(24.5939647498949,22.6389806710746,51.1947768017134));
#16196=CARTESIAN_POINT('Ctrl Pts',(24.6101358897808,22.6827344516939,51.1497750043391));
#16197=CARTESIAN_POINT('Ctrl Pts',(24.610744984223,22.6843798444226,51.1481062382515));
#16198=CARTESIAN_POINT('Ctrl Pts',(24.6113603597352,22.6860394732673,51.1464466094067));
#16199=CARTESIAN_POINT('',(33.8408406745439,23.0395928638606,52.));
#16200=CARTESIAN_POINT('Origin',(29.2994615223724,20.9477335482704,52.));
#16201=CARTESIAN_POINT('',(33.9875626850096,22.6860394732673,51.1464466094067));
#16202=CARTESIAN_POINT('Ctrl Pts',(33.9875626850096,22.6860394732673,51.1464466094067));
#16203=CARTESIAN_POINT('Ctrl Pts',(33.9881780605218,22.6843798444226,51.1481062382515));
#16204=CARTESIAN_POINT('Ctrl Pts',(33.988787154964,22.6827344516939,51.1497750043391));
#16205=CARTESIAN_POINT('Ctrl Pts',(34.0049582948499,22.6389806710746,51.1947768017134));
#16206=CARTESIAN_POINT('Ctrl Pts',(34.0180435398556,22.6017210834816,51.2498576675305));
#16207=CARTESIAN_POINT('Ctrl Pts',(34.035173686233,22.5520157275868,51.3712699229884));
#16208=CARTESIAN_POINT('Ctrl Pts',(34.0392910466663,22.5395928638606,51.4376004544113));
#16209=CARTESIAN_POINT('Ctrl Pts',(34.0392910466663,22.5395928638606,51.5623995455887));
#16210=CARTESIAN_POINT('Ctrl Pts',(34.035173686233,22.5520157275868,51.6287300770116));
#16211=CARTESIAN_POINT('Ctrl Pts',(34.0180435398556,22.6017210834816,51.7501423324695));
#16212=CARTESIAN_POINT('Ctrl Pts',(34.0049582948499,22.6389806710746,51.8052231982866));
#16213=CARTESIAN_POINT('Ctrl Pts',(33.9723690346461,22.7271564800506,51.8959141016255));
#16214=CARTESIAN_POINT('Ctrl Pts',(33.9500814962454,22.7852096676192,51.9357615493743));
#16215=CARTESIAN_POINT('Ctrl Pts',(33.8986190776695,22.9104700099307,51.9877768144645));
#16216=CARTESIAN_POINT('Ctrl Pts',(33.8693826555337,22.9776288701721,52.));
#16217=CARTESIAN_POINT('Ctrl Pts',(33.8408406745439,23.0395928638606,52.));
#16218=CARTESIAN_POINT('',(31.79383017385,25.2811069490433,48.5513791336308));
#16219=CARTESIAN_POINT('Origin',(29.2994615223724,20.9477335482704,52.8847525344037));
#16220=CARTESIAN_POINT('',(32.3261813122727,24.92755355845,47.6978257430375));
#16221=CARTESIAN_POINT('Ctrl Pts',(32.3261813122727,24.92755355845,47.6978257430375));
#16222=CARTESIAN_POINT('Ctrl Pts',(32.2311086046043,24.9998579453427,47.6978257430375));
#16223=CARTESIAN_POINT('Ctrl Pts',(32.1253144474337,25.0744920557659,47.7140189797529));
#16224=CARTESIAN_POINT('Ctrl Pts',(31.9158788492386,25.2103549049237,47.7786797574698));
#16225=CARTESIAN_POINT('Ctrl Pts',(31.812115448829,25.2717240182291,47.8264553384537));
#16226=CARTESIAN_POINT('Ctrl Pts',(31.6740901805616,25.348221870878,47.9239881120561));
#16227=CARTESIAN_POINT('Ctrl Pts',(31.6233390280396,25.3750874905218,47.9680392894922));
#16228=CARTESIAN_POINT('Ctrl Pts',(31.5656077205711,25.4047562084472,48.0459951427578));
#16229=CARTESIAN_POINT('Ctrl Pts',(31.5494384204252,25.4129061770103,48.0739431957104));
#16230=CARTESIAN_POINT('Ctrl Pts',(31.5266830274399,25.4242998143135,48.1333421546345));
#16231=CARTESIAN_POINT('Ctrl Pts',(31.5200949176888,25.42755355845,48.1647903548472));
#16232=CARTESIAN_POINT('Ctrl Pts',(31.5200949176888,25.42755355845,48.1978257430375));
#16233=CARTESIAN_POINT('Ctrl Pts',(31.5200949176888,25.42755355845,48.2308611312278));
#16234=CARTESIAN_POINT('Ctrl Pts',(31.5266830274399,25.4242998143135,48.2623093314405));
#16235=CARTESIAN_POINT('Ctrl Pts',(31.5494384204251,25.4129061770103,48.3217082903646));
#16236=CARTESIAN_POINT('Ctrl Pts',(31.5656077205711,25.4047562084472,48.3496563433172));
#16237=CARTESIAN_POINT('Ctrl Pts',(31.6233390280396,25.3750874905218,48.4276121965828));
#16238=CARTESIAN_POINT('Ctrl Pts',(31.6740901805616,25.348221870878,48.4716633740189));
#16239=CARTESIAN_POINT('Ctrl Pts',(31.7458731531068,25.3084375377237,48.522387364616));
#16240=CARTESIAN_POINT('Ctrl Pts',(31.7694876094241,25.2951189724682,48.5373671102059));
#16241=CARTESIAN_POINT('Ctrl Pts',(31.79383017385,25.2811069490433,48.5513791336308));
#16242=CARTESIAN_POINT('Origin',(29.2994615223724,20.9477335482704,47.6978257430375));
#16243=CARTESIAN_POINT('Origin',(71.2994615223724,-45.9821613702938,64.));
#16244=CARTESIAN_POINT('',(83.7994615223724,-45.9821613702938,64.));
#16245=CARTESIAN_POINT('Origin',(71.2994615223724,-45.9821613702938,64.));
#16246=CARTESIAN_POINT('',(83.7994615223724,-45.9821613702938,52.));
#16247=CARTESIAN_POINT('',(83.7994615223724,-45.9821613702938,64.));
#16248=CARTESIAN_POINT('',(58.8166289045012,-45.3272645584125,52.));
#16249=CARTESIAN_POINT('Origin',(71.2994615223724,-45.9821613702938,52.));
#16250=CARTESIAN_POINT('',(58.8529273319278,-44.8272645584125,51.5));
#16251=CARTESIAN_POINT('Ctrl Pts',(58.8529273319278,-44.8272645584125,51.5));
#16252=CARTESIAN_POINT('Ctrl Pts',(58.8529273319278,-44.8272645584125,51.5628289407498));
#16253=CARTESIAN_POINT('Ctrl Pts',(58.8517413197398,-44.83983109791,51.6298216562663));
#16254=CARTESIAN_POINT('Ctrl Pts',(58.847162227239,-44.8908782000976,51.7530059059081));
#16255=CARTESIAN_POINT('Ctrl Pts',(58.843796823021,-44.9293569823108,51.8091992050848));
#16256=CARTESIAN_POINT('Ctrl Pts',(58.8366132516778,-45.0181089553366,51.8979511781107));
#16257=CARTESIAN_POINT('Ctrl Pts',(58.8323191872735,-45.0743219277052,51.936421701237));
#16258=CARTESIAN_POINT('Ctrl Pts',(58.8239610728064,-45.1974964800649,51.9874465324277));
#16259=CARTESIAN_POINT('Ctrl Pts',(58.8199238582361,-45.264460227701,52.));
#16260=CARTESIAN_POINT('Ctrl Pts',(58.8166289045012,-45.3272645584125,52.));
#16261=CARTESIAN_POINT('',(58.8529273319278,-44.8272645584125,48.1978257430375));
#16262=CARTESIAN_POINT('',(58.8529273319278,-44.8272645584125,64.));
#16263=CARTESIAN_POINT('Ctrl Pts',(58.9094931389573,-44.3272645584125,47.6978257430375));
#16264=CARTESIAN_POINT('Ctrl Pts',(58.9011336612411,-44.3898507353038,47.6978257430375));
#16265=CARTESIAN_POINT('Ctrl Pts',(58.8927334019429,-44.4567282803349,47.7102969796753));
#16266=CARTESIAN_POINT('Ctrl Pts',(58.8782032929536,-44.5799514130651,47.7612544377797));
#16267=CARTESIAN_POINT('Ctrl Pts',(58.872046708812,-44.636291625979,47.7997460294175));
#16268=CARTESIAN_POINT('Ctrl Pts',(58.8627467322493,-44.7251367458781,47.8885911493166));
#16269=CARTESIAN_POINT('Ctrl Pts',(58.8589701728764,-44.7636241839714,47.9447717029639));
#16270=CARTESIAN_POINT('Ctrl Pts',(58.8540741990285,-44.8146887744293,48.0679654140368));
#16271=CARTESIAN_POINT('Ctrl Pts',(58.8529273319278,-44.8272645584125,48.1349780461073));
#16272=CARTESIAN_POINT('Ctrl Pts',(58.8529273319278,-44.8272645584125,48.1978257430375));
#16273=CARTESIAN_POINT('',(83.745995712817,-44.8272645584125,48.1978257430375));
#16274=CARTESIAN_POINT('Ctrl Pts',(83.745995712817,-44.8272645584125,48.1978257430375));
#16275=CARTESIAN_POINT('Ctrl Pts',(83.745995712817,-44.8272645584125,48.1349780461073));
#16276=CARTESIAN_POINT('Ctrl Pts',(83.7448488457163,-44.8146887744293,48.0679654140368));
#16277=CARTESIAN_POINT('Ctrl Pts',(83.7399528718684,-44.7636241839714,47.9447717029639));
#16278=CARTESIAN_POINT('Ctrl Pts',(83.7361763124955,-44.7251367458782,47.8885911493166));
#16279=CARTESIAN_POINT('Ctrl Pts',(83.7268763359328,-44.636291625979,47.7997460294175));
#16280=CARTESIAN_POINT('Ctrl Pts',(83.7207197517911,-44.5799514130651,47.7612544377797));
#16281=CARTESIAN_POINT('Ctrl Pts',(83.7061896428019,-44.4567282803349,47.7102969796753));
#16282=CARTESIAN_POINT('Ctrl Pts',(83.6977893835036,-44.3898507353038,47.6978257430375));
#16283=CARTESIAN_POINT('Ctrl Pts',(83.6894299057875,-44.3272645584125,47.6978257430375));
#16284=CARTESIAN_POINT('',(83.745995712817,-44.8272645584125,51.5));
#16285=CARTESIAN_POINT('',(83.745995712817,-44.8272645584125,64.));
#16286=CARTESIAN_POINT('',(83.7822941402435,-45.3272645584125,52.));
#16287=CARTESIAN_POINT('Ctrl Pts',(83.7822941402435,-45.3272645584125,52.));
#16288=CARTESIAN_POINT('Ctrl Pts',(83.7789991865087,-45.264460227701,52.));
#16289=CARTESIAN_POINT('Ctrl Pts',(83.7749619719384,-45.1974964800649,51.9874465324277));
#16290=CARTESIAN_POINT('Ctrl Pts',(83.7666038574713,-45.0743219277052,51.936421701237));
#16291=CARTESIAN_POINT('Ctrl Pts',(83.762309793067,-45.0181089553366,51.8979511781107));
#16292=CARTESIAN_POINT('Ctrl Pts',(83.7551262217237,-44.9293569823108,51.8091992050848));
#16293=CARTESIAN_POINT('Ctrl Pts',(83.7517608175058,-44.8908782000976,51.7530059059081));
#16294=CARTESIAN_POINT('Ctrl Pts',(83.747181725005,-44.83983109791,51.6298216562663));
#16295=CARTESIAN_POINT('Ctrl Pts',(83.745995712817,-44.8272645584125,51.5628289407498));
#16296=CARTESIAN_POINT('Ctrl Pts',(83.745995712817,-44.8272645584125,51.5));
#16297=CARTESIAN_POINT('Origin',(71.2994615223724,-45.9821613702938,52.));
#16298=CARTESIAN_POINT('Origin',(71.2994615223724,20.9477335482704,64.));
#16299=CARTESIAN_POINT('',(76.2994615223724,20.9477335482704,64.));
#16300=CARTESIAN_POINT('Origin',(71.2994615223724,20.9477335482704,64.));
#16301=CARTESIAN_POINT('',(76.2994615223724,20.9477335482704,47.6978257430375));
#16302=CARTESIAN_POINT('',(76.2994615223724,20.9477335482704,64.));
#16303=CARTESIAN_POINT('',(76.0987510891795,19.545300072509,47.6978257430375));
#16304=CARTESIAN_POINT('Origin',(71.2994615223724,20.9477335482704,47.6978257430375));
#16305=CARTESIAN_POINT('',(75.9233934931417,19.045300072509,47.1978257430375));
#16306=CARTESIAN_POINT('Ctrl Pts',(75.9233934931417,19.045300072509,47.1978257430375));
#16307=CARTESIAN_POINT('Ctrl Pts',(75.9233934931417,19.045300072509,47.2606262015597));
#16308=CARTESIAN_POINT('Ctrl Pts',(75.9286235220756,19.0578693331568,47.3272049658121));
#16309=CARTESIAN_POINT('Ctrl Pts',(75.9487439245958,19.1079235845375,47.4488825757172));
#16310=CARTESIAN_POINT('Ctrl Pts',(75.9635333627505,19.1453760973014,47.50401144732));
#16311=CARTESIAN_POINT('Ctrl Pts',(75.9963894622215,19.2327496876229,47.5933468507728));
#16312=CARTESIAN_POINT('Ctrl Pts',(76.0169336674919,19.2894923661088,47.6326971370671));
#16313=CARTESIAN_POINT('Ctrl Pts',(76.0588328495999,19.4138848506455,47.6849404681153));
#16314=CARTESIAN_POINT('Ctrl Pts',(76.0801249019844,19.4815591055255,47.6978257430375));
#16315=CARTESIAN_POINT('Ctrl Pts',(76.0987510891795,19.545300072509,47.6978257430375));
#16316=CARTESIAN_POINT('',(75.9233934931417,19.045300072509,36.1978257430375));
#16317=CARTESIAN_POINT('',(75.9233934931417,19.045300072509,64.));
#16318=CARTESIAN_POINT('',(75.6844716015559,18.545300072509,35.6978257430375));
#16319=CARTESIAN_POINT('Ctrl Pts',(75.6844716015559,18.545300072509,35.6978257430375));
#16320=CARTESIAN_POINT('Ctrl Pts',(75.7183437123576,18.6071246969023,35.6978257430375));
#16321=CARTESIAN_POINT('Ctrl Pts',(75.7533284422121,18.6744087742691,35.7099831569546));
#16322=CARTESIAN_POINT('Ctrl Pts',(75.8154443123393,18.800447936422,35.7624419799854));
#16323=CARTESIAN_POINT('Ctrl Pts',(75.8426335478405,18.8591453590194,35.8028130850757));
#16324=CARTESIAN_POINT('Ctrl Pts',(75.8819451449858,18.9470131641942,35.8942412268742));
#16325=CARTESIAN_POINT('Ctrl Pts',(75.8976695801488,18.983759545124,35.9488335262825));
#16326=CARTESIAN_POINT('Ctrl Pts',(75.9183580123699,19.0329211748031,36.0694921472959));
#16327=CARTESIAN_POINT('Ctrl Pts',(75.9233934931417,19.045300072509,36.1355610097978));
#16328=CARTESIAN_POINT('Ctrl Pts',(75.9233934931417,19.045300072509,36.1978257430375));
#16329=CARTESIAN_POINT('',(66.9144514431889,18.545300072509,35.6978257430375));
#16330=CARTESIAN_POINT('Origin',(71.2994615223724,20.9477335482704,35.6978257430375));
#16331=CARTESIAN_POINT('',(66.6755295516031,19.045300072509,36.1978257430375));
#16332=CARTESIAN_POINT('Ctrl Pts',(66.6755295516031,19.045300072509,36.1978257430375));
#16333=CARTESIAN_POINT('Ctrl Pts',(66.6755295516031,19.045300072509,36.1355610097978));
#16334=CARTESIAN_POINT('Ctrl Pts',(66.6805650323748,19.0329211748031,36.0694921472959));
#16335=CARTESIAN_POINT('Ctrl Pts',(66.701253464596,18.983759545124,35.9488335262825));
#16336=CARTESIAN_POINT('Ctrl Pts',(66.716977899759,18.9470131641942,35.8942412268742));
#16337=CARTESIAN_POINT('Ctrl Pts',(66.7562894969043,18.8591453590194,35.8028130850757));
#16338=CARTESIAN_POINT('Ctrl Pts',(66.7834787324055,18.800447936422,35.7624419799854));
#16339=CARTESIAN_POINT('Ctrl Pts',(66.8455946025327,18.6744087742692,35.7099831569546));
#16340=CARTESIAN_POINT('Ctrl Pts',(66.8805793323872,18.6071246969023,35.6978257430375));
#16341=CARTESIAN_POINT('Ctrl Pts',(66.9144514431889,18.545300072509,35.6978257430375));
#16342=CARTESIAN_POINT('',(66.6755295516031,19.045300072509,47.1978257430375));
#16343=CARTESIAN_POINT('',(66.6755295516031,19.045300072509,64.));
#16344=CARTESIAN_POINT('',(66.5001719555652,19.545300072509,47.6978257430375));
#16345=CARTESIAN_POINT('Ctrl Pts',(66.5001719555652,19.545300072509,47.6978257430375));
#16346=CARTESIAN_POINT('Ctrl Pts',(66.5187981427604,19.4815591055255,47.6978257430375));
#16347=CARTESIAN_POINT('Ctrl Pts',(66.5400901951449,19.4138848506455,47.6849404681153));
#16348=CARTESIAN_POINT('Ctrl Pts',(66.5819893772529,19.2894923661088,47.6326971370671));
#16349=CARTESIAN_POINT('Ctrl Pts',(66.6025335825233,19.2327496876229,47.5933468507728));
#16350=CARTESIAN_POINT('Ctrl Pts',(66.6353896819943,19.1453760973014,47.50401144732));
#16351=CARTESIAN_POINT('Ctrl Pts',(66.6501791201489,19.1079235845375,47.4488825757172));
#16352=CARTESIAN_POINT('Ctrl Pts',(66.6702995226691,19.0578693331568,47.3272049658121));
#16353=CARTESIAN_POINT('Ctrl Pts',(66.6755295516031,19.045300072509,47.2606262015597));
#16354=CARTESIAN_POINT('Ctrl Pts',(66.6755295516031,19.045300072509,47.1978257430375));
#16355=CARTESIAN_POINT('',(68.2727417324721,24.92755355845,47.6978257430375));
#16356=CARTESIAN_POINT('Origin',(71.2994615223724,20.9477335482704,47.6978257430375));
#16357=CARTESIAN_POINT('',(68.8050928708948,25.2811069490433,48.5513791336308));
#16358=CARTESIAN_POINT('Ctrl Pts',(68.8050928708948,25.2811069490433,48.5513791336308));
#16359=CARTESIAN_POINT('Ctrl Pts',(68.8294354351799,25.2951189723872,48.5373671102869));
#16360=CARTESIAN_POINT('Ctrl Pts',(68.8530498914273,25.308437537607,48.5223873647648));
#16361=CARTESIAN_POINT('Ctrl Pts',(68.9248328641831,25.348221870878,48.4716633740189));
#16362=CARTESIAN_POINT('Ctrl Pts',(68.9755840167052,25.3750874905218,48.4276121965828));
#16363=CARTESIAN_POINT('Ctrl Pts',(69.0333153241737,25.4047562084472,48.3496563433172));
#16364=CARTESIAN_POINT('Ctrl Pts',(69.0494846243196,25.4129061770103,48.3217082903646));
#16365=CARTESIAN_POINT('Ctrl Pts',(69.0722400173048,25.4242998143135,48.2623093314405));
#16366=CARTESIAN_POINT('Ctrl Pts',(69.078828127056,25.42755355845,48.2308611312278));
#16367=CARTESIAN_POINT('Ctrl Pts',(69.078828127056,25.42755355845,48.1978257430375));
#16368=CARTESIAN_POINT('Ctrl Pts',(69.078828127056,25.42755355845,48.1647903548472));
#16369=CARTESIAN_POINT('Ctrl Pts',(69.0722400173048,25.4242998143135,48.1333421546345));
#16370=CARTESIAN_POINT('Ctrl Pts',(69.0494846243196,25.4129061770103,48.0739431957104));
#16371=CARTESIAN_POINT('Ctrl Pts',(69.0333153241737,25.4047562084472,48.0459951427578));
#16372=CARTESIAN_POINT('Ctrl Pts',(68.9755840167052,25.3750874905218,47.9680392894922));
#16373=CARTESIAN_POINT('Ctrl Pts',(68.9248328641831,25.348221870878,47.9239881120561));
#16374=CARTESIAN_POINT('Ctrl Pts',(68.7868075959158,25.2717240182291,47.8264553384537));
#16375=CARTESIAN_POINT('Ctrl Pts',(68.6830441955061,25.2103549049236,47.7786797574698));
#16376=CARTESIAN_POINT('Ctrl Pts',(68.4736085973111,25.0744920557659,47.7140189797529));
#16377=CARTESIAN_POINT('Ctrl Pts',(68.3678144401405,24.9998579453427,47.6978257430375));
#16378=CARTESIAN_POINT('Ctrl Pts',(68.2727417324721,24.92755355845,47.6978257430375));
#16379=CARTESIAN_POINT('',(66.6113603597352,22.6860394732673,51.1464466094067));
#16380=CARTESIAN_POINT('Origin',(71.2994615223724,20.9477335482704,52.8847525344037));
#16381=CARTESIAN_POINT('',(66.7580823702008,23.0395928638606,52.));
#16382=CARTESIAN_POINT('Ctrl Pts',(66.7580823702008,23.0395928638606,52.));
#16383=CARTESIAN_POINT('Ctrl Pts',(66.7295403892111,22.9776288701721,52.));
#16384=CARTESIAN_POINT('Ctrl Pts',(66.7003039670752,22.9104700099307,51.9877768144645));
#16385=CARTESIAN_POINT('Ctrl Pts',(66.6488415484994,22.7852096676192,51.9357615493743));
#16386=CARTESIAN_POINT('Ctrl Pts',(66.6265540100987,22.7271564800506,51.8959141016255));
#16387=CARTESIAN_POINT('Ctrl Pts',(66.5939647498949,22.6389806710746,51.8052231982866));
#16388=CARTESIAN_POINT('Ctrl Pts',(66.5808795048891,22.6017210834815,51.7501423324695));
#16389=CARTESIAN_POINT('Ctrl Pts',(66.5637493585117,22.5520157275868,51.6287300770116));
#16390=CARTESIAN_POINT('Ctrl Pts',(66.5596319980784,22.5395928638606,51.5623995455887));
#16391=CARTESIAN_POINT('Ctrl Pts',(66.5596319980784,22.5395928638606,51.4376004544113));
#16392=CARTESIAN_POINT('Ctrl Pts',(66.5637493585117,22.5520157275868,51.3712699229884));
#16393=CARTESIAN_POINT('Ctrl Pts',(66.5808795048891,22.6017210834815,51.2498576675305));
#16394=CARTESIAN_POINT('Ctrl Pts',(66.5939647498949,22.6389806710746,51.1947768017134));
#16395=CARTESIAN_POINT('Ctrl Pts',(66.6101358897808,22.6827344516939,51.1497750043391));
#16396=CARTESIAN_POINT('Ctrl Pts',(66.610744984223,22.6843798444226,51.1481062382515));
#16397=CARTESIAN_POINT('Ctrl Pts',(66.6113603597352,22.6860394732673,51.1464466094067));
#16398=CARTESIAN_POINT('',(75.840840674544,23.0395928638606,52.));
#16399=CARTESIAN_POINT('Origin',(71.2994615223724,20.9477335482704,52.));
#16400=CARTESIAN_POINT('',(75.9875626850096,22.6860394732673,51.1464466094067));
#16401=CARTESIAN_POINT('Ctrl Pts',(75.9875626850096,22.6860394732673,51.1464466094067));
#16402=CARTESIAN_POINT('Ctrl Pts',(75.9881780605218,22.6843798444226,51.1481062382515));
#16403=CARTESIAN_POINT('Ctrl Pts',(75.988787154964,22.6827344516939,51.1497750043391));
#16404=CARTESIAN_POINT('Ctrl Pts',(76.0049582948499,22.6389806710746,51.1947768017134));
#16405=CARTESIAN_POINT('Ctrl Pts',(76.0180435398557,22.6017210834815,51.2498576675305));
#16406=CARTESIAN_POINT('Ctrl Pts',(76.035173686233,22.5520157275867,51.3712699229885));
#16407=CARTESIAN_POINT('Ctrl Pts',(76.0392910466663,22.5395928638606,51.4376004544113));
#16408=CARTESIAN_POINT('Ctrl Pts',(76.0392910466663,22.5395928638606,51.5623995455887));
#16409=CARTESIAN_POINT('Ctrl Pts',(76.035173686233,22.5520157275868,51.6287300770116));
#16410=CARTESIAN_POINT('Ctrl Pts',(76.0180435398557,22.6017210834815,51.7501423324695));
#16411=CARTESIAN_POINT('Ctrl Pts',(76.0049582948499,22.6389806710746,51.8052231982866));
#16412=CARTESIAN_POINT('Ctrl Pts',(75.9723690346461,22.7271564800506,51.8959141016255));
#16413=CARTESIAN_POINT('Ctrl Pts',(75.9500814962454,22.7852096676192,51.9357615493743));
#16414=CARTESIAN_POINT('Ctrl Pts',(75.8986190776695,22.9104700099307,51.9877768144645));
#16415=CARTESIAN_POINT('Ctrl Pts',(75.8693826555337,22.9776288701721,52.));
#16416=CARTESIAN_POINT('Ctrl Pts',(75.840840674544,23.0395928638606,52.));
#16417=CARTESIAN_POINT('',(73.79383017385,25.2811069490433,48.5513791336308));
#16418=CARTESIAN_POINT('Origin',(71.2994615223724,20.9477335482704,52.8847525344037));
#16419=CARTESIAN_POINT('',(74.3261813122727,24.92755355845,47.6978257430375));
#16420=CARTESIAN_POINT('Ctrl Pts',(74.3261813122727,24.92755355845,47.6978257430375));
#16421=CARTESIAN_POINT('Ctrl Pts',(74.2311086046043,24.9998579453427,47.6978257430375));
#16422=CARTESIAN_POINT('Ctrl Pts',(74.1253144474337,25.0744920557659,47.7140189797529));
#16423=CARTESIAN_POINT('Ctrl Pts',(73.9158788492387,25.2103549049236,47.7786797574698));
#16424=CARTESIAN_POINT('Ctrl Pts',(73.812115448829,25.2717240182291,47.8264553384537));
#16425=CARTESIAN_POINT('Ctrl Pts',(73.6740901805616,25.348221870878,47.9239881120561));
#16426=CARTESIAN_POINT('Ctrl Pts',(73.6233390280396,25.3750874905218,47.9680392894922));
#16427=CARTESIAN_POINT('Ctrl Pts',(73.5656077205711,25.4047562084472,48.0459951427578));
#16428=CARTESIAN_POINT('Ctrl Pts',(73.5494384204252,25.4129061770103,48.0739431957104));
#16429=CARTESIAN_POINT('Ctrl Pts',(73.52668302744,25.4242998143135,48.1333421546345));
#16430=CARTESIAN_POINT('Ctrl Pts',(73.5200949176888,25.42755355845,48.1647903548472));
#16431=CARTESIAN_POINT('Ctrl Pts',(73.5200949176888,25.42755355845,48.1978257430375));
#16432=CARTESIAN_POINT('Ctrl Pts',(73.5200949176888,25.42755355845,48.2308611312278));
#16433=CARTESIAN_POINT('Ctrl Pts',(73.5266830274399,25.4242998143135,48.2623093314405));
#16434=CARTESIAN_POINT('Ctrl Pts',(73.5494384204251,25.4129061770103,48.3217082903646));
#16435=CARTESIAN_POINT('Ctrl Pts',(73.5656077205711,25.4047562084472,48.3496563433172));
#16436=CARTESIAN_POINT('Ctrl Pts',(73.6233390280396,25.3750874905218,48.4276121965828));
#16437=CARTESIAN_POINT('Ctrl Pts',(73.6740901805616,25.348221870878,48.4716633740189));
#16438=CARTESIAN_POINT('Ctrl Pts',(73.7458731531068,25.3084375377237,48.522387364616));
#16439=CARTESIAN_POINT('Ctrl Pts',(73.7694876094241,25.2951189724682,48.5373671102059));
#16440=CARTESIAN_POINT('Ctrl Pts',(73.79383017385,25.2811069490433,48.5513791336308));
#16441=CARTESIAN_POINT('Origin',(71.2994615223724,20.9477335482704,47.6978257430375));
#16442=CARTESIAN_POINT('Origin',(-12.7005384776276,20.9477335482704,64.));
#16443=CARTESIAN_POINT('',(-7.70053847762761,20.9477335482704,64.));
#16444=CARTESIAN_POINT('Origin',(-12.7005384776276,20.9477335482704,64.));
#16445=CARTESIAN_POINT('',(-7.70053847762761,20.9477335482704,47.6978257430375));
#16446=CARTESIAN_POINT('',(-7.70053847762761,20.9477335482704,64.));
#16447=CARTESIAN_POINT('',(-7.90124891082047,19.545300072509,47.6978257430375));
#16448=CARTESIAN_POINT('Origin',(-12.7005384776276,20.9477335482704,47.6978257430375));
#16449=CARTESIAN_POINT('',(-8.0766065068583,19.045300072509,47.1978257430375));
#16450=CARTESIAN_POINT('Ctrl Pts',(-8.0766065068583,19.045300072509,47.1978257430375));
#16451=CARTESIAN_POINT('Ctrl Pts',(-8.0766065068583,19.045300072509,47.2606262015597));
#16452=CARTESIAN_POINT('Ctrl Pts',(-8.07137647792435,19.0578693331568,47.3272049658121));
#16453=CARTESIAN_POINT('Ctrl Pts',(-8.05125607540415,19.1079235845375,47.4488825757172));
#16454=CARTESIAN_POINT('Ctrl Pts',(-8.03646663724948,19.1453760973014,47.50401144732));
#16455=CARTESIAN_POINT('Ctrl Pts',(-8.00361053777846,19.2327496876229,47.5933468507728));
#16456=CARTESIAN_POINT('Ctrl Pts',(-7.98306633250816,19.2894923661088,47.6326971370671));
#16457=CARTESIAN_POINT('Ctrl Pts',(-7.94116715040014,19.4138848506455,47.6849404681153));
#16458=CARTESIAN_POINT('Ctrl Pts',(-7.91987509801561,19.4815591055256,47.6978257430375));
#16459=CARTESIAN_POINT('Ctrl Pts',(-7.90124891082047,19.545300072509,47.6978257430375));
#16460=CARTESIAN_POINT('',(-8.0766065068583,19.045300072509,36.1978257430375));
#16461=CARTESIAN_POINT('',(-8.0766065068583,19.045300072509,64.));
#16462=CARTESIAN_POINT('',(-8.31552839844407,18.545300072509,35.6978257430375));
#16463=CARTESIAN_POINT('Ctrl Pts',(-8.31552839844407,18.545300072509,35.6978257430375));
#16464=CARTESIAN_POINT('Ctrl Pts',(-8.28165628764236,18.6071246969023,35.6978257430375));
#16465=CARTESIAN_POINT('Ctrl Pts',(-8.24667155778788,18.6744087742692,35.7099831569546));
#16466=CARTESIAN_POINT('Ctrl Pts',(-8.18455568766068,18.800447936422,35.7624419799854));
#16467=CARTESIAN_POINT('Ctrl Pts',(-8.15736645215949,18.8591453590194,35.8028130850757));
#16468=CARTESIAN_POINT('Ctrl Pts',(-8.11805485501417,18.9470131641943,35.8942412268742));
#16469=CARTESIAN_POINT('Ctrl Pts',(-8.10233041985118,18.983759545124,35.9488335262825));
#16470=CARTESIAN_POINT('Ctrl Pts',(-8.08164198763004,19.0329211748031,36.0694921472959));
#16471=CARTESIAN_POINT('Ctrl Pts',(-8.0766065068583,19.045300072509,36.1355610097978));
#16472=CARTESIAN_POINT('Ctrl Pts',(-8.0766065068583,19.045300072509,36.1978257430375));
#16473=CARTESIAN_POINT('',(-17.0855485568112,18.545300072509,35.6978257430375));
#16474=CARTESIAN_POINT('Origin',(-12.7005384776276,20.9477335482704,35.6978257430375));
#16475=CARTESIAN_POINT('',(-17.3244704483969,19.045300072509,36.1978257430375));
#16476=CARTESIAN_POINT('Ctrl Pts',(-17.3244704483969,19.045300072509,36.1978257430375));
#16477=CARTESIAN_POINT('Ctrl Pts',(-17.3244704483969,19.045300072509,36.1355610097978));
#16478=CARTESIAN_POINT('Ctrl Pts',(-17.3194349676252,19.0329211748031,36.0694921472959));
#16479=CARTESIAN_POINT('Ctrl Pts',(-17.298746535404,18.983759545124,35.9488335262825));
#16480=CARTESIAN_POINT('Ctrl Pts',(-17.2830221002411,18.9470131641943,35.8942412268742));
#16481=CARTESIAN_POINT('Ctrl Pts',(-17.2437105030957,18.8591453590194,35.8028130850757));
#16482=CARTESIAN_POINT('Ctrl Pts',(-17.2165212675945,18.800447936422,35.7624419799854));
#16483=CARTESIAN_POINT('Ctrl Pts',(-17.1544053974673,18.6744087742692,35.7099831569546));
#16484=CARTESIAN_POINT('Ctrl Pts',(-17.1194206676129,18.6071246969023,35.6978257430375));
#16485=CARTESIAN_POINT('Ctrl Pts',(-17.0855485568111,18.545300072509,35.6978257430375));
#16486=CARTESIAN_POINT('',(-17.3244704483969,19.045300072509,47.1978257430375));
#16487=CARTESIAN_POINT('',(-17.3244704483969,19.045300072509,64.));
#16488=CARTESIAN_POINT('',(-17.4998280444348,19.545300072509,47.6978257430375));
#16489=CARTESIAN_POINT('Ctrl Pts',(-17.4998280444348,19.545300072509,47.6978257430375));
#16490=CARTESIAN_POINT('Ctrl Pts',(-17.4812018572396,19.4815591055256,47.6978257430375));
#16491=CARTESIAN_POINT('Ctrl Pts',(-17.4599098048551,19.4138848506455,47.6849404681153));
#16492=CARTESIAN_POINT('Ctrl Pts',(-17.4180106227471,19.2894923661088,47.6326971370671));
#16493=CARTESIAN_POINT('Ctrl Pts',(-17.3974664174768,19.2327496876229,47.5933468507728));
#16494=CARTESIAN_POINT('Ctrl Pts',(-17.3646103180057,19.1453760973014,47.50401144732));
#16495=CARTESIAN_POINT('Ctrl Pts',(-17.3498208798511,19.1079235845375,47.4488825757172));
#16496=CARTESIAN_POINT('Ctrl Pts',(-17.3297004773309,19.0578693331568,47.3272049658121));
#16497=CARTESIAN_POINT('Ctrl Pts',(-17.3244704483969,19.045300072509,47.2606262015597));
#16498=CARTESIAN_POINT('Ctrl Pts',(-17.3244704483969,19.045300072509,47.1978257430375));
#16499=CARTESIAN_POINT('',(-15.7272582675279,24.92755355845,47.6978257430375));
#16500=CARTESIAN_POINT('Origin',(-12.7005384776276,20.9477335482704,47.6978257430375));
#16501=CARTESIAN_POINT('',(-15.1949071291052,25.2811069490433,48.5513791336308));
#16502=CARTESIAN_POINT('Ctrl Pts',(-15.1949071291052,25.2811069490433,48.5513791336308));
#16503=CARTESIAN_POINT('Ctrl Pts',(-15.17056456482,25.2951189723872,48.5373671102869));
#16504=CARTESIAN_POINT('Ctrl Pts',(-15.1469501085726,25.308437537607,48.5223873647648));
#16505=CARTESIAN_POINT('Ctrl Pts',(-15.0751671358168,25.348221870878,48.4716633740189));
#16506=CARTESIAN_POINT('Ctrl Pts',(-15.0244159832948,25.3750874905218,48.4276121965828));
#16507=CARTESIAN_POINT('Ctrl Pts',(-14.9666846758263,25.4047562084472,48.3496563433172));
#16508=CARTESIAN_POINT('Ctrl Pts',(-14.9505153756804,25.4129061770103,48.3217082903646));
#16509=CARTESIAN_POINT('Ctrl Pts',(-14.9277599826951,25.4242998143135,48.2623093314405));
#16510=CARTESIAN_POINT('Ctrl Pts',(-14.921171872944,25.42755355845,48.2308611312278));
#16511=CARTESIAN_POINT('Ctrl Pts',(-14.921171872944,25.42755355845,48.1978257430375));
#16512=CARTESIAN_POINT('Ctrl Pts',(-14.921171872944,25.42755355845,48.1647903548472));
#16513=CARTESIAN_POINT('Ctrl Pts',(-14.9277599826951,25.4242998143135,48.1333421546345));
#16514=CARTESIAN_POINT('Ctrl Pts',(-14.9505153756804,25.4129061770103,48.0739431957104));
#16515=CARTESIAN_POINT('Ctrl Pts',(-14.9666846758263,25.4047562084472,48.0459951427578));
#16516=CARTESIAN_POINT('Ctrl Pts',(-15.0244159832948,25.3750874905218,47.9680392894922));
#16517=CARTESIAN_POINT('Ctrl Pts',(-15.0751671358168,25.348221870878,47.9239881120561));
#16518=CARTESIAN_POINT('Ctrl Pts',(-15.2131924040842,25.2717240182291,47.8264553384537));
#16519=CARTESIAN_POINT('Ctrl Pts',(-15.3169558044939,25.2103549049237,47.7786797574698));
#16520=CARTESIAN_POINT('Ctrl Pts',(-15.5263914026889,25.0744920557659,47.7140189797529));
#16521=CARTESIAN_POINT('Ctrl Pts',(-15.6321855598595,24.9998579453427,47.6978257430375));
#16522=CARTESIAN_POINT('Ctrl Pts',(-15.7272582675279,24.92755355845,47.6978257430375));
#16523=CARTESIAN_POINT('',(-17.3886396402648,22.6860394732673,51.1464466094067));
#16524=CARTESIAN_POINT('Origin',(-12.7005384776276,20.9477335482704,52.8847525344037));
#16525=CARTESIAN_POINT('',(-17.2419176297992,23.0395928638606,52.));
#16526=CARTESIAN_POINT('Ctrl Pts',(-17.2419176297992,23.0395928638606,52.));
#16527=CARTESIAN_POINT('Ctrl Pts',(-17.2704596107889,22.9776288701721,52.));
#16528=CARTESIAN_POINT('Ctrl Pts',(-17.2996960329247,22.9104700099307,51.9877768144645));
#16529=CARTESIAN_POINT('Ctrl Pts',(-17.3511584515006,22.7852096676192,51.9357615493743));
#16530=CARTESIAN_POINT('Ctrl Pts',(-17.3734459899013,22.7271564800506,51.8959141016255));
#16531=CARTESIAN_POINT('Ctrl Pts',(-17.4060352501051,22.6389806710746,51.8052231982866));
#16532=CARTESIAN_POINT('Ctrl Pts',(-17.4191204951109,22.6017210834816,51.7501423324695));
#16533=CARTESIAN_POINT('Ctrl Pts',(-17.4362506414882,22.5520157275868,51.6287300770116));
#16534=CARTESIAN_POINT('Ctrl Pts',(-17.4403680019216,22.5395928638606,51.5623995455887));
#16535=CARTESIAN_POINT('Ctrl Pts',(-17.4403680019216,22.5395928638606,51.4376004544113));
#16536=CARTESIAN_POINT('Ctrl Pts',(-17.4362506414882,22.5520157275868,51.3712699229884));
#16537=CARTESIAN_POINT('Ctrl Pts',(-17.4191204951109,22.6017210834816,51.2498576675305));
#16538=CARTESIAN_POINT('Ctrl Pts',(-17.4060352501051,22.6389806710746,51.1947768017134));
#16539=CARTESIAN_POINT('Ctrl Pts',(-17.3898641102192,22.682734451694,51.1497750043391));
#16540=CARTESIAN_POINT('Ctrl Pts',(-17.389255015777,22.6843798444226,51.1481062382515));
#16541=CARTESIAN_POINT('Ctrl Pts',(-17.3886396402648,22.6860394732673,51.1464466094067));
#16542=CARTESIAN_POINT('',(-8.15915932545606,23.0395928638606,52.));
#16543=CARTESIAN_POINT('Origin',(-12.7005384776276,20.9477335482704,52.));
#16544=CARTESIAN_POINT('',(-8.01243731499038,22.6860394732673,51.1464466094067));
#16545=CARTESIAN_POINT('Ctrl Pts',(-8.01243731499038,22.6860394732673,51.1464466094067));
#16546=CARTESIAN_POINT('Ctrl Pts',(-8.0118219394782,22.6843798444226,51.1481062382515));
#16547=CARTESIAN_POINT('Ctrl Pts',(-8.01121284503603,22.682734451694,51.1497750043391));
#16548=CARTESIAN_POINT('Ctrl Pts',(-7.99504170515014,22.6389806710746,51.1947768017134));
#16549=CARTESIAN_POINT('Ctrl Pts',(-7.98195646014436,22.6017210834816,51.2498576675305));
#16550=CARTESIAN_POINT('Ctrl Pts',(-7.96482631376698,22.5520157275868,51.3712699229884));
#16551=CARTESIAN_POINT('Ctrl Pts',(-7.96070895333366,22.5395928638606,51.4376004544113));
#16552=CARTESIAN_POINT('Ctrl Pts',(-7.96070895333366,22.5395928638606,51.5623995455887));
#16553=CARTESIAN_POINT('Ctrl Pts',(-7.96482631376698,22.5520157275868,51.6287300770116));
#16554=CARTESIAN_POINT('Ctrl Pts',(-7.98195646014436,22.6017210834816,51.7501423324695));
#16555=CARTESIAN_POINT('Ctrl Pts',(-7.99504170515014,22.6389806710746,51.8052231982866));
#16556=CARTESIAN_POINT('Ctrl Pts',(-8.02763096535394,22.7271564800506,51.8959141016255));
#16557=CARTESIAN_POINT('Ctrl Pts',(-8.04991850375465,22.7852096676192,51.9357615493743));
#16558=CARTESIAN_POINT('Ctrl Pts',(-8.10138092233047,22.9104700099307,51.9877768144645));
#16559=CARTESIAN_POINT('Ctrl Pts',(-8.13061734446632,22.9776288701721,52.));
#16560=CARTESIAN_POINT('Ctrl Pts',(-8.15915932545606,23.0395928638606,52.));
#16561=CARTESIAN_POINT('',(-10.2061698261501,25.2811069490433,48.5513791336308));
#16562=CARTESIAN_POINT('Origin',(-12.7005384776276,20.9477335482704,52.8847525344037));
#16563=CARTESIAN_POINT('',(-9.67381868772735,24.92755355845,47.6978257430375));
#16564=CARTESIAN_POINT('Ctrl Pts',(-9.67381868772736,24.92755355845,47.6978257430375));
#16565=CARTESIAN_POINT('Ctrl Pts',(-9.76889139539571,24.9998579453427,47.6978257430375));
#16566=CARTESIAN_POINT('Ctrl Pts',(-9.87468555256633,25.0744920557659,47.7140189797529));
#16567=CARTESIAN_POINT('Ctrl Pts',(-10.0841211507614,25.2103549049237,47.7786797574698));
#16568=CARTESIAN_POINT('Ctrl Pts',(-10.187884551171,25.2717240182291,47.8264553384537));
#16569=CARTESIAN_POINT('Ctrl Pts',(-10.3259098194384,25.348221870878,47.9239881120561));
#16570=CARTESIAN_POINT('Ctrl Pts',(-10.3766609719604,25.3750874905218,47.9680392894922));
#16571=CARTESIAN_POINT('Ctrl Pts',(-10.434392279429,25.4047562084472,48.0459951427578));
#16572=CARTESIAN_POINT('Ctrl Pts',(-10.4505615795749,25.4129061770103,48.0739431957104));
#16573=CARTESIAN_POINT('Ctrl Pts',(-10.4733169725601,25.4242998143135,48.1333421546345));
#16574=CARTESIAN_POINT('Ctrl Pts',(-10.4799050823113,25.42755355845,48.1647903548472));
#16575=CARTESIAN_POINT('Ctrl Pts',(-10.4799050823113,25.42755355845,48.1978257430375));
#16576=CARTESIAN_POINT('Ctrl Pts',(-10.4799050823113,25.42755355845,48.2308611312278));
#16577=CARTESIAN_POINT('Ctrl Pts',(-10.4733169725601,25.4242998143135,48.2623093314405));
#16578=CARTESIAN_POINT('Ctrl Pts',(-10.4505615795749,25.4129061770103,48.3217082903646));
#16579=CARTESIAN_POINT('Ctrl Pts',(-10.434392279429,25.4047562084472,48.3496563433172));
#16580=CARTESIAN_POINT('Ctrl Pts',(-10.3766609719604,25.3750874905218,48.4276121965828));
#16581=CARTESIAN_POINT('Ctrl Pts',(-10.3259098194384,25.348221870878,48.4716633740189));
#16582=CARTESIAN_POINT('Ctrl Pts',(-10.2541268468932,25.3084375377237,48.522387364616));
#16583=CARTESIAN_POINT('Ctrl Pts',(-10.2305123905759,25.2951189724682,48.5373671102059));
#16584=CARTESIAN_POINT('Ctrl Pts',(-10.2061698261501,25.2811069490433,48.5513791336308));
#16585=CARTESIAN_POINT('Origin',(-12.7005384776276,20.9477335482704,47.6978257430375));
#16586=CARTESIAN_POINT('Origin',(-54.7005384776276,20.9477335482704,64.));
#16587=CARTESIAN_POINT('',(-49.7005384776276,20.9477335482704,64.));
#16588=CARTESIAN_POINT('Origin',(-54.7005384776276,20.9477335482704,64.));
#16589=CARTESIAN_POINT('',(-49.7005384776276,20.9477335482704,47.6978257430375));
#16590=CARTESIAN_POINT('',(-49.7005384776276,20.9477335482704,64.));
#16591=CARTESIAN_POINT('',(-49.9012489108205,19.5453000725091,47.6978257430375));
#16592=CARTESIAN_POINT('Origin',(-54.7005384776276,20.9477335482704,47.6978257430375));
#16593=CARTESIAN_POINT('',(-50.0766065068583,19.0453000725091,47.1978257430375));
#16594=CARTESIAN_POINT('Ctrl Pts',(-50.0766065068583,19.0453000725091,47.1978257430375));
#16595=CARTESIAN_POINT('Ctrl Pts',(-50.0766065068583,19.0453000725091,47.2606262015597));
#16596=CARTESIAN_POINT('Ctrl Pts',(-50.0713764779243,19.0578693331568,47.3272049658121));
#16597=CARTESIAN_POINT('Ctrl Pts',(-50.0512560754041,19.1079235845375,47.4488825757172));
#16598=CARTESIAN_POINT('Ctrl Pts',(-50.0364666372495,19.1453760973015,47.50401144732));
#16599=CARTESIAN_POINT('Ctrl Pts',(-50.0036105377785,19.2327496876229,47.5933468507728));
#16600=CARTESIAN_POINT('Ctrl Pts',(-49.9830663325081,19.2894923661088,47.6326971370671));
#16601=CARTESIAN_POINT('Ctrl Pts',(-49.9411671504001,19.4138848506455,47.6849404681153));
#16602=CARTESIAN_POINT('Ctrl Pts',(-49.9198750980156,19.4815591055256,47.6978257430375));
#16603=CARTESIAN_POINT('Ctrl Pts',(-49.9012489108205,19.5453000725091,47.6978257430375));
#16604=CARTESIAN_POINT('',(-50.0766065068583,19.0453000725091,36.1978257430375));
#16605=CARTESIAN_POINT('',(-50.0766065068583,19.0453000725091,64.));
#16606=CARTESIAN_POINT('',(-50.3155283984441,18.5453000725091,35.6978257430375));
#16607=CARTESIAN_POINT('Ctrl Pts',(-50.3155283984441,18.5453000725091,35.6978257430375));
#16608=CARTESIAN_POINT('Ctrl Pts',(-50.2816562876424,18.6071246969023,35.6978257430375));
#16609=CARTESIAN_POINT('Ctrl Pts',(-50.2466715577879,18.6744087742692,35.7099831569546));
#16610=CARTESIAN_POINT('Ctrl Pts',(-50.1845556876607,18.800447936422,35.7624419799854));
#16611=CARTESIAN_POINT('Ctrl Pts',(-50.1573664521595,18.8591453590194,35.8028130850757));
#16612=CARTESIAN_POINT('Ctrl Pts',(-50.1180548550142,18.9470131641943,35.8942412268742));
#16613=CARTESIAN_POINT('Ctrl Pts',(-50.1023304198512,18.9837595451241,35.9488335262825));
#16614=CARTESIAN_POINT('Ctrl Pts',(-50.08164198763,19.0329211748031,36.0694921472959));
#16615=CARTESIAN_POINT('Ctrl Pts',(-50.0766065068583,19.0453000725091,36.1355610097978));
#16616=CARTESIAN_POINT('Ctrl Pts',(-50.0766065068583,19.0453000725091,36.1978257430375));
#16617=CARTESIAN_POINT('',(-59.0855485568112,18.5453000725091,35.6978257430375));
#16618=CARTESIAN_POINT('Origin',(-54.7005384776276,20.9477335482704,35.6978257430375));
#16619=CARTESIAN_POINT('',(-59.3244704483969,19.0453000725091,36.1978257430375));
#16620=CARTESIAN_POINT('Ctrl Pts',(-59.3244704483969,19.0453000725091,36.1978257430375));
#16621=CARTESIAN_POINT('Ctrl Pts',(-59.3244704483969,19.0453000725091,36.1355610097978));
#16622=CARTESIAN_POINT('Ctrl Pts',(-59.3194349676252,19.0329211748031,36.0694921472959));
#16623=CARTESIAN_POINT('Ctrl Pts',(-59.298746535404,18.9837595451241,35.9488335262825));
#16624=CARTESIAN_POINT('Ctrl Pts',(-59.2830221002411,18.9470131641943,35.8942412268742));
#16625=CARTESIAN_POINT('Ctrl Pts',(-59.2437105030957,18.8591453590194,35.8028130850757));
#16626=CARTESIAN_POINT('Ctrl Pts',(-59.2165212675946,18.800447936422,35.7624419799854));
#16627=CARTESIAN_POINT('Ctrl Pts',(-59.1544053974674,18.6744087742692,35.7099831569546));
#16628=CARTESIAN_POINT('Ctrl Pts',(-59.1194206676129,18.6071246969023,35.6978257430375));
#16629=CARTESIAN_POINT('Ctrl Pts',(-59.0855485568112,18.5453000725091,35.6978257430375));
#16630=CARTESIAN_POINT('',(-59.3244704483969,19.0453000725091,47.1978257430375));
#16631=CARTESIAN_POINT('',(-59.3244704483969,19.0453000725091,64.));
#16632=CARTESIAN_POINT('',(-59.4998280444348,19.5453000725091,47.6978257430375));
#16633=CARTESIAN_POINT('Ctrl Pts',(-59.4998280444348,19.5453000725091,47.6978257430375));
#16634=CARTESIAN_POINT('Ctrl Pts',(-59.4812018572396,19.4815591055256,47.6978257430375));
#16635=CARTESIAN_POINT('Ctrl Pts',(-59.4599098048551,19.4138848506455,47.6849404681153));
#16636=CARTESIAN_POINT('Ctrl Pts',(-59.4180106227471,19.2894923661088,47.6326971370671));
#16637=CARTESIAN_POINT('Ctrl Pts',(-59.3974664174768,19.2327496876229,47.5933468507728));
#16638=CARTESIAN_POINT('Ctrl Pts',(-59.3646103180058,19.1453760973015,47.50401144732));
#16639=CARTESIAN_POINT('Ctrl Pts',(-59.3498208798511,19.1079235845375,47.4488825757172));
#16640=CARTESIAN_POINT('Ctrl Pts',(-59.3297004773309,19.0578693331568,47.3272049658121));
#16641=CARTESIAN_POINT('Ctrl Pts',(-59.3244704483969,19.0453000725091,47.2606262015597));
#16642=CARTESIAN_POINT('Ctrl Pts',(-59.3244704483969,19.0453000725091,47.1978257430375));
#16643=CARTESIAN_POINT('',(-57.7272582675279,24.92755355845,47.6978257430375));
#16644=CARTESIAN_POINT('Origin',(-54.7005384776276,20.9477335482704,47.6978257430375));
#16645=CARTESIAN_POINT('',(-57.1949071291051,25.2811069490433,48.5513791336308));
#16646=CARTESIAN_POINT('Ctrl Pts',(-57.1949071291051,25.2811069490433,48.5513791336308));
#16647=CARTESIAN_POINT('Ctrl Pts',(-57.17056456482,25.2951189723872,48.5373671102869));
#16648=CARTESIAN_POINT('Ctrl Pts',(-57.1469501085726,25.308437537607,48.5223873647648));
#16649=CARTESIAN_POINT('Ctrl Pts',(-57.0751671358168,25.348221870878,48.4716633740189));
#16650=CARTESIAN_POINT('Ctrl Pts',(-57.0244159832948,25.3750874905218,48.4276121965828));
#16651=CARTESIAN_POINT('Ctrl Pts',(-56.9666846758262,25.4047562084472,48.3496563433172));
#16652=CARTESIAN_POINT('Ctrl Pts',(-56.9505153756803,25.4129061770103,48.3217082903646));
#16653=CARTESIAN_POINT('Ctrl Pts',(-56.9277599826951,25.4242998143135,48.2623093314405));
#16654=CARTESIAN_POINT('Ctrl Pts',(-56.9211718729439,25.42755355845,48.2308611312278));
#16655=CARTESIAN_POINT('Ctrl Pts',(-56.9211718729439,25.42755355845,48.1978257430375));
#16656=CARTESIAN_POINT('Ctrl Pts',(-56.9211718729439,25.42755355845,48.1647903548472));
#16657=CARTESIAN_POINT('Ctrl Pts',(-56.9277599826951,25.4242998143135,48.1333421546345));
#16658=CARTESIAN_POINT('Ctrl Pts',(-56.9505153756803,25.4129061770103,48.0739431957104));
#16659=CARTESIAN_POINT('Ctrl Pts',(-56.9666846758262,25.4047562084472,48.0459951427578));
#16660=CARTESIAN_POINT('Ctrl Pts',(-57.0244159832948,25.3750874905218,47.9680392894922));
#16661=CARTESIAN_POINT('Ctrl Pts',(-57.0751671358168,25.348221870878,47.9239881120561));
#16662=CARTESIAN_POINT('Ctrl Pts',(-57.2131924040842,25.2717240182291,47.8264553384537));
#16663=CARTESIAN_POINT('Ctrl Pts',(-57.3169558044938,25.2103549049237,47.7786797574698));
#16664=CARTESIAN_POINT('Ctrl Pts',(-57.5263914026889,25.0744920557659,47.7140189797529));
#16665=CARTESIAN_POINT('Ctrl Pts',(-57.6321855598595,24.9998579453427,47.6978257430375));
#16666=CARTESIAN_POINT('Ctrl Pts',(-57.7272582675279,24.92755355845,47.6978257430375));
#16667=CARTESIAN_POINT('',(-59.3886396402648,22.6860394732673,51.1464466094067));
#16668=CARTESIAN_POINT('Origin',(-54.7005384776276,20.9477335482704,52.8847525344037));
#16669=CARTESIAN_POINT('',(-59.2419176297992,23.0395928638606,52.));
#16670=CARTESIAN_POINT('Ctrl Pts',(-59.2419176297992,23.0395928638606,52.));
#16671=CARTESIAN_POINT('Ctrl Pts',(-59.2704596107889,22.9776288701721,52.));
#16672=CARTESIAN_POINT('Ctrl Pts',(-59.2996960329248,22.9104700099307,51.9877768144645));
#16673=CARTESIAN_POINT('Ctrl Pts',(-59.3511584515006,22.7852096676192,51.9357615493743));
#16674=CARTESIAN_POINT('Ctrl Pts',(-59.3734459899013,22.7271564800506,51.8959141016255));
#16675=CARTESIAN_POINT('Ctrl Pts',(-59.4060352501051,22.6389806710746,51.8052231982866));
#16676=CARTESIAN_POINT('Ctrl Pts',(-59.4191204951109,22.6017210834816,51.7501423324695));
#16677=CARTESIAN_POINT('Ctrl Pts',(-59.4362506414883,22.5520157275868,51.6287300770116));
#16678=CARTESIAN_POINT('Ctrl Pts',(-59.4403680019216,22.5395928638606,51.5623995455887));
#16679=CARTESIAN_POINT('Ctrl Pts',(-59.4403680019216,22.5395928638606,51.4376004544113));
#16680=CARTESIAN_POINT('Ctrl Pts',(-59.4362506414883,22.5520157275868,51.3712699229884));
#16681=CARTESIAN_POINT('Ctrl Pts',(-59.4191204951109,22.6017210834816,51.2498576675305));
#16682=CARTESIAN_POINT('Ctrl Pts',(-59.4060352501051,22.6389806710747,51.1947768017135));
#16683=CARTESIAN_POINT('Ctrl Pts',(-59.3898641102192,22.682734451694,51.1497750043391));
#16684=CARTESIAN_POINT('Ctrl Pts',(-59.389255015777,22.6843798444226,51.1481062382515));
#16685=CARTESIAN_POINT('Ctrl Pts',(-59.3886396402648,22.6860394732673,51.1464466094067));
#16686=CARTESIAN_POINT('',(-50.1591593254561,23.0395928638606,52.));
#16687=CARTESIAN_POINT('Origin',(-54.7005384776276,20.9477335482704,52.));
#16688=CARTESIAN_POINT('',(-50.0124373149904,22.6860394732673,51.1464466094067));
#16689=CARTESIAN_POINT('Ctrl Pts',(-50.0124373149904,22.6860394732673,51.1464466094067));
#16690=CARTESIAN_POINT('Ctrl Pts',(-50.0118219394782,22.6843798444226,51.1481062382515));
#16691=CARTESIAN_POINT('Ctrl Pts',(-50.011212845036,22.682734451694,51.1497750043391));
#16692=CARTESIAN_POINT('Ctrl Pts',(-49.9950417051501,22.6389806710746,51.1947768017134));
#16693=CARTESIAN_POINT('Ctrl Pts',(-49.9819564601444,22.6017210834816,51.2498576675305));
#16694=CARTESIAN_POINT('Ctrl Pts',(-49.964826313767,22.5520157275868,51.3712699229884));
#16695=CARTESIAN_POINT('Ctrl Pts',(-49.9607089533337,22.5395928638606,51.4376004544113));
#16696=CARTESIAN_POINT('Ctrl Pts',(-49.9607089533337,22.5395928638606,51.5623995455887));
#16697=CARTESIAN_POINT('Ctrl Pts',(-49.964826313767,22.5520157275868,51.6287300770116));
#16698=CARTESIAN_POINT('Ctrl Pts',(-49.9819564601444,22.6017210834816,51.7501423324695));
#16699=CARTESIAN_POINT('Ctrl Pts',(-49.9950417051502,22.6389806710747,51.8052231982866));
#16700=CARTESIAN_POINT('Ctrl Pts',(-50.0276309653539,22.7271564800506,51.8959141016255));
#16701=CARTESIAN_POINT('Ctrl Pts',(-50.0499185037546,22.7852096676192,51.9357615493743));
#16702=CARTESIAN_POINT('Ctrl Pts',(-50.1013809223305,22.9104700099307,51.9877768144645));
#16703=CARTESIAN_POINT('Ctrl Pts',(-50.1306173444663,22.9776288701721,52.));
#16704=CARTESIAN_POINT('Ctrl Pts',(-50.1591593254561,23.0395928638606,52.));
#16705=CARTESIAN_POINT('',(-52.2061698261501,25.2811069490433,48.5513791336308));
#16706=CARTESIAN_POINT('Origin',(-54.7005384776276,20.9477335482704,52.8847525344037));
#16707=CARTESIAN_POINT('',(-51.6738186877274,24.92755355845,47.6978257430375));
#16708=CARTESIAN_POINT('Ctrl Pts',(-51.6738186877274,24.92755355845,47.6978257430375));
#16709=CARTESIAN_POINT('Ctrl Pts',(-51.7688913953957,24.9998579453427,47.6978257430375));
#16710=CARTESIAN_POINT('Ctrl Pts',(-51.8746855525663,25.0744920557659,47.7140189797529));
#16711=CARTESIAN_POINT('Ctrl Pts',(-52.0841211507614,25.2103549049237,47.7786797574698));
#16712=CARTESIAN_POINT('Ctrl Pts',(-52.1878845511711,25.2717240182291,47.8264553384537));
#16713=CARTESIAN_POINT('Ctrl Pts',(-52.3259098194384,25.348221870878,47.9239881120561));
#16714=CARTESIAN_POINT('Ctrl Pts',(-52.3766609719605,25.3750874905218,47.9680392894922));
#16715=CARTESIAN_POINT('Ctrl Pts',(-52.434392279429,25.4047562084472,48.0459951427578));
#16716=CARTESIAN_POINT('Ctrl Pts',(-52.4505615795749,25.4129061770103,48.0739431957104));
#16717=CARTESIAN_POINT('Ctrl Pts',(-52.4733169725601,25.4242998143135,48.1333421546345));
#16718=CARTESIAN_POINT('Ctrl Pts',(-52.4799050823113,25.42755355845,48.1647903548472));
#16719=CARTESIAN_POINT('Ctrl Pts',(-52.4799050823113,25.42755355845,48.1978257430375));
#16720=CARTESIAN_POINT('Ctrl Pts',(-52.4799050823113,25.42755355845,48.2308611312278));
#16721=CARTESIAN_POINT('Ctrl Pts',(-52.4733169725601,25.4242998143135,48.2623093314405));
#16722=CARTESIAN_POINT('Ctrl Pts',(-52.4505615795749,25.4129061770103,48.3217082903646));
#16723=CARTESIAN_POINT('Ctrl Pts',(-52.434392279429,25.4047562084472,48.3496563433172));
#16724=CARTESIAN_POINT('Ctrl Pts',(-52.3766609719605,25.3750874905218,48.4276121965828));
#16725=CARTESIAN_POINT('Ctrl Pts',(-52.3259098194384,25.348221870878,48.4716633740189));
#16726=CARTESIAN_POINT('Ctrl Pts',(-52.2541268468932,25.3084375377237,48.522387364616));
#16727=CARTESIAN_POINT('Ctrl Pts',(-52.2305123905759,25.2951189724682,48.5373671102059));
#16728=CARTESIAN_POINT('Ctrl Pts',(-52.2061698261501,25.2811069490433,48.5513791336308));
#16729=CARTESIAN_POINT('Origin',(-54.7005384776276,20.9477335482704,47.6978257430375));
#16730=CARTESIAN_POINT('Origin',(8.29946152237238,41.9477335482704,64.));
#16731=CARTESIAN_POINT('',(13.2994615223724,41.9477335482704,64.));
#16732=CARTESIAN_POINT('Origin',(8.29946152237238,41.9477335482704,64.));
#16733=CARTESIAN_POINT('',(13.2994615223724,41.9477335482704,52.));
#16734=CARTESIAN_POINT('',(13.2994615223724,41.9477335482704,64.));
#16735=CARTESIAN_POINT('Origin',(8.29946152237238,41.9477335482704,52.));
#16736=CARTESIAN_POINT('Origin',(-33.7005384776276,-41.9477335482704,64.));
#16737=CARTESIAN_POINT('',(-28.7005384776276,-41.9477335482704,64.));
#16738=CARTESIAN_POINT('Origin',(-33.7005384776276,-41.9477335482704,64.));
#16739=CARTESIAN_POINT('',(-28.7005384776276,-41.9477335482704,64.));
#16740=CARTESIAN_POINT('',(-29.612959590116,-44.8272645584125,48.1978257430375));
#16741=CARTESIAN_POINT('Ctrl Pts',(-29.612959590116,-44.8272645584125,48.1978257430375));
#16742=CARTESIAN_POINT('Ctrl Pts',(-29.612959590116,-44.8272645584125,48.1321584122493));
#16743=CARTESIAN_POINT('Ctrl Pts',(-29.6032015594757,-44.8135380049881,
48.0636994127672));
#16744=CARTESIAN_POINT('Ctrl Pts',(-29.5671921138605,-44.7613527165994,
47.9408836439009));
#16745=CARTESIAN_POINT('Ctrl Pts',(-29.5411446978572,-44.7229773515989,
47.8864317550374));
#16746=CARTESIAN_POINT('Ctrl Pts',(-29.483890379582,-44.6352673224994,47.7987217259379));
#16747=CARTESIAN_POINT('Ctrl Pts',(-29.4481192034526,-44.5787128115292,
47.7605853033887));
#16748=CARTESIAN_POINT('Ctrl Pts',(-29.3745620549058,-44.4559300231491,
47.710126421675));
#16749=CARTESIAN_POINT('Ctrl Pts',(-29.3368235722438,-44.3896643528756,
47.6978257430375));
#16750=CARTESIAN_POINT('Ctrl Pts',(-29.3030582705349,-44.3272645584124,
47.6978257430375));
#16751=CARTESIAN_POINT('',(-29.612959590116,-44.8272645584124,51.5));
#16752=CARTESIAN_POINT('',(-29.612959590116,-44.8272645584125,64.));
#16753=CARTESIAN_POINT('',(-30.0156001943604,-45.3272645584124,52.));
#16754=CARTESIAN_POINT('Ctrl Pts',(-30.0156001943604,-45.3272645584124,
52.));
#16755=CARTESIAN_POINT('Ctrl Pts',(-29.9626248485631,-45.269501845417,52.));
#16756=CARTESIAN_POINT('Ctrl Pts',(-29.90662334431,-45.2054409446566,51.9894566895945));
#16757=CARTESIAN_POINT('Ctrl Pts',(-29.8039582965593,-45.0819180329636,
51.9406971089121));
#16758=CARTESIAN_POINT('Ctrl Pts',(-29.7572642176841,-45.0225259231798,
51.9023681459539));
#16759=CARTESIAN_POINT('Ctrl Pts',(-29.6887928314324,-44.9324583590974,
51.8123005818715));
#16760=CARTESIAN_POINT('Ctrl Pts',(-29.6606197247029,-44.8939359317371,
51.7582688558033));
#16761=CARTESIAN_POINT('Ctrl Pts',(-29.622738109016,-44.8412774147571,51.6352518100092));
#16762=CARTESIAN_POINT('Ctrl Pts',(-29.612959590116,-44.8272645584124,51.5662353407203));
#16763=CARTESIAN_POINT('Ctrl Pts',(-29.612959590116,-44.8272645584124,51.5));
#16764=CARTESIAN_POINT('',(-37.3854767608948,-45.3272645584124,52.));
#16765=CARTESIAN_POINT('Origin',(-33.7005384776276,-41.9477335482704,52.));
#16766=CARTESIAN_POINT('',(-37.7881173651392,-44.8272645584124,51.5));
#16767=CARTESIAN_POINT('Ctrl Pts',(-37.7881173651392,-44.8272645584124,
51.5));
#16768=CARTESIAN_POINT('Ctrl Pts',(-37.7881173651392,-44.8272645584124,
51.5662353407203));
#16769=CARTESIAN_POINT('Ctrl Pts',(-37.7783388462392,-44.8412774147571,
51.6352518100092));
#16770=CARTESIAN_POINT('Ctrl Pts',(-37.7404572305523,-44.8939359317371,
51.7582688558033));
#16771=CARTESIAN_POINT('Ctrl Pts',(-37.7122841238229,-44.9324583590974,
51.8123005818715));
#16772=CARTESIAN_POINT('Ctrl Pts',(-37.6438127375711,-45.0225259231798,
51.9023681459539));
#16773=CARTESIAN_POINT('Ctrl Pts',(-37.5971186586959,-45.0819180329636,
51.9406971089121));
#16774=CARTESIAN_POINT('Ctrl Pts',(-37.4944536109452,-45.2054409446566,
51.9894566895945));
#16775=CARTESIAN_POINT('Ctrl Pts',(-37.4384521066922,-45.269501845417,52.));
#16776=CARTESIAN_POINT('Ctrl Pts',(-37.3854767608948,-45.3272645584124,
52.));
#16777=CARTESIAN_POINT('',(-37.7881173651392,-44.8272645584125,48.1978257430375));
#16778=CARTESIAN_POINT('',(-37.7881173651392,-44.8272645584125,64.));
#16779=CARTESIAN_POINT('Ctrl Pts',(-38.0980186847204,-44.3272645584124,
47.6978257430375));
#16780=CARTESIAN_POINT('Ctrl Pts',(-38.0642533830114,-44.3896643528756,
47.6978257430375));
#16781=CARTESIAN_POINT('Ctrl Pts',(-38.0265149003494,-44.4559300231491,
47.710126421675));
#16782=CARTESIAN_POINT('Ctrl Pts',(-37.9529577518027,-44.5787128115292,
47.7605853033887));
#16783=CARTESIAN_POINT('Ctrl Pts',(-37.9171865756733,-44.6352673224994,
47.7987217259379));
#16784=CARTESIAN_POINT('Ctrl Pts',(-37.859932257398,-44.7229773515989,47.8864317550374));
#16785=CARTESIAN_POINT('Ctrl Pts',(-37.8338848413947,-44.7613527165994,
47.9408836439009));
#16786=CARTESIAN_POINT('Ctrl Pts',(-37.7978753957795,-44.8135380049881,
48.0636994127672));
#16787=CARTESIAN_POINT('Ctrl Pts',(-37.7881173651392,-44.8272645584124,
48.1321584122493));
#16788=CARTESIAN_POINT('Ctrl Pts',(-37.7881173651392,-44.8272645584124,
48.1978257430375));
#16789=CARTESIAN_POINT('Origin',(-90.,-22.0741207385023,47.1978257430375));
#16790=CARTESIAN_POINT('',(-90.,-21.5741207385023,47.1978257430375));
#16791=CARTESIAN_POINT('Origin',(-90.,-22.0741207385023,47.1978257430375));
#16792=CARTESIAN_POINT('',(-89.5,-21.5741207385023,47.1978257430375));
#16793=CARTESIAN_POINT('Origin',(-89.5,-22.0741207385023,47.1978257430375));
#16794=CARTESIAN_POINT('',(-90.,-21.5741207385023,47.1978257430375));
#16795=CARTESIAN_POINT('Origin',(-90.,-22.0741207385023,47.1978257430375));
#16796=CARTESIAN_POINT('',(-90.,-21.5741207385023,47.1978257430375));
#16797=CARTESIAN_POINT('Origin',(-90.,-22.0741207385023,47.1978257430375));
#16798=CARTESIAN_POINT('',(89.5,-21.5741207385024,47.1978257430375));
#16799=CARTESIAN_POINT('',(-90.,-21.5741207385023,47.1978257430375));
#16800=CARTESIAN_POINT('Origin',(89.5,-22.0741207385024,47.1978257430375));
#16801=CARTESIAN_POINT('Origin',(-90.,-22.0741207385023,47.1978257430375));
#16802=CARTESIAN_POINT('',(-90.,-21.5741207385023,47.1978257430375));
#16803=CARTESIAN_POINT('Origin',(-90.,-21.5741207385023,35.6978257430375));
#16804=CARTESIAN_POINT('',(89.5,-21.5741207385024,36.1978257430375));
#16805=CARTESIAN_POINT('',(-90.,-21.5741207385023,36.1978257430375));
#16806=CARTESIAN_POINT('',(89.5,-21.5741207385024,43.8489128715187));
#16807=CARTESIAN_POINT('Origin',(-90.,-21.5741207385023,35.6978257430375));
#16808=CARTESIAN_POINT('',(-90.,-21.5741207385023,36.1978257430375));
#16809=CARTESIAN_POINT('Origin',(-90.,-21.5741207385023,35.6978257430375));
#16810=CARTESIAN_POINT('',(-89.5,-21.5741207385023,36.1978257430375));
#16811=CARTESIAN_POINT('',(-89.5,-21.5741207385023,43.8489128715187));
#16812=CARTESIAN_POINT('',(-90.,-21.5741207385023,36.1978257430375));
#16813=CARTESIAN_POINT('Origin',(-90.,-21.5741207385023,35.6978257430375));
#16814=CARTESIAN_POINT('',(-90.,-21.5741207385023,36.1978257430375));
#16815=CARTESIAN_POINT('Origin',(-90.,-21.0741207385023,36.1978257430375));
#16816=CARTESIAN_POINT('',(-90.,-21.0741207385023,35.6978257430375));
#16817=CARTESIAN_POINT('Origin',(-90.,-21.0741207385023,36.1978257430375));
#16818=CARTESIAN_POINT('',(-89.5,-21.0741207385023,35.6978257430375));
#16819=CARTESIAN_POINT('Origin',(-89.5,-21.0741207385023,36.1978257430375));
#16820=CARTESIAN_POINT('',(-90.,-21.0741207385023,35.6978257430375));
#16821=CARTESIAN_POINT('Origin',(-90.,-21.0741207385023,36.1978257430375));
#16822=CARTESIAN_POINT('',(-90.,-21.0741207385023,35.6978257430375));
#16823=CARTESIAN_POINT('Origin',(-90.,-21.0741207385023,36.1978257430375));
#16824=CARTESIAN_POINT('',(89.5,-21.0741207385024,35.6978257430375));
#16825=CARTESIAN_POINT('',(-90.,-21.0741207385023,35.6978257430375));
#16826=CARTESIAN_POINT('Origin',(89.5,-21.0741207385024,36.1978257430375));
#16827=CARTESIAN_POINT('Origin',(-90.,18.5453000725091,36.1978257430375));
#16828=CARTESIAN_POINT('',(-89.5,18.5453000725091,35.6978257430375));
#16829=CARTESIAN_POINT('',(-90.,18.5453000725091,35.6978257430375));
#16830=CARTESIAN_POINT('',(-89.5,19.0453000725091,36.1978257430375));
#16831=CARTESIAN_POINT('Origin',(-89.5,18.5453000725091,36.1978257430375));
#16832=CARTESIAN_POINT('',(-90.,19.0453000725091,36.1978257430375));
#16833=CARTESIAN_POINT('Origin',(-90.,18.5453000725091,36.1978257430375));
#16834=CARTESIAN_POINT('',(-90.,18.5453000725091,35.6978257430375));
#16835=CARTESIAN_POINT('',(-90.,19.0453000725091,36.1978257430375));
#16836=CARTESIAN_POINT('Origin',(-90.,18.5453000725091,36.1978257430375));
#16837=CARTESIAN_POINT('',(89.5,19.045300072509,36.1978257430375));
#16838=CARTESIAN_POINT('',(-90.,19.0453000725091,36.1978257430375));
#16839=CARTESIAN_POINT('',(89.5,18.545300072509,35.6978257430375));
#16840=CARTESIAN_POINT('Origin',(89.5,18.545300072509,36.1978257430375));
#16841=CARTESIAN_POINT('',(-90.,18.5453000725091,35.6978257430375));
#16842=CARTESIAN_POINT('Origin',(-90.,18.5453000725091,36.1978257430375));
#16843=CARTESIAN_POINT('',(-90.,19.0453000725091,36.1978257430375));
#16844=CARTESIAN_POINT('',(-90.,18.5453000725091,35.6978257430375));
#16845=CARTESIAN_POINT('Origin',(-90.,18.5453000725091,36.1978257430375));
#16846=CARTESIAN_POINT('',(-90.,18.5453000725091,35.6978257430375));
#16847=CARTESIAN_POINT('',(-90.,19.0453000725091,36.1978257430375));
#16848=CARTESIAN_POINT('Origin',(-90.,19.0453000725091,47.6978257430375));
#16849=CARTESIAN_POINT('',(-89.5,19.0453000725091,47.1978257430375));
#16850=CARTESIAN_POINT('',(-89.5,19.0453000725091,49.8489128715187));
#16851=CARTESIAN_POINT('',(-90.,19.0453000725091,47.1978257430375));
#16852=CARTESIAN_POINT('Origin',(-90.,19.0453000725091,47.6978257430375));
#16853=CARTESIAN_POINT('',(-90.,19.0453000725091,47.1978257430375));
#16854=CARTESIAN_POINT('Origin',(-90.,19.0453000725091,47.6978257430375));
#16855=CARTESIAN_POINT('',(89.5,19.045300072509,47.1978257430375));
#16856=CARTESIAN_POINT('',(-90.,19.0453000725091,47.1978257430375));
#16857=CARTESIAN_POINT('',(89.5,19.045300072509,49.8489128715187));
#16858=CARTESIAN_POINT('Origin',(-90.,19.0453000725091,47.6978257430375));
#16859=CARTESIAN_POINT('',(-90.,19.0453000725091,47.1978257430375));
#16860=CARTESIAN_POINT('Origin',(-90.,19.0453000725091,47.6978257430375));
#16861=CARTESIAN_POINT('',(-90.,19.0453000725091,47.1978257430375));
#16862=CARTESIAN_POINT('Origin',(-45.,23.0395928638606,51.5));
#16863=CARTESIAN_POINT('',(-89.5,22.6860394732674,51.1464466094067));
#16864=CARTESIAN_POINT('',(-45.,22.6860394732673,51.1464466094067));
#16865=CARTESIAN_POINT('',(-89.5,23.0395928638606,52.));
#16866=CARTESIAN_POINT('Origin',(-89.5,23.0395928638606,51.5));
#16867=CARTESIAN_POINT('',(-45.,23.0395928638606,52.));
#16868=CARTESIAN_POINT('Origin',(-45.,23.0395928638606,51.5));
#16869=CARTESIAN_POINT('',(-45.,22.6860394732673,51.1464466094067));
#16870=CARTESIAN_POINT('',(-45.,23.0395928638606,52.));
#16871=CARTESIAN_POINT('Origin',(-45.,23.0395928638606,51.5));
#16872=CARTESIAN_POINT('',(89.5,23.0395928638606,52.));
#16873=CARTESIAN_POINT('',(-45.,23.0395928638606,52.));
#16874=CARTESIAN_POINT('',(89.5,22.6860394732673,51.1464466094067));
#16875=CARTESIAN_POINT('Origin',(89.5,23.0395928638606,51.5));
#16876=CARTESIAN_POINT('',(-45.,22.6860394732673,51.1464466094067));
#16877=CARTESIAN_POINT('Origin',(-45.,23.0395928638606,51.5));
#16878=CARTESIAN_POINT('',(-45.,23.0395928638606,52.));
#16879=CARTESIAN_POINT('',(-45.,22.6860394732673,51.1464466094067));
#16880=CARTESIAN_POINT('Origin',(-90.,19.5453000725091,47.1978257430375));
#16881=CARTESIAN_POINT('',(-89.5,19.5453000725091,47.6978257430375));
#16882=CARTESIAN_POINT('Origin',(-89.5,19.5453000725091,47.1978257430375));
#16883=CARTESIAN_POINT('',(-90.,19.5453000725091,47.6978257430375));
#16884=CARTESIAN_POINT('Origin',(-90.,19.5453000725091,47.1978257430375));
#16885=CARTESIAN_POINT('',(-90.,19.5453000725091,47.6978257430375));
#16886=CARTESIAN_POINT('Origin',(-90.,19.5453000725091,47.1978257430375));
#16887=CARTESIAN_POINT('',(89.5,19.545300072509,47.6978257430375));
#16888=CARTESIAN_POINT('',(-90.,19.5453000725091,47.6978257430375));
#16889=CARTESIAN_POINT('Origin',(89.5,19.545300072509,47.1978257430375));
#16890=CARTESIAN_POINT('Origin',(-90.,19.5453000725091,47.1978257430375));
#16891=CARTESIAN_POINT('',(-90.,19.5453000725091,47.6978257430375));
#16892=CARTESIAN_POINT('Origin',(-90.,19.5453000725091,47.1978257430375));
#16893=CARTESIAN_POINT('',(-90.,19.5453000725091,47.6978257430375));
#16894=CARTESIAN_POINT('Origin',(-90.,21.8324860826741,52.));
#16895=CARTESIAN_POINT('',(-89.5,25.2811069490433,48.5513791336308));
#16896=CARTESIAN_POINT('',(-90.,25.2811069490433,48.5513791336308));
#16897=CARTESIAN_POINT('',(-89.5,32.6243645620056,41.2081215206685));
#16898=CARTESIAN_POINT('Origin',(-90.,21.8324860826741,52.));
#16899=CARTESIAN_POINT('',(-90.,25.2811069490433,48.5513791336308));
#16900=CARTESIAN_POINT('Origin',(-90.,21.8324860826741,52.));
#16901=CARTESIAN_POINT('',(89.5,25.2811069490433,48.5513791336308));
#16902=CARTESIAN_POINT('',(89.5,0.124364562005535,73.7081215206685));
#16903=CARTESIAN_POINT('',(-90.,25.2811069490433,48.5513791336308));
#16904=CARTESIAN_POINT('Origin',(-90.,21.8324860826741,52.));
#16905=CARTESIAN_POINT('',(-90.,25.2811069490433,48.5513791336308));
#16906=CARTESIAN_POINT('Origin',(-90.,26.1346603396366,47.6978257430375));
#16907=CARTESIAN_POINT('',(89.5,24.92755355845,47.6978257430375));
#16908=CARTESIAN_POINT('',(-90.,24.92755355845,47.6978257430375));
#16909=CARTESIAN_POINT('',(89.5,-19.4326698301817,47.6978257430375));
#16910=CARTESIAN_POINT('Origin',(-90.,26.1346603396366,47.6978257430375));
#16911=CARTESIAN_POINT('',(-89.5,24.92755355845,47.6978257430375));
#16912=CARTESIAN_POINT('',(-89.5,45.5673301698183,47.6978257430375));
#16913=CARTESIAN_POINT('',(-90.,24.92755355845,47.6978257430375));
#16914=CARTESIAN_POINT('Origin',(-90.,26.1346603396366,47.6978257430375));
#16915=CARTESIAN_POINT('',(-90.,24.92755355845,47.6978257430375));
#16916=CARTESIAN_POINT('Origin',(-90.,26.1346603396366,47.6978257430375));
#16917=CARTESIAN_POINT('',(-90.,24.92755355845,47.6978257430375));
#16918=CARTESIAN_POINT('Origin',(-90.,24.92755355845,48.1978257430375));
#16919=CARTESIAN_POINT('Origin',(-89.5,24.92755355845,48.1978257430375));
#16920=CARTESIAN_POINT('Origin',(-90.,24.92755355845,48.1978257430375));
#16921=CARTESIAN_POINT('Origin',(-90.,24.92755355845,48.1978257430375));
#16922=CARTESIAN_POINT('Origin',(89.5,24.92755355845,48.1978257430375));
#16923=CARTESIAN_POINT('Origin',(-90.,24.92755355845,48.1978257430375));
#16924=CARTESIAN_POINT('Origin',(0.,0.,52.));
#16925=CARTESIAN_POINT('',(-45.,-45.3272645584124,52.));
#16926=CARTESIAN_POINT('',(-45.,-45.3272645584124,52.));
#16927=CARTESIAN_POINT('',(-45.,-45.3272645584124,52.));
#16928=CARTESIAN_POINT('',(-45.,-45.3272645584124,52.));
#16929=CARTESIAN_POINT('',(89.5,-45.3272645584125,52.));
#16930=CARTESIAN_POINT('',(-45.,-45.3272645584124,52.));
#16931=CARTESIAN_POINT('',(89.5,-64.5,52.));
#16932=CARTESIAN_POINT('',(89.5,-32.5,52.));
#16933=CARTESIAN_POINT('',(-89.5,-64.5,52.));
#16934=CARTESIAN_POINT('',(-45.,-64.5,52.));
#16935=CARTESIAN_POINT('',(-89.5,32.5,52.));
#16936=CARTESIAN_POINT('Origin',(-45.,-45.3272645584124,51.5));
#16937=CARTESIAN_POINT('',(-45.,-44.8272645584124,51.5));
#16938=CARTESIAN_POINT('Origin',(-45.,-45.3272645584124,51.5));
#16939=CARTESIAN_POINT('',(89.5,-44.8272645584125,51.5));
#16940=CARTESIAN_POINT('',(-45.,-44.8272645584124,51.5));
#16941=CARTESIAN_POINT('Origin',(89.5,-45.3272645584125,51.5));
#16942=CARTESIAN_POINT('Origin',(-45.,-45.3272645584124,51.5));
#16943=CARTESIAN_POINT('',(-45.,-44.8272645584124,51.5));
#16944=CARTESIAN_POINT('Origin',(-45.,-45.3272645584124,51.5));
#16945=CARTESIAN_POINT('',(-45.,-44.8272645584124,51.5));
#16946=CARTESIAN_POINT('Origin',(-45.,-45.3272645584124,51.5));
#16947=CARTESIAN_POINT('',(-45.,-44.8272645584124,51.5));
#16948=CARTESIAN_POINT('Origin',(-90.,-44.8272645584124,47.6978257430375));
#16949=CARTESIAN_POINT('',(89.5,-44.8272645584125,48.1978257430375));
#16950=CARTESIAN_POINT('',(-90.,-44.8272645584124,48.1978257430375));
#16951=CARTESIAN_POINT('',(89.5,-44.8272645584125,49.8489128715187));
#16952=CARTESIAN_POINT('Origin',(-90.,-44.8272645584124,47.6978257430375));
#16953=CARTESIAN_POINT('',(-90.,-44.8272645584124,48.1978257430375));
#16954=CARTESIAN_POINT('Origin',(-90.,-44.8272645584124,47.6978257430375));
#16955=CARTESIAN_POINT('',(-90.,-44.8272645584124,48.1978257430375));
#16956=CARTESIAN_POINT('Origin',(-90.,-44.8272645584124,47.6978257430375));
#16957=CARTESIAN_POINT('',(-90.,-44.8272645584124,48.1978257430375));
#16958=CARTESIAN_POINT('Origin',(-90.,-44.3272645584124,48.1978257430375));
#16959=CARTESIAN_POINT('Origin',(-90.,-44.3272645584124,48.1978257430375));
#16960=CARTESIAN_POINT('Origin',(89.5,-44.3272645584125,48.1978257430375));
#16961=CARTESIAN_POINT('Origin',(-90.,-44.3272645584124,48.1978257430375));
#16962=CARTESIAN_POINT('Origin',(-90.,-44.3272645584124,48.1978257430375));
#16963=CARTESIAN_POINT('Origin',(-90.,19.0453000725091,35.6978257430375));
#16964=CARTESIAN_POINT('',(-90.,-21.0741207385023,35.6978257430375));
#16965=CARTESIAN_POINT('',(-89.5,42.0226500362545,35.6978257430375));
#16966=CARTESIAN_POINT('',(89.5,-22.9773499637455,35.6978257430375));
#16967=CARTESIAN_POINT('Origin',(0.,0.,52.));
#16968=CARTESIAN_POINT('',(-45.,23.0395928638606,52.));
#16969=CARTESIAN_POINT('',(-89.5,64.5,52.));
#16970=CARTESIAN_POINT('',(-89.5,32.5,52.));
#16971=CARTESIAN_POINT('',(89.5,64.5,52.));
#16972=CARTESIAN_POINT('',(45.,64.5,52.));
#16973=CARTESIAN_POINT('',(89.5,-32.5,52.));
#16974=CARTESIAN_POINT('Origin',(89.5,24.92755355845,48.1978257430375));
#16975=CARTESIAN_POINT('',(90.,24.92755355845,48.1978257430375));
#16976=CARTESIAN_POINT('Origin',(89.5,24.92755355845,48.1978257430375));
#16977=CARTESIAN_POINT('Origin',(89.5,24.92755355845,48.1978257430375));
#16978=CARTESIAN_POINT('Origin',(-89.5,24.92755355845,48.1978257430375));
#16979=CARTESIAN_POINT('',(-90.,24.92755355845,48.1978257430375));
#16980=CARTESIAN_POINT('Origin',(-89.5,24.92755355845,48.1978257430375));
#16981=CARTESIAN_POINT('Origin',(-89.5,24.92755355845,48.1978257430375));
#16982=CARTESIAN_POINT('Origin',(89.5,19.545300072509,47.1978257430375));
#16983=CARTESIAN_POINT('',(90.,19.545300072509,48.1978257430375));
#16984=CARTESIAN_POINT('Origin',(89.5,19.545300072509,48.1978257430375));
#16985=CARTESIAN_POINT('',(90.,18.545300072509,47.1978257430375));
#16986=CARTESIAN_POINT('Origin',(90.,19.545300072509,47.1978257430375));
#16987=CARTESIAN_POINT('Origin',(89.5,18.545300072509,47.1978257430375));
#16988=CARTESIAN_POINT('Origin',(89.5,-19.4326698301817,48.1978257430375));
#16989=CARTESIAN_POINT('',(90.,-19.4326698301817,48.1978257430375));
#16990=CARTESIAN_POINT('Origin',(89.5,23.0395928638606,51.5));
#16991=CARTESIAN_POINT('',(90.,23.0395928638606,52.5));
#16992=CARTESIAN_POINT('',(90.,22.3324860826741,50.7928932188135));
#16993=CARTESIAN_POINT('Origin',(90.,23.0395928638606,51.5));
#16994=CARTESIAN_POINT('Origin',(89.5,22.332486082674,50.7928932188135));
#16995=CARTESIAN_POINT('Origin',(89.5,23.0395928638606,52.5));
#16996=CARTESIAN_POINT('Origin',(-89.5,19.5453000725091,47.1978257430375));
#16997=CARTESIAN_POINT('',(-90.,18.5453000725091,47.1978257430375));
#16998=CARTESIAN_POINT('Origin',(-89.5,18.5453000725091,47.1978257430375));
#16999=CARTESIAN_POINT('',(-90.,19.5453000725091,48.1978257430375));
#17000=CARTESIAN_POINT('Origin',(-90.,19.5453000725091,47.1978257430375));
#17001=CARTESIAN_POINT('Origin',(-89.5,19.5453000725091,48.1978257430375));
#17002=CARTESIAN_POINT('Origin',(-89.5,23.0395928638606,51.5));
#17003=CARTESIAN_POINT('',(-90.,22.3324860826741,50.7928932188135));
#17004=CARTESIAN_POINT('',(-90.,23.0395928638606,52.5));
#17005=CARTESIAN_POINT('Origin',(-90.,23.0395928638606,51.5));
#17006=CARTESIAN_POINT('Origin',(-89.5,23.0395928638606,52.5));
#17007=CARTESIAN_POINT('Origin',(-89.5,22.3324860826741,50.7928932188135));
#17008=CARTESIAN_POINT('Origin',(-89.5,32.2708111714123,40.8545681300752));
#17009=CARTESIAN_POINT('',(-90.,32.2708111714123,40.8545681300752));
#17010=CARTESIAN_POINT('Origin',(89.5,18.545300072509,36.1978257430375));
#17011=CARTESIAN_POINT('',(90.,18.545300072509,36.1978257430375));
#17012=CARTESIAN_POINT('Origin',(89.5,18.545300072509,36.1978257430375));
#17013=CARTESIAN_POINT('Origin',(89.5,18.545300072509,36.1978257430375));
#17014=CARTESIAN_POINT('Origin',(89.5,18.545300072509,49.8489128715187));
#17015=CARTESIAN_POINT('',(90.,18.545300072509,49.8489128715187));
#17016=CARTESIAN_POINT('Origin',(89.5,64.5,52.5));
#17017=CARTESIAN_POINT('',(90.,64.5,52.5));
#17018=CARTESIAN_POINT('',(89.5,65.,52.5));
#17019=CARTESIAN_POINT('Origin',(89.5,64.5,52.5));
#17020=CARTESIAN_POINT('Origin',(89.5,64.5,52.5));
#17021=CARTESIAN_POINT('Origin',(89.5,64.5,52.5));
#17022=CARTESIAN_POINT('Origin',(89.5,-32.5,52.5));
#17023=CARTESIAN_POINT('',(90.,-32.5,52.5));
#17024=CARTESIAN_POINT('Origin',(-89.5,18.5453000725091,36.1978257430375));
#17025=CARTESIAN_POINT('',(-90.,18.5453000725091,36.1978257430375));
#17026=CARTESIAN_POINT('Origin',(-89.5,18.5453000725091,36.1978257430375));
#17027=CARTESIAN_POINT('Origin',(-89.5,18.5453000725091,36.1978257430375));
#17028=CARTESIAN_POINT('Origin',(-89.5,64.5,52.5));
#17029=CARTESIAN_POINT('',(-89.5,65.,52.5));
#17030=CARTESIAN_POINT('Origin',(-89.5,64.5,52.5));
#17031=CARTESIAN_POINT('',(-90.,64.5,52.5));
#17032=CARTESIAN_POINT('Origin',(-89.5,64.5,52.5));
#17033=CARTESIAN_POINT('Origin',(-89.5,64.5,52.5));
#17034=CARTESIAN_POINT('Origin',(-89.5,32.5,52.5));
#17035=CARTESIAN_POINT('',(-90.,32.5,52.5));
#17036=CARTESIAN_POINT('Origin',(89.5,-21.0741207385024,36.1978257430375));
#17037=CARTESIAN_POINT('',(90.,-21.0741207385024,36.1978257430375));
#17038=CARTESIAN_POINT('Origin',(89.5,-21.0741207385024,36.1978257430375));
#17039=CARTESIAN_POINT('Origin',(89.5,-21.0741207385024,36.1978257430375));
#17040=CARTESIAN_POINT('Origin',(89.5,-22.9773499637455,36.1978257430375));
#17041=CARTESIAN_POINT('',(90.,-22.9773499637455,36.1978257430375));
#17042=CARTESIAN_POINT('Origin',(89.5,64.5,63.5));
#17043=CARTESIAN_POINT('',(90.,64.5,63.5));
#17044=CARTESIAN_POINT('',(89.5,64.5,64.));
#17045=CARTESIAN_POINT('Origin',(89.5,64.5,63.5));
#17046=CARTESIAN_POINT('',(89.5,65.,63.5));
#17047=CARTESIAN_POINT('Origin',(89.5,64.5,63.5));
#17048=CARTESIAN_POINT('Origin',(89.5,64.5,63.5));
#17049=CARTESIAN_POINT('Origin',(89.5,64.5,52.));
#17050=CARTESIAN_POINT('',(90.,64.5,52.));
#17051=CARTESIAN_POINT('',(89.5,65.,52.));
#17052=CARTESIAN_POINT('Origin',(-89.5,-21.0741207385023,36.1978257430375));
#17053=CARTESIAN_POINT('',(-90.,-21.0741207385023,36.1978257430375));
#17054=CARTESIAN_POINT('Origin',(-89.5,-21.0741207385023,36.1978257430375));
#17055=CARTESIAN_POINT('Origin',(-89.5,-21.0741207385023,36.1978257430375));
#17056=CARTESIAN_POINT('Origin',(-89.5,64.5,63.5));
#17057=CARTESIAN_POINT('',(-89.5,65.,63.5));
#17058=CARTESIAN_POINT('',(-89.5,64.5,64.));
#17059=CARTESIAN_POINT('Origin',(-89.5,64.5,63.5));
#17060=CARTESIAN_POINT('',(-90.,64.5,63.5));
#17061=CARTESIAN_POINT('Origin',(-89.5,64.5,63.5));
#17062=CARTESIAN_POINT('Origin',(-89.5,64.5,63.5));
#17063=CARTESIAN_POINT('Origin',(-89.5,64.5,52.));
#17064=CARTESIAN_POINT('',(-89.5,65.,52.));
#17065=CARTESIAN_POINT('',(-90.,64.5,52.));
#17066=CARTESIAN_POINT('Origin',(89.5,-22.0741207385024,47.1978257430375));
#17067=CARTESIAN_POINT('',(90.,-21.0741207385024,47.1978257430375));
#17068=CARTESIAN_POINT('Origin',(89.5,-21.0741207385024,47.1978257430375));
#17069=CARTESIAN_POINT('',(90.,-22.0741207385024,48.1978257430375));
#17070=CARTESIAN_POINT('Origin',(90.,-22.0741207385024,47.1978257430375));
#17071=CARTESIAN_POINT('Origin',(89.5,-22.0741207385024,48.1978257430375));
#17072=CARTESIAN_POINT('Origin',(89.5,-21.0741207385024,43.8489128715187));
#17073=CARTESIAN_POINT('',(90.,-21.0741207385024,43.8489128715187));
#17074=CARTESIAN_POINT('Origin',(89.5,-64.5,63.5));
#17075=CARTESIAN_POINT('',(89.5,-65.,63.5));
#17076=CARTESIAN_POINT('',(89.5,-64.5,64.));
#17077=CARTESIAN_POINT('Origin',(89.5,-64.5,63.5));
#17078=CARTESIAN_POINT('',(90.,-64.5,63.5));
#17079=CARTESIAN_POINT('Origin',(89.5,-64.5,63.5));
#17080=CARTESIAN_POINT('Origin',(89.5,-64.5,63.5));
#17081=CARTESIAN_POINT('Origin',(-89.5,-22.0741207385023,47.1978257430375));
#17082=CARTESIAN_POINT('',(-90.,-22.0741207385023,48.1978257430375));
#17083=CARTESIAN_POINT('Origin',(-89.5,-22.0741207385023,48.1978257430375));
#17084=CARTESIAN_POINT('',(-90.,-21.0741207385023,47.1978257430375));
#17085=CARTESIAN_POINT('Origin',(-90.,-22.0741207385023,47.1978257430375));
#17086=CARTESIAN_POINT('Origin',(-89.5,-21.0741207385023,47.1978257430375));
#17087=CARTESIAN_POINT('Origin',(-89.5,-64.5,63.5));
#17088=CARTESIAN_POINT('',(-90.,-64.5,63.5));
#17089=CARTESIAN_POINT('',(-89.5,-64.5,64.));
#17090=CARTESIAN_POINT('Origin',(-89.5,-64.5,63.5));
#17091=CARTESIAN_POINT('',(-89.5,-65.,63.5));
#17092=CARTESIAN_POINT('Origin',(-89.5,-64.5,63.5));
#17093=CARTESIAN_POINT('Origin',(-89.5,-64.5,63.5));
#17094=CARTESIAN_POINT('Origin',(89.5,-44.3272645584125,48.1978257430375));
#17095=CARTESIAN_POINT('',(90.,-44.3272645584125,48.1978257430375));
#17096=CARTESIAN_POINT('Origin',(89.5,-44.3272645584125,48.1978257430375));
#17097=CARTESIAN_POINT('Origin',(89.5,-44.3272645584125,48.1978257430375));
#17098=CARTESIAN_POINT('Origin',(89.5,-43.2870603692512,48.1978257430375));
#17099=CARTESIAN_POINT('',(90.,-43.2870603692512,48.1978257430375));
#17100=CARTESIAN_POINT('Origin',(89.5,-64.5,52.5));
#17101=CARTESIAN_POINT('',(89.5,-65.,52.5));
#17102=CARTESIAN_POINT('',(90.,-64.5,52.5));
#17103=CARTESIAN_POINT('Origin',(89.5,-64.5,52.5));
#17104=CARTESIAN_POINT('Origin',(89.5,-64.5,52.5));
#17105=CARTESIAN_POINT('Origin',(89.5,-64.5,52.5));
#17106=CARTESIAN_POINT('Origin',(-89.5,-44.3272645584124,48.1978257430375));
#17107=CARTESIAN_POINT('',(-90.,-44.3272645584124,48.1978257430375));
#17108=CARTESIAN_POINT('Origin',(-89.5,-44.3272645584124,48.1978257430375));
#17109=CARTESIAN_POINT('Origin',(-89.5,-44.3272645584124,48.1978257430375));
#17110=CARTESIAN_POINT('Origin',(-89.5,-64.5,52.5));
#17111=CARTESIAN_POINT('',(-90.,-64.5,52.5));
#17112=CARTESIAN_POINT('',(-89.5,-65.,52.5));
#17113=CARTESIAN_POINT('Origin',(-89.5,-64.5,52.5));
#17114=CARTESIAN_POINT('Origin',(-89.5,-64.5,52.5));
#17115=CARTESIAN_POINT('Origin',(-89.5,-64.5,52.5));
#17116=CARTESIAN_POINT('Origin',(89.5,-45.3272645584125,51.5));
#17117=CARTESIAN_POINT('',(90.,-44.3272645584125,51.5));
#17118=CARTESIAN_POINT('Origin',(89.5,-44.3272645584125,51.5));
#17119=CARTESIAN_POINT('',(90.,-45.3272645584125,52.5));
#17120=CARTESIAN_POINT('Origin',(90.,-45.3272645584125,51.5));
#17121=CARTESIAN_POINT('Origin',(89.5,-45.3272645584125,52.5));
#17122=CARTESIAN_POINT('Origin',(89.5,-44.3272645584125,49.8489128715187));
#17123=CARTESIAN_POINT('',(90.,-44.3272645584125,49.8489128715187));
#17124=CARTESIAN_POINT('Origin',(89.5,-32.5,52.5));
#17125=CARTESIAN_POINT('',(90.,-32.5,52.5));
#17126=CARTESIAN_POINT('Origin',(-89.5,-45.3272645584124,51.5));
#17127=CARTESIAN_POINT('',(-90.,-45.3272645584124,52.5));
#17128=CARTESIAN_POINT('Origin',(-89.5,-45.3272645584124,52.5));
#17129=CARTESIAN_POINT('',(-90.,-44.3272645584124,51.5));
#17130=CARTESIAN_POINT('Origin',(-90.,-45.3272645584124,51.5));
#17131=CARTESIAN_POINT('Origin',(-89.5,-44.3272645584124,51.5));
#17132=CARTESIAN_POINT('Origin',(-89.5,32.5,52.5));
#17133=CARTESIAN_POINT('',(-90.,32.5,52.5));
#17134=CARTESIAN_POINT('Origin',(-89.5,-44.3272645584124,49.8489128715187));
#17135=CARTESIAN_POINT('',(-90.,-44.3272645584124,49.8489128715187));
#17136=CARTESIAN_POINT('Origin',(-45.,-64.5,52.5));
#17137=CARTESIAN_POINT('',(-45.,-65.,52.5));
#17138=CARTESIAN_POINT('Origin',(-89.5,-64.5,52.));
#17139=CARTESIAN_POINT('',(-90.,-64.5,52.));
#17140=CARTESIAN_POINT('',(-89.5,-65.,52.));
#17141=CARTESIAN_POINT('Origin',(-89.5,21.7129396307488,48.1978257430375));
#17142=CARTESIAN_POINT('',(-90.,21.7129396307488,48.1978257430375));
#17143=CARTESIAN_POINT('Origin',(-90.,-44.3272645584124,48.1978257430375));
#17144=CARTESIAN_POINT('',(-90.,-44.8272645584124,48.1978257430375));
#17145=CARTESIAN_POINT('Origin',(89.5,-64.5,52.));
#17146=CARTESIAN_POINT('',(89.5,-65.,52.));
#17147=CARTESIAN_POINT('',(90.,-64.5,52.));
#17148=CARTESIAN_POINT('Origin',(-45.,-64.5,63.5));
#17149=CARTESIAN_POINT('',(-45.,-64.5,64.));
#17150=CARTESIAN_POINT('',(-45.,-65.,63.5));
#17151=CARTESIAN_POINT('Origin',(-89.5,32.5,63.5));
#17152=CARTESIAN_POINT('',(-89.5,32.5,64.));
#17153=CARTESIAN_POINT('',(-90.,32.5,63.5));
#17154=CARTESIAN_POINT('Origin',(-89.5,-21.0741207385023,43.8489128715187));
#17155=CARTESIAN_POINT('',(-90.,-21.0741207385023,43.8489128715187));
#17156=CARTESIAN_POINT('Origin',(89.5,-32.5,63.5));
#17157=CARTESIAN_POINT('',(89.5,-32.5,64.));
#17158=CARTESIAN_POINT('',(90.,-32.5,63.5));
#17159=CARTESIAN_POINT('Origin',(45.,64.5,63.5));
#17160=CARTESIAN_POINT('',(45.,64.5,64.));
#17161=CARTESIAN_POINT('',(45.,65.,63.5));
#17162=CARTESIAN_POINT('Origin',(-89.5,42.0226500362545,36.1978257430375));
#17163=CARTESIAN_POINT('',(-90.,42.0226500362545,36.1978257430375));
#17164=CARTESIAN_POINT('Origin',(-90.,-21.0741207385023,36.1978257430375));
#17165=CARTESIAN_POINT('',(-90.,-21.5741207385023,36.1978257430375));
#17166=CARTESIAN_POINT('Origin',(45.,64.5,52.5));
#17167=CARTESIAN_POINT('',(45.,65.,52.5));
#17168=CARTESIAN_POINT('Origin',(-89.5,18.5453000725091,49.8489128715187));
#17169=CARTESIAN_POINT('',(-90.,18.5453000725091,49.8489128715187));
#17170=CARTESIAN_POINT('Origin',(-45.,23.0395928638606,51.5));
#17171=CARTESIAN_POINT('',(-45.,22.6860394732673,51.1464466094067));
#17172=CARTESIAN_POINT('Origin',(-89.5,45.5673301698183,48.1978257430375));
#17173=CARTESIAN_POINT('',(-90.,45.5673301698183,48.1978257430375));
#17174=CARTESIAN_POINT('Origin',(89.5,-0.229188828587741,73.3545681300752));
#17175=CARTESIAN_POINT('',(90.,-0.229188828587741,73.3545681300752));
#17176=CARTESIAN_POINT('Origin',(-90.,24.92755355845,48.1978257430375));
#17177=CARTESIAN_POINT('',(-90.,24.92755355845,47.6978257430375));
#17178=CARTESIAN_POINT('',(-90.,25.2811069490433,48.5513791336308));
#17179=CARTESIAN_POINT('Origin',(-90.,65.,52.));
#17180=CARTESIAN_POINT('Origin',(-90.,21.8324860826741,52.));
#17181=CARTESIAN_POINT('Origin',(90.,65.,52.));
#17182=CARTESIAN_POINT('Origin',(-90.,-44.8272645584124,47.6978257430375));
#17183=CARTESIAN_POINT('Origin',(-90.,-65.,52.));
#17184=CARTESIAN_POINT('Origin',(0.,0.,64.));
#17185=CARTESIAN_POINT('Origin',(-90.,-21.5741207385023,35.6978257430375));
#17186=CARTESIAN_POINT('Origin',(-90.,26.1346603396366,47.6978257430375));
#17187=CARTESIAN_POINT('Origin',(90.,-65.,52.));
#17819=UNCERTAINTY_MEASURE_WITH_UNIT(LENGTH_MEASURE(0.01),#17837,
'DISTANCE_ACCURACY_VALUE',
'Maximum model space distance between geometric entities at asserted c
onnectivities');
#17824=UNCERTAINTY_MEASURE_WITH_UNIT(LENGTH_MEASURE(0.01),#17837,
'DISTANCE_ACCURACY_VALUE',
'Maximum model space distance between geometric entities at asserted c
onnectivities');
#17831=(
GEOMETRIC_REPRESENTATION_CONTEXT(3)
GLOBAL_UNCERTAINTY_ASSIGNED_CONTEXT((#17819))
GLOBAL_UNIT_ASSIGNED_CONTEXT((#17837,#17839,#17840))
REPRESENTATION_CONTEXT('','3D')
);
#17836=(
GEOMETRIC_REPRESENTATION_CONTEXT(3)
GLOBAL_UNCERTAINTY_ASSIGNED_CONTEXT((#17824))
GLOBAL_UNIT_ASSIGNED_CONTEXT((#17837,#17839,#17840))
REPRESENTATION_CONTEXT('','3D')
);
#17837=(
LENGTH_UNIT()
NAMED_UNIT(*)
SI_UNIT(.MILLI.,.METRE.)
);
#17839=(
NAMED_UNIT(*)
PLANE_ANGLE_UNIT()
SI_UNIT($,.RADIAN.)
);
#17840=(
NAMED_UNIT(*)
SI_UNIT($,.STERADIAN.)
SOLID_ANGLE_UNIT()
);
#17847=SHAPE_DEFINITION_REPRESENTATION(#17858,#17879);
#17858=PRODUCT_DEFINITION_SHAPE('',$,#17891);
#17879=SHAPE_REPRESENTATION('',(#10399),#17831);
#17884=PRODUCT_DEFINITION_CONTEXT('part definition',#17919,'design');
#17891=PRODUCT_DEFINITION('Moving_Carriage_01','Moving_Carriage_01',#17902,
#17884);
#17902=PRODUCT_DEFINITION_FORMATION('',$,#17927);
#17919=APPLICATION_CONTEXT(
'Core Data for Automotive Mechanical Design Process');
#17920=PRODUCT_CONTEXT('part definition',#17919,'mechanical');
#17927=PRODUCT('Moving_Carriage_01','Moving_Carriage_01',$,(#17920));
#17953=COLOUR_RGB('Light Blue',0.38,0.62,0.78);
#17954=FILL_AREA_STYLE_COLOUR('',#17953);
#17955=FILL_AREA_STYLE('',(#17954));
#17956=SURFACE_STYLE_FILL_AREA(#17955);
#17957=SURFACE_SIDE_STYLE('',(#17956));
#17958=SURFACE_STYLE_USAGE(.BOTH.,#17957);
#17959=PRESENTATION_STYLE_ASSIGNMENT((#17958));
ENDSEC;
END-ISO-10303-21;
